ISO-10303-21;
HEADER;
/* Generated by software containing ST-Developer
 * from STEP Tools, Inc. (www.steptools.com) 
 */

FILE_DESCRIPTION(
/* description */ ('Independent four-jaw lathe chuck,200mm body,40mm bore,36\X2\2013\X0\7
6mm nominal opposed jaw opening. Four shared machined T-jaws and model
ed partial M12x1.75 feed screws, native independent screw/slider links
, removable bolted bronze-bearing cartridges, fully captured ring/wash
er/head thrust stacks and registered bolted backplate. Custom spindle 
interface; no compatibility, speed, grip force or safety rating assign
ed.'),
/* implementation_level */ '2;1');

FILE_NAME(
/* name */ 'Socket head cap screw M6x40.step',
/* time_stamp */ '2026-11-09T20:24:54-08:00',
/* author */ (''),
/* organization */ (''),
/* preprocessor_version */ 'ST-DEVELOPER v20.2',
/* originating_system */ 'Autodesk Translation Framework v15.17.0.0',
/* authorisation */ '');

FILE_SCHEMA (('AUTOMOTIVE_DESIGN { 1 0 10303 214 3 1 1 }'));
ENDSEC;

DATA;
#10=MECHANICAL_DESIGN_GEOMETRIC_PRESENTATION_REPRESENTATION('',(#244),#69491);
#211=CONICAL_SURFACE('',#15696,2.5,0.785398163397448);
#222=SHAPE_REPRESENTATION_RELATIONSHIP('SRR','None',#69579,#233);
#233=ADVANCED_BREP_SHAPE_REPRESENTATION('',(#255),#69488);
#244=STYLED_ITEM('',(#69640),#255);
#255=MANIFOLD_SOLID_BREP('Body1',#14739);
#294=B_SPLINE_SURFACE_WITH_KNOTS('',3,3,((#62492,#62493,#62494,#62495,#62496,
#62497,#62498,#62499,#62500,#62501,#62502,#62503,#62504,#62505,#62506,#62507,
#62508,#62509,#62510,#62511,#62512,#62513,#62514,#62515,#62516,#62517,#62518,
#62519,#62520,#62521,#62522,#62523,#62524,#62525,#62526,#62527,#62528,#62529,
#62530,#62531,#62532,#62533,#62534,#62535,#62536,#62537,#62538,#62539,#62540,
#62541,#62542,#62543,#62544,#62545,#62546,#62547,#62548,#62549,#62550,#62551,
#62552,#62553,#62554,#62555,#62556,#62557,#62558,#62559,#62560,#62561,#62562,
#62563,#62564,#62565,#62566,#62567,#62568,#62569,#62570,#62571,#62572,#62573,
#62574,#62575,#62576,#62577,#62578,#62579,#62580,#62581,#62582,#62583,#62584,
#62585,#62586,#62587,#62588,#62589,#62590,#62591,#62592,#62593,#62594,#62595,
#62596,#62597,#62598,#62599,#62600,#62601,#62602,#62603,#62604,#62605,#62606,
#62607,#62608,#62609,#62610,#62611,#62612,#62613,#62614,#62615,#62616,#62617,
#62618,#62619,#62620,#62621,#62622,#62623,#62624,#62625,#62626,#62627,#62628,
#62629,#62630,#62631,#62632,#62633,#62634,#62635,#62636,#62637,#62638,#62639,
#62640,#62641,#62642,#62643,#62644,#62645,#62646,#62647,#62648,#62649,#62650,
#62651,#62652,#62653,#62654,#62655,#62656,#62657,#62658,#62659,#62660,#62661,
#62662,#62663,#62664,#62665,#62666,#62667,#62668,#62669,#62670,#62671,#62672,
#62673,#62674,#62675,#62676,#62677,#62678,#62679,#62680,#62681,#62682,#62683,
#62684,#62685,#62686,#62687,#62688,#62689,#62690,#62691,#62692,#62693,#62694,
#62695,#62696,#62697,#62698,#62699,#62700,#62701,#62702,#62703,#62704,#62705,
#62706,#62707,#62708,#62709,#62710,#62711,#62712,#62713,#62714,#62715,#62716,
#62717,#62718,#62719,#62720,#62721,#62722,#62723,#62724,#62725,#62726,#62727,
#62728,#62729,#62730,#62731,#62732,#62733,#62734,#62735,#62736,#62737,#62738,
#62739,#62740,#62741,#62742,#62743),(#62744,#62745,#62746,#62747,#62748,
#62749,#62750,#62751,#62752,#62753,#62754,#62755,#62756,#62757,#62758,#62759,
#62760,#62761,#62762,#62763,#62764,#62765,#62766,#62767,#62768,#62769,#62770,
#62771,#62772,#62773,#62774,#62775,#62776,#62777,#62778,#62779,#62780,#62781,
#62782,#62783,#62784,#62785,#62786,#62787,#62788,#62789,#62790,#62791,#62792,
#62793,#62794,#62795,#62796,#62797,#62798,#62799,#62800,#62801,#62802,#62803,
#62804,#62805,#62806,#62807,#62808,#62809,#62810,#62811,#62812,#62813,#62814,
#62815,#62816,#62817,#62818,#62819,#62820,#62821,#62822,#62823,#62824,#62825,
#62826,#62827,#62828,#62829,#62830,#62831,#62832,#62833,#62834,#62835,#62836,
#62837,#62838,#62839,#62840,#62841,#62842,#62843,#62844,#62845,#62846,#62847,
#62848,#62849,#62850,#62851,#62852,#62853,#62854,#62855,#62856,#62857,#62858,
#62859,#62860,#62861,#62862,#62863,#62864,#62865,#62866,#62867,#62868,#62869,
#62870,#62871,#62872,#62873,#62874,#62875,#62876,#62877,#62878,#62879,#62880,
#62881,#62882,#62883,#62884,#62885,#62886,#62887,#62888,#62889,#62890,#62891,
#62892,#62893,#62894,#62895,#62896,#62897,#62898,#62899,#62900,#62901,#62902,
#62903,#62904,#62905,#62906,#62907,#62908,#62909,#62910,#62911,#62912,#62913,
#62914,#62915,#62916,#62917,#62918,#62919,#62920,#62921,#62922,#62923,#62924,
#62925,#62926,#62927,#62928,#62929,#62930,#62931,#62932,#62933,#62934,#62935,
#62936,#62937,#62938,#62939,#62940,#62941,#62942,#62943,#62944,#62945,#62946,
#62947,#62948,#62949,#62950,#62951,#62952,#62953,#62954,#62955,#62956,#62957,
#62958,#62959,#62960,#62961,#62962,#62963,#62964,#62965,#62966,#62967,#62968,
#62969,#62970,#62971,#62972,#62973,#62974,#62975,#62976,#62977,#62978,#62979,
#62980,#62981,#62982,#62983,#62984,#62985,#62986,#62987,#62988,#62989,#62990,
#62991,#62992,#62993,#62994,#62995),(#62996,#62997,#62998,#62999,#63000,
#63001,#63002,#63003,#63004,#63005,#63006,#63007,#63008,#63009,#63010,#63011,
#63012,#63013,#63014,#63015,#63016,#63017,#63018,#63019,#63020,#63021,#63022,
#63023,#63024,#63025,#63026,#63027,#63028,#63029,#63030,#63031,#63032,#63033,
#63034,#63035,#63036,#63037,#63038,#63039,#63040,#63041,#63042,#63043,#63044,
#63045,#63046,#63047,#63048,#63049,#63050,#63051,#63052,#63053,#63054,#63055,
#63056,#63057,#63058,#63059,#63060,#63061,#63062,#63063,#63064,#63065,#63066,
#63067,#63068,#63069,#63070,#63071,#63072,#63073,#63074,#63075,#63076,#63077,
#63078,#63079,#63080,#63081,#63082,#63083,#63084,#63085,#63086,#63087,#63088,
#63089,#63090,#63091,#63092,#63093,#63094,#63095,#63096,#63097,#63098,#63099,
#63100,#63101,#63102,#63103,#63104,#63105,#63106,#63107,#63108,#63109,#63110,
#63111,#63112,#63113,#63114,#63115,#63116,#63117,#63118,#63119,#63120,#63121,
#63122,#63123,#63124,#63125,#63126,#63127,#63128,#63129,#63130,#63131,#63132,
#63133,#63134,#63135,#63136,#63137,#63138,#63139,#63140,#63141,#63142,#63143,
#63144,#63145,#63146,#63147,#63148,#63149,#63150,#63151,#63152,#63153,#63154,
#63155,#63156,#63157,#63158,#63159,#63160,#63161,#63162,#63163,#63164,#63165,
#63166,#63167,#63168,#63169,#63170,#63171,#63172,#63173,#63174,#63175,#63176,
#63177,#63178,#63179,#63180,#63181,#63182,#63183,#63184,#63185,#63186,#63187,
#63188,#63189,#63190,#63191,#63192,#63193,#63194,#63195,#63196,#63197,#63198,
#63199,#63200,#63201,#63202,#63203,#63204,#63205,#63206,#63207,#63208,#63209,
#63210,#63211,#63212,#63213,#63214,#63215,#63216,#63217,#63218,#63219,#63220,
#63221,#63222,#63223,#63224,#63225,#63226,#63227,#63228,#63229,#63230,#63231,
#63232,#63233,#63234,#63235,#63236,#63237,#63238,#63239,#63240,#63241,#63242,
#63243,#63244,#63245,#63246,#63247),(#63248,#63249,#63250,#63251,#63252,
#63253,#63254,#63255,#63256,#63257,#63258,#63259,#63260,#63261,#63262,#63263,
#63264,#63265,#63266,#63267,#63268,#63269,#63270,#63271,#63272,#63273,#63274,
#63275,#63276,#63277,#63278,#63279,#63280,#63281,#63282,#63283,#63284,#63285,
#63286,#63287,#63288,#63289,#63290,#63291,#63292,#63293,#63294,#63295,#63296,
#63297,#63298,#63299,#63300,#63301,#63302,#63303,#63304,#63305,#63306,#63307,
#63308,#63309,#63310,#63311,#63312,#63313,#63314,#63315,#63316,#63317,#63318,
#63319,#63320,#63321,#63322,#63323,#63324,#63325,#63326,#63327,#63328,#63329,
#63330,#63331,#63332,#63333,#63334,#63335,#63336,#63337,#63338,#63339,#63340,
#63341,#63342,#63343,#63344,#63345,#63346,#63347,#63348,#63349,#63350,#63351,
#63352,#63353,#63354,#63355,#63356,#63357,#63358,#63359,#63360,#63361,#63362,
#63363,#63364,#63365,#63366,#63367,#63368,#63369,#63370,#63371,#63372,#63373,
#63374,#63375,#63376,#63377,#63378,#63379,#63380,#63381,#63382,#63383,#63384,
#63385,#63386,#63387,#63388,#63389,#63390,#63391,#63392,#63393,#63394,#63395,
#63396,#63397,#63398,#63399,#63400,#63401,#63402,#63403,#63404,#63405,#63406,
#63407,#63408,#63409,#63410,#63411,#63412,#63413,#63414,#63415,#63416,#63417,
#63418,#63419,#63420,#63421,#63422,#63423,#63424,#63425,#63426,#63427,#63428,
#63429,#63430,#63431,#63432,#63433,#63434,#63435,#63436,#63437,#63438,#63439,
#63440,#63441,#63442,#63443,#63444,#63445,#63446,#63447,#63448,#63449,#63450,
#63451,#63452,#63453,#63454,#63455,#63456,#63457,#63458,#63459,#63460,#63461,
#63462,#63463,#63464,#63465,#63466,#63467,#63468,#63469,#63470,#63471,#63472,
#63473,#63474,#63475,#63476,#63477,#63478,#63479,#63480,#63481,#63482,#63483,
#63484,#63485,#63486,#63487,#63488,#63489,#63490,#63491,#63492,#63493,#63494,
#63495,#63496,#63497,#63498,#63499)),.UNSPECIFIED.,.F.,.F.,.F.,(4,4),(4,
1,1,1,1,1,1,1,1,1,1,1,1,1,1,1,1,1,1,1,1,1,1,1,1,1,1,1,1,1,1,1,1,1,1,1,1,
1,1,1,1,1,1,1,1,1,1,1,1,1,1,1,1,1,1,1,1,1,1,1,1,1,1,1,1,1,1,1,1,1,1,1,1,
1,1,1,1,1,1,1,1,1,1,1,1,1,1,1,1,1,1,1,1,1,1,1,1,1,1,1,1,1,1,1,1,1,1,1,1,
1,1,1,1,1,1,1,1,1,1,1,1,1,1,1,1,1,1,1,1,1,1,1,1,1,1,1,1,1,1,1,1,1,1,1,1,
1,1,1,1,1,1,1,1,1,1,1,1,1,1,1,1,1,1,1,1,1,1,1,1,1,1,1,1,1,1,1,1,1,1,1,1,
1,1,1,1,1,1,1,1,1,1,1,1,1,1,1,1,1,1,1,1,1,1,1,1,1,1,1,1,1,1,1,1,1,1,1,1,
1,1,1,1,1,1,1,1,1,1,1,1,1,1,1,1,1,1,1,1,1,1,1,1,1,1,1,1,1,1,1,1,4),(0.,
0.0658467982010768),(11.6150328478187,12.6149992660887,13.6149656843588,
14.6149321026288,15.6148985208988,16.6148649391689,17.6148313574389,18.614797775709,
19.614764193979,20.614730612249,21.6146970305191,22.6146634487891,23.6146298670591,
24.6145962853292,25.6145627035992,26.6145291218693,27.6144955401393,28.6144619584093,
29.6144283766794,30.6143947949494,31.6143612132194,32.6143276314895,33.6142940497595,
34.6142604680296,35.6142268862996,36.6141933045696,37.6141597228397,38.6141261411097,
39.6140925593798,40.6140589776498,41.6140253959198,42.6139918141899,43.6139582324599,
44.6139246507299,45.613891069,46.61385748727,47.6138239055401,48.6137903238101,
49.6137567420801,50.6137231603502,51.6136895786202,52.6136559968902,53.6136224151603,
54.6135888334303,55.6135552517004,56.6135216699704,57.6134880882404,58.6134545065105,
59.6134209247805,60.6133873430505,61.6133537613206,62.6133201795906,63.6132865978607,
64.6132530161307,65.6132194344007,66.6131858526708,67.6131522709408,68.6131186892109,
69.6130851074809,70.6130515257509,71.613017944021,72.612984362291,73.612950780561,
74.6129171988311,75.6128836171011,76.6128500353712,77.6128164536412,78.6127828719112,
79.6127492901813,80.6127157084513,81.6126821267214,82.6126485449914,83.6126149632614,
84.6125813815315,85.6125477998015,86.6125142180715,87.6124806363416,88.6124470546116,
89.6124134728817,90.6123798911517,91.6123463094217,92.6123127276918,93.6122791459618,
94.6122455642318,95.6122119825019,96.6121784007719,97.612144819042,98.612111237312,
99.612077655582,100.612044073852,101.612010492122,102.611976910392,103.611943328662,
104.611909746932,105.611876165202,106.611842583472,107.611809001742,108.611775420012,
109.611741838282,110.611708256552,111.611674674822,112.611641093093,113.611607511363,
114.611573929633,115.611540347903,116.611506766173,117.611473184443,118.611439602713,
119.611406020983,120.611372439253,121.611338857523,122.611305275793,123.611271694063,
124.611238112333,125.611204530603,126.611170948873,127.611137367143,128.611103785413,
129.611070203683,130.611036621953,131.611003040223,132.610969458493,133.610935876763,
134.610902295033,135.610868713303,136.610835131573,137.610801549843,138.610767968113,
139.610734386384,140.610700804654,141.610667222924,142.610633641194,143.610600059464,
144.610566477734,145.610532896004,146.610499314274,147.610465732544,148.610432150814,
149.610398569084,150.610364987354,151.610331405624,152.610297823894,153.610264242164,
154.610230660434,155.610197078704,156.610163496974,157.610129915244,158.610096333514,
159.610062751784,160.610029170054,161.609995588324,162.609962006594,163.609928424864,
164.609894843134,165.609861261405,166.609827679675,167.609794097945,168.609760516215,
169.609726934485,170.609693352755,171.609659771025,172.609626189295,173.609592607565,
174.609559025835,175.609525444105,176.609491862375,177.609458280645,178.609424698915,
179.609391117185,180.609357535455,181.609323953725,182.609290371995,183.609256790265,
184.609223208535,185.609189626805,186.609156045075,187.609122463345,188.609088881615,
189.609055299885,190.609021718155,191.608988136425,192.608954554696,193.608920972966,
194.608887391236,195.608853809506,196.608820227776,197.608786646046,198.608753064316,
199.608719482586,200.608685900856,201.608652319126,202.608618737396,203.608585155666,
204.608551573936,205.608517992206,206.608484410476,207.608450828746,208.608417247016,
209.608383665286,210.608350083556,211.608316501826,212.608282920096,213.608249338366,
214.608215756636,215.608182174906,216.608148593176,217.608115011447,218.608081429717,
219.608047847987,220.608014266257,221.607980684527,222.607947102797,223.607913521067,
224.607879939337,225.607846357607,226.607812775877,227.607779194147,228.607745612417,
229.607712030687,230.607678448957,231.607644867227,232.607611285497,233.607577703767,
234.607544122037,235.607510540307,236.607476958577,237.607443376847,238.607409795117,
239.607376213387,240.607342631657,241.607309049927,242.607275468197,243.607241886467,
244.607208304738,245.607174723008,246.607141141278,247.607107559548,248.607073977818,
249.607040396088,250.607006814358,251.606973232628,252.606939650898,253.606906069168,
254.606872487438,255.606838905708,256.606805323978,257.606771742248,258.606738160518,
259.606704578788,260.606670997058),.UNSPECIFIED.);
#295=B_SPLINE_SURFACE_WITH_KNOTS('',3,3,((#63634,#63635,#63636,#63637,#63638,
#63639,#63640,#63641,#63642,#63643,#63644,#63645,#63646,#63647,#63648,#63649,
#63650,#63651,#63652,#63653,#63654,#63655,#63656,#63657,#63658,#63659,#63660,
#63661,#63662,#63663,#63664,#63665,#63666,#63667,#63668,#63669,#63670,#63671,
#63672,#63673,#63674,#63675,#63676,#63677,#63678,#63679,#63680,#63681,#63682,
#63683,#63684,#63685,#63686,#63687,#63688,#63689,#63690,#63691,#63692,#63693,
#63694,#63695,#63696,#63697,#63698,#63699,#63700,#63701,#63702,#63703,#63704,
#63705,#63706,#63707,#63708,#63709,#63710,#63711,#63712,#63713,#63714,#63715,
#63716,#63717,#63718,#63719,#63720,#63721,#63722,#63723,#63724,#63725,#63726,
#63727,#63728,#63729,#63730,#63731,#63732,#63733,#63734,#63735,#63736,#63737,
#63738,#63739,#63740,#63741,#63742,#63743,#63744,#63745,#63746,#63747,#63748,
#63749,#63750,#63751,#63752,#63753,#63754,#63755,#63756,#63757,#63758,#63759,
#63760,#63761,#63762,#63763,#63764,#63765,#63766,#63767,#63768,#63769,#63770,
#63771,#63772,#63773,#63774,#63775,#63776,#63777,#63778,#63779,#63780,#63781,
#63782,#63783,#63784,#63785,#63786,#63787,#63788,#63789,#63790,#63791,#63792,
#63793,#63794,#63795,#63796,#63797,#63798,#63799,#63800,#63801,#63802,#63803,
#63804,#63805,#63806,#63807,#63808,#63809,#63810,#63811,#63812,#63813,#63814,
#63815,#63816,#63817,#63818,#63819,#63820,#63821,#63822,#63823,#63824,#63825,
#63826,#63827,#63828,#63829,#63830,#63831,#63832,#63833,#63834,#63835,#63836,
#63837,#63838,#63839,#63840,#63841,#63842,#63843,#63844,#63845,#63846,#63847,
#63848,#63849,#63850,#63851,#63852,#63853,#63854,#63855,#63856,#63857,#63858,
#63859,#63860,#63861,#63862,#63863,#63864,#63865,#63866,#63867,#63868,#63869,
#63870,#63871,#63872,#63873,#63874,#63875,#63876,#63877,#63878,#63879,#63880,
#63881,#63882,#63883,#63884,#63885,#63886,#63887,#63888),(#63889,#63890,
#63891,#63892,#63893,#63894,#63895,#63896,#63897,#63898,#63899,#63900,#63901,
#63902,#63903,#63904,#63905,#63906,#63907,#63908,#63909,#63910,#63911,#63912,
#63913,#63914,#63915,#63916,#63917,#63918,#63919,#63920,#63921,#63922,#63923,
#63924,#63925,#63926,#63927,#63928,#63929,#63930,#63931,#63932,#63933,#63934,
#63935,#63936,#63937,#63938,#63939,#63940,#63941,#63942,#63943,#63944,#63945,
#63946,#63947,#63948,#63949,#63950,#63951,#63952,#63953,#63954,#63955,#63956,
#63957,#63958,#63959,#63960,#63961,#63962,#63963,#63964,#63965,#63966,#63967,
#63968,#63969,#63970,#63971,#63972,#63973,#63974,#63975,#63976,#63977,#63978,
#63979,#63980,#63981,#63982,#63983,#63984,#63985,#63986,#63987,#63988,#63989,
#63990,#63991,#63992,#63993,#63994,#63995,#63996,#63997,#63998,#63999,#64000,
#64001,#64002,#64003,#64004,#64005,#64006,#64007,#64008,#64009,#64010,#64011,
#64012,#64013,#64014,#64015,#64016,#64017,#64018,#64019,#64020,#64021,#64022,
#64023,#64024,#64025,#64026,#64027,#64028,#64029,#64030,#64031,#64032,#64033,
#64034,#64035,#64036,#64037,#64038,#64039,#64040,#64041,#64042,#64043,#64044,
#64045,#64046,#64047,#64048,#64049,#64050,#64051,#64052,#64053,#64054,#64055,
#64056,#64057,#64058,#64059,#64060,#64061,#64062,#64063,#64064,#64065,#64066,
#64067,#64068,#64069,#64070,#64071,#64072,#64073,#64074,#64075,#64076,#64077,
#64078,#64079,#64080,#64081,#64082,#64083,#64084,#64085,#64086,#64087,#64088,
#64089,#64090,#64091,#64092,#64093,#64094,#64095,#64096,#64097,#64098,#64099,
#64100,#64101,#64102,#64103,#64104,#64105,#64106,#64107,#64108,#64109,#64110,
#64111,#64112,#64113,#64114,#64115,#64116,#64117,#64118,#64119,#64120,#64121,
#64122,#64123,#64124,#64125,#64126,#64127,#64128,#64129,#64130,#64131,#64132,
#64133,#64134,#64135,#64136,#64137,#64138,#64139,#64140,#64141,#64142,#64143),
(#64144,#64145,#64146,#64147,#64148,#64149,#64150,#64151,#64152,#64153,
#64154,#64155,#64156,#64157,#64158,#64159,#64160,#64161,#64162,#64163,#64164,
#64165,#64166,#64167,#64168,#64169,#64170,#64171,#64172,#64173,#64174,#64175,
#64176,#64177,#64178,#64179,#64180,#64181,#64182,#64183,#64184,#64185,#64186,
#64187,#64188,#64189,#64190,#64191,#64192,#64193,#64194,#64195,#64196,#64197,
#64198,#64199,#64200,#64201,#64202,#64203,#64204,#64205,#64206,#64207,#64208,
#64209,#64210,#64211,#64212,#64213,#64214,#64215,#64216,#64217,#64218,#64219,
#64220,#64221,#64222,#64223,#64224,#64225,#64226,#64227,#64228,#64229,#64230,
#64231,#64232,#64233,#64234,#64235,#64236,#64237,#64238,#64239,#64240,#64241,
#64242,#64243,#64244,#64245,#64246,#64247,#64248,#64249,#64250,#64251,#64252,
#64253,#64254,#64255,#64256,#64257,#64258,#64259,#64260,#64261,#64262,#64263,
#64264,#64265,#64266,#64267,#64268,#64269,#64270,#64271,#64272,#64273,#64274,
#64275,#64276,#64277,#64278,#64279,#64280,#64281,#64282,#64283,#64284,#64285,
#64286,#64287,#64288,#64289,#64290,#64291,#64292,#64293,#64294,#64295,#64296,
#64297,#64298,#64299,#64300,#64301,#64302,#64303,#64304,#64305,#64306,#64307,
#64308,#64309,#64310,#64311,#64312,#64313,#64314,#64315,#64316,#64317,#64318,
#64319,#64320,#64321,#64322,#64323,#64324,#64325,#64326,#64327,#64328,#64329,
#64330,#64331,#64332,#64333,#64334,#64335,#64336,#64337,#64338,#64339,#64340,
#64341,#64342,#64343,#64344,#64345,#64346,#64347,#64348,#64349,#64350,#64351,
#64352,#64353,#64354,#64355,#64356,#64357,#64358,#64359,#64360,#64361,#64362,
#64363,#64364,#64365,#64366,#64367,#64368,#64369,#64370,#64371,#64372,#64373,
#64374,#64375,#64376,#64377,#64378,#64379,#64380,#64381,#64382,#64383,#64384,
#64385,#64386,#64387,#64388,#64389,#64390,#64391,#64392,#64393,#64394,#64395,
#64396,#64397,#64398),(#64399,#64400,#64401,#64402,#64403,#64404,#64405,
#64406,#64407,#64408,#64409,#64410,#64411,#64412,#64413,#64414,#64415,#64416,
#64417,#64418,#64419,#64420,#64421,#64422,#64423,#64424,#64425,#64426,#64427,
#64428,#64429,#64430,#64431,#64432,#64433,#64434,#64435,#64436,#64437,#64438,
#64439,#64440,#64441,#64442,#64443,#64444,#64445,#64446,#64447,#64448,#64449,
#64450,#64451,#64452,#64453,#64454,#64455,#64456,#64457,#64458,#64459,#64460,
#64461,#64462,#64463,#64464,#64465,#64466,#64467,#64468,#64469,#64470,#64471,
#64472,#64473,#64474,#64475,#64476,#64477,#64478,#64479,#64480,#64481,#64482,
#64483,#64484,#64485,#64486,#64487,#64488,#64489,#64490,#64491,#64492,#64493,
#64494,#64495,#64496,#64497,#64498,#64499,#64500,#64501,#64502,#64503,#64504,
#64505,#64506,#64507,#64508,#64509,#64510,#64511,#64512,#64513,#64514,#64515,
#64516,#64517,#64518,#64519,#64520,#64521,#64522,#64523,#64524,#64525,#64526,
#64527,#64528,#64529,#64530,#64531,#64532,#64533,#64534,#64535,#64536,#64537,
#64538,#64539,#64540,#64541,#64542,#64543,#64544,#64545,#64546,#64547,#64548,
#64549,#64550,#64551,#64552,#64553,#64554,#64555,#64556,#64557,#64558,#64559,
#64560,#64561,#64562,#64563,#64564,#64565,#64566,#64567,#64568,#64569,#64570,
#64571,#64572,#64573,#64574,#64575,#64576,#64577,#64578,#64579,#64580,#64581,
#64582,#64583,#64584,#64585,#64586,#64587,#64588,#64589,#64590,#64591,#64592,
#64593,#64594,#64595,#64596,#64597,#64598,#64599,#64600,#64601,#64602,#64603,
#64604,#64605,#64606,#64607,#64608,#64609,#64610,#64611,#64612,#64613,#64614,
#64615,#64616,#64617,#64618,#64619,#64620,#64621,#64622,#64623,#64624,#64625,
#64626,#64627,#64628,#64629,#64630,#64631,#64632,#64633,#64634,#64635,#64636,
#64637,#64638,#64639,#64640,#64641,#64642,#64643,#64644,#64645,#64646,#64647,
#64648,#64649,#64650,#64651,#64652,#64653)),.UNSPECIFIED.,.F.,.F.,.F.,(4,
4),(4,1,1,1,1,1,1,1,1,1,1,1,1,1,1,1,1,1,1,1,1,1,1,1,1,1,1,1,1,1,1,1,1,1,
1,1,1,1,1,1,1,1,1,1,1,1,1,1,1,1,1,1,1,1,1,1,1,1,1,1,1,1,1,1,1,1,1,1,1,1,
1,1,1,1,1,1,1,1,1,1,1,1,1,1,1,1,1,1,1,1,1,1,1,1,1,1,1,1,1,1,1,1,1,1,1,1,
1,1,1,1,1,1,1,1,1,1,1,1,1,1,1,1,1,1,1,1,1,1,1,1,1,1,1,1,1,1,1,1,1,1,1,1,
1,1,1,1,1,1,1,1,1,1,1,1,1,1,1,1,1,1,1,1,1,1,1,1,1,1,1,1,1,1,1,1,1,1,1,1,
1,1,1,1,1,1,1,1,1,1,1,1,1,1,1,1,1,1,1,1,1,1,1,1,1,1,1,1,1,1,1,1,1,1,1,1,
1,1,1,1,1,1,1,1,1,1,1,1,1,1,1,1,1,1,1,1,1,1,1,1,1,1,1,1,1,1,1,1,1,1,1,1,
1,1,4),(0.,0.0658467982010768),(8.30747755240138,9.30374849019562,10.3000194279899,
11.2962903657841,12.2925613035783,13.2888322413726,14.2851031791668,15.2813741169611,
16.2776450547553,17.2739159925495,18.2701869303438,19.266457868138,20.2627288059323,
21.2589997437265,22.2552706815207,23.251541619315,24.2478125571092,25.2440834949035,
26.2403544326977,27.236625370492,28.2328963082862,29.2291672460804,30.2254381838747,
31.2217091216689,32.2179800594632,33.2142509972574,34.2105219350516,35.2067928728459,
36.2030638106401,37.1993347484344,38.1956056862286,39.1918766240228,40.1881475618171,
41.1844184996113,42.1806894374056,43.1769603751998,44.1732313129941,45.1695022507883,
46.1657731885825,47.1620441263768,48.158315064171,49.1545860019653,50.1508569397595,
51.1471278775537,52.143398815348,53.1396697531422,54.1359406909365,55.1322116287307,
56.1284825665249,57.1247535043192,58.1210244421134,59.1172953799077,60.1135663177019,
61.1098372554961,62.1061081932904,63.1023791310846,64.0986500688789,65.0949210066731,
66.0911919444674,67.0874628822616,68.0837338200558,69.0800047578501,70.0762756956443,
71.0725466334385,72.0688175712328,73.065088509027,74.0613594468213,75.0576303846155,
76.0539013224098,77.050172260204,78.0464431979982,79.0427141357925,80.0389850735867,
81.035256011381,82.0315269491752,83.0277978869695,84.0240688247637,85.0203397625579,
86.0166107003522,87.0128816381464,88.0091525759407,89.0054235137349,90.0016944515291,
90.9979653893234,91.9942363271176,92.9905072649119,93.9867782027061,94.9830491405003,
95.9793200782946,96.9755910160888,97.9718619538831,98.9681328916773,99.9644038294716,
100.960674767266,101.95694570506,102.953216642854,103.949487580649,104.945758518443,
105.942029456237,106.938300394031,107.934571331825,108.93084226962,109.927113207414,
110.923384145208,111.919655083002,112.915926020797,113.912196958591,114.908467896385,
115.904738834179,116.901009771974,117.897280709768,118.893551647562,119.889822585356,
120.886093523151,121.882364460945,122.878635398739,123.874906336533,124.871177274328,
125.867448212122,126.863719149916,127.85999008771,128.856261025505,129.852531963299,
130.848802901093,131.845073838887,132.841344776681,133.837615714476,134.83388665227,
135.830157590064,136.826428527858,137.822699465653,138.818970403447,139.815241341241,
140.811512279035,141.80778321683,142.804054154624,143.800325092418,144.796596030212,
145.792866968007,146.789137905801,147.785408843595,148.781679781389,149.777950719184,
150.774221656978,151.770492594772,152.766763532566,153.763034470361,154.759305408155,
155.755576345949,156.751847283743,157.748118221538,158.744389159332,159.740660097126,
160.73693103492,161.733201972714,162.729472910509,163.725743848303,164.722014786097,
165.718285723891,166.714556661686,167.71082759948,168.707098537274,169.703369475068,
170.699640412863,171.695911350657,172.692182288451,173.688453226245,174.68472416404,
175.680995101834,176.677266039628,177.673536977422,178.669807915217,179.666078853011,
180.662349790805,181.658620728599,182.654891666394,183.651162604188,184.647433541982,
185.643704479776,186.63997541757,187.636246355365,188.632517293159,189.628788230953,
190.625059168747,191.621330106542,192.617601044336,193.61387198213,194.610142919924,
195.606413857719,196.602684795513,197.598955733307,198.595226671101,199.591497608896,
200.58776854669,201.584039484484,202.580310422278,203.576581360073,204.572852297867,
205.569123235661,206.565394173455,207.56166511125,208.557936049044,209.554206986838,
210.550477924632,211.546748862427,212.543019800221,213.539290738015,214.535561675809,
215.531832613603,216.528103551398,217.524374489192,218.520645426986,219.51691636478,
220.513187302575,221.509458240369,222.505729178163,223.502000115957,224.498271053752,
225.494541991546,226.49081292934,227.487083867134,228.483354804929,229.479625742723,
230.475896680517,231.472167618311,232.468438556106,233.4647094939,234.460980431694,
235.457251369488,236.453522307283,237.449793245077,238.446064182871,239.442335120665,
240.438606058459,241.434876996254,242.431147934048,243.427418871842,244.423689809636,
245.419960747431,246.416231685225,247.412502623019,248.408773560813,249.405044498608,
250.401315436402,251.397586374196,252.39385731199,253.390128249785,254.386399187579,
255.382670125373,256.378941063167,257.375212000962,258.371482938756,259.36775387655),
 .UNSPECIFIED.);
#359=FACE_BOUND('',#2057,.T.);
#360=FACE_BOUND('',#2060,.T.);
#500=PLANE('',#15702);
#501=PLANE('',#15703);
#502=PLANE('',#15704);
#503=PLANE('',#15705);
#504=PLANE('',#15706);
#505=PLANE('',#15707);
#506=PLANE('',#15708);
#507=PLANE('',#15709);
#508=PLANE('',#15713);
#509=PLANE('',#15714);
#1124=FACE_OUTER_BOUND('',#1966,.T.);
#1125=FACE_OUTER_BOUND('',#1967,.T.);
#1126=FACE_OUTER_BOUND('',#1968,.T.);
#1127=FACE_OUTER_BOUND('',#1969,.T.);
#1128=FACE_OUTER_BOUND('',#1970,.T.);
#1129=FACE_OUTER_BOUND('',#1971,.T.);
#1130=FACE_OUTER_BOUND('',#1972,.T.);
#1131=FACE_OUTER_BOUND('',#1973,.T.);
#1132=FACE_OUTER_BOUND('',#1974,.T.);
#1133=FACE_OUTER_BOUND('',#1975,.T.);
#1134=FACE_OUTER_BOUND('',#1976,.T.);
#1135=FACE_OUTER_BOUND('',#1977,.T.);
#1136=FACE_OUTER_BOUND('',#1978,.T.);
#1137=FACE_OUTER_BOUND('',#1979,.T.);
#1138=FACE_OUTER_BOUND('',#1980,.T.);
#1139=FACE_OUTER_BOUND('',#1981,.T.);
#1140=FACE_OUTER_BOUND('',#1982,.T.);
#1141=FACE_OUTER_BOUND('',#1983,.T.);
#1142=FACE_OUTER_BOUND('',#1984,.T.);
#1143=FACE_OUTER_BOUND('',#1985,.T.);
#1144=FACE_OUTER_BOUND('',#1986,.T.);
#1145=FACE_OUTER_BOUND('',#1987,.T.);
#1146=FACE_OUTER_BOUND('',#1988,.T.);
#1147=FACE_OUTER_BOUND('',#1989,.T.);
#1148=FACE_OUTER_BOUND('',#1990,.T.);
#1149=FACE_OUTER_BOUND('',#1991,.T.);
#1150=FACE_OUTER_BOUND('',#1992,.T.);
#1151=FACE_OUTER_BOUND('',#1993,.T.);
#1152=FACE_OUTER_BOUND('',#1994,.T.);
#1153=FACE_OUTER_BOUND('',#1995,.T.);
#1154=FACE_OUTER_BOUND('',#1996,.T.);
#1155=FACE_OUTER_BOUND('',#1997,.T.);
#1156=FACE_OUTER_BOUND('',#1998,.T.);
#1157=FACE_OUTER_BOUND('',#1999,.T.);
#1158=FACE_OUTER_BOUND('',#2000,.T.);
#1159=FACE_OUTER_BOUND('',#2001,.T.);
#1160=FACE_OUTER_BOUND('',#2002,.T.);
#1161=FACE_OUTER_BOUND('',#2003,.T.);
#1162=FACE_OUTER_BOUND('',#2004,.T.);
#1163=FACE_OUTER_BOUND('',#2005,.T.);
#1164=FACE_OUTER_BOUND('',#2006,.T.);
#1165=FACE_OUTER_BOUND('',#2007,.T.);
#1166=FACE_OUTER_BOUND('',#2008,.T.);
#1167=FACE_OUTER_BOUND('',#2009,.T.);
#1168=FACE_OUTER_BOUND('',#2010,.T.);
#1169=FACE_OUTER_BOUND('',#2011,.T.);
#1170=FACE_OUTER_BOUND('',#2012,.T.);
#1171=FACE_OUTER_BOUND('',#2013,.T.);
#1172=FACE_OUTER_BOUND('',#2014,.T.);
#1173=FACE_OUTER_BOUND('',#2015,.T.);
#1174=FACE_OUTER_BOUND('',#2016,.T.);
#1175=FACE_OUTER_BOUND('',#2017,.T.);
#1176=FACE_OUTER_BOUND('',#2018,.T.);
#1177=FACE_OUTER_BOUND('',#2019,.T.);
#1178=FACE_OUTER_BOUND('',#2020,.T.);
#1179=FACE_OUTER_BOUND('',#2021,.T.);
#1180=FACE_OUTER_BOUND('',#2022,.T.);
#1181=FACE_OUTER_BOUND('',#2023,.T.);
#1182=FACE_OUTER_BOUND('',#2024,.T.);
#1183=FACE_OUTER_BOUND('',#2025,.T.);
#1184=FACE_OUTER_BOUND('',#2026,.T.);
#1185=FACE_OUTER_BOUND('',#2027,.T.);
#1186=FACE_OUTER_BOUND('',#2028,.T.);
#1187=FACE_OUTER_BOUND('',#2029,.T.);
#1188=FACE_OUTER_BOUND('',#2030,.T.);
#1189=FACE_OUTER_BOUND('',#2031,.T.);
#1190=FACE_OUTER_BOUND('',#2032,.T.);
#1191=FACE_OUTER_BOUND('',#2033,.T.);
#1192=FACE_OUTER_BOUND('',#2034,.T.);
#1193=FACE_OUTER_BOUND('',#2035,.T.);
#1194=FACE_OUTER_BOUND('',#2036,.T.);
#1195=FACE_OUTER_BOUND('',#2037,.T.);
#1196=FACE_OUTER_BOUND('',#2038,.T.);
#1197=FACE_OUTER_BOUND('',#2039,.T.);
#1198=FACE_OUTER_BOUND('',#2040,.T.);
#1199=FACE_OUTER_BOUND('',#2041,.T.);
#1200=FACE_OUTER_BOUND('',#2042,.T.);
#1201=FACE_OUTER_BOUND('',#2043,.T.);
#1202=FACE_OUTER_BOUND('',#2044,.T.);
#1203=FACE_OUTER_BOUND('',#2045,.T.);
#1204=FACE_OUTER_BOUND('',#2046,.T.);
#1205=FACE_OUTER_BOUND('',#2047,.T.);
#1206=FACE_OUTER_BOUND('',#2048,.T.);
#1207=FACE_OUTER_BOUND('',#2049,.T.);
#1208=FACE_OUTER_BOUND('',#2050,.T.);
#1209=FACE_OUTER_BOUND('',#2051,.T.);
#1210=FACE_OUTER_BOUND('',#2052,.T.);
#1211=FACE_OUTER_BOUND('',#2053,.T.);
#1212=FACE_OUTER_BOUND('',#2054,.T.);
#1213=FACE_OUTER_BOUND('',#2055,.T.);
#1214=FACE_OUTER_BOUND('',#2056,.T.);
#1215=FACE_OUTER_BOUND('',#2058,.T.);
#1216=FACE_OUTER_BOUND('',#2059,.T.);
#1217=FACE_OUTER_BOUND('',#2061,.T.);
#1966=EDGE_LOOP('',(#12359,#12360,#12361,#12362));
#1967=EDGE_LOOP('',(#12363,#12364,#12365,#12366));
#1968=EDGE_LOOP('',(#12367,#12368,#12369,#12370));
#1969=EDGE_LOOP('',(#12371,#12372,#12373,#12374));
#1970=EDGE_LOOP('',(#12375,#12376,#12377,#12378));
#1971=EDGE_LOOP('',(#12379,#12380,#12381,#12382));
#1972=EDGE_LOOP('',(#12383,#12384,#12385,#12386));
#1973=EDGE_LOOP('',(#12387,#12388,#12389,#12390));
#1974=EDGE_LOOP('',(#12391,#12392,#12393,#12394));
#1975=EDGE_LOOP('',(#12395,#12396,#12397,#12398));
#1976=EDGE_LOOP('',(#12399,#12400,#12401,#12402));
#1977=EDGE_LOOP('',(#12403,#12404,#12405,#12406));
#1978=EDGE_LOOP('',(#12407,#12408,#12409,#12410));
#1979=EDGE_LOOP('',(#12411,#12412,#12413,#12414));
#1980=EDGE_LOOP('',(#12415,#12416,#12417,#12418));
#1981=EDGE_LOOP('',(#12419,#12420,#12421,#12422));
#1982=EDGE_LOOP('',(#12423,#12424,#12425,#12426));
#1983=EDGE_LOOP('',(#12427,#12428,#12429,#12430));
#1984=EDGE_LOOP('',(#12431,#12432,#12433,#12434));
#1985=EDGE_LOOP('',(#12435,#12436,#12437,#12438));
#1986=EDGE_LOOP('',(#12439,#12440,#12441,#12442));
#1987=EDGE_LOOP('',(#12443,#12444,#12445,#12446));
#1988=EDGE_LOOP('',(#12447,#12448,#12449,#12450));
#1989=EDGE_LOOP('',(#12451,#12452,#12453,#12454));
#1990=EDGE_LOOP('',(#12455,#12456,#12457,#12458));
#1991=EDGE_LOOP('',(#12459,#12460,#12461,#12462));
#1992=EDGE_LOOP('',(#12463,#12464,#12465,#12466));
#1993=EDGE_LOOP('',(#12467,#12468,#12469,#12470));
#1994=EDGE_LOOP('',(#12471,#12472,#12473,#12474));
#1995=EDGE_LOOP('',(#12475,#12476,#12477,#12478));
#1996=EDGE_LOOP('',(#12479,#12480,#12481,#12482));
#1997=EDGE_LOOP('',(#12483,#12484,#12485,#12486));
#1998=EDGE_LOOP('',(#12487,#12488,#12489,#12490));
#1999=EDGE_LOOP('',(#12491,#12492,#12493,#12494));
#2000=EDGE_LOOP('',(#12495,#12496,#12497,#12498));
#2001=EDGE_LOOP('',(#12499,#12500,#12501,#12502));
#2002=EDGE_LOOP('',(#12503,#12504,#12505,#12506));
#2003=EDGE_LOOP('',(#12507,#12508,#12509,#12510));
#2004=EDGE_LOOP('',(#12511,#12512,#12513,#12514));
#2005=EDGE_LOOP('',(#12515,#12516,#12517,#12518));
#2006=EDGE_LOOP('',(#12519,#12520,#12521,#12522));
#2007=EDGE_LOOP('',(#12523,#12524,#12525,#12526));
#2008=EDGE_LOOP('',(#12527,#12528,#12529,#12530));
#2009=EDGE_LOOP('',(#12531,#12532,#12533,#12534));
#2010=EDGE_LOOP('',(#12535,#12536,#12537,#12538));
#2011=EDGE_LOOP('',(#12539,#12540,#12541,#12542));
#2012=EDGE_LOOP('',(#12543,#12544,#12545,#12546));
#2013=EDGE_LOOP('',(#12547,#12548,#12549,#12550));
#2014=EDGE_LOOP('',(#12551,#12552,#12553,#12554));
#2015=EDGE_LOOP('',(#12555,#12556,#12557,#12558));
#2016=EDGE_LOOP('',(#12559,#12560,#12561,#12562));
#2017=EDGE_LOOP('',(#12563,#12564,#12565,#12566));
#2018=EDGE_LOOP('',(#12567,#12568,#12569,#12570));
#2019=EDGE_LOOP('',(#12571,#12572,#12573,#12574));
#2020=EDGE_LOOP('',(#12575,#12576,#12577,#12578));
#2021=EDGE_LOOP('',(#12579,#12580,#12581,#12582));
#2022=EDGE_LOOP('',(#12583,#12584,#12585,#12586));
#2023=EDGE_LOOP('',(#12587,#12588,#12589,#12590));
#2024=EDGE_LOOP('',(#12591,#12592,#12593,#12594));
#2025=EDGE_LOOP('',(#12595,#12596,#12597,#12598));
#2026=EDGE_LOOP('',(#12599,#12600,#12601,#12602));
#2027=EDGE_LOOP('',(#12603,#12604,#12605,#12606));
#2028=EDGE_LOOP('',(#12607,#12608,#12609,#12610));
#2029=EDGE_LOOP('',(#12611,#12612,#12613,#12614));
#2030=EDGE_LOOP('',(#12615,#12616,#12617,#12618));
#2031=EDGE_LOOP('',(#12619,#12620,#12621,#12622));
#2032=EDGE_LOOP('',(#12623,#12624,#12625,#12626));
#2033=EDGE_LOOP('',(#12627,#12628,#12629,#12630));
#2034=EDGE_LOOP('',(#12631,#12632,#12633,#12634));
#2035=EDGE_LOOP('',(#12635,#12636,#12637,#12638));
#2036=EDGE_LOOP('',(#12639,#12640,#12641,#12642));
#2037=EDGE_LOOP('',(#12643,#12644,#12645,#12646));
#2038=EDGE_LOOP('',(#12647,#12648,#12649,#12650));
#2039=EDGE_LOOP('',(#12651,#12652,#12653,#12654));
#2040=EDGE_LOOP('',(#12655,#12656,#12657,#12658));
#2041=EDGE_LOOP('',(#12659,#12660,#12661,#12662));
#2042=EDGE_LOOP('',(#12663,#12664,#12665,#12666));
#2043=EDGE_LOOP('',(#12667,#12668,#12669,#12670));
#2044=EDGE_LOOP('',(#12671,#12672,#12673,#12674,#12675,#12676,#12677,#12678));
#2045=EDGE_LOOP('',(#12679,#12680,#12681,#12682,#12683,#12684,#12685,#12686,
#12687,#12688,#12689,#12690,#12691,#12692,#12693,#12694,#12695,#12696,#12697,
#12698,#12699,#12700,#12701,#12702,#12703,#12704,#12705,#12706,#12707,#12708,
#12709,#12710,#12711,#12712,#12713,#12714,#12715,#12716,#12717,#12718,#12719,
#12720,#12721,#12722,#12723,#12724,#12725,#12726,#12727,#12728,#12729,#12730,
#12731,#12732,#12733,#12734,#12735,#12736,#12737,#12738,#12739,#12740,#12741,
#12742,#12743,#12744,#12745,#12746,#12747,#12748,#12749,#12750,#12751,#12752,
#12753,#12754,#12755,#12756,#12757,#12758,#12759,#12760));
#2046=EDGE_LOOP('',(#12761,#12762,#12763,#12764));
#2047=EDGE_LOOP('',(#12765,#12766,#12767,#12768,#12769,#12770,#12771,#12772,
#12773,#12774,#12775,#12776,#12777,#12778,#12779,#12780,#12781,#12782,#12783,
#12784,#12785,#12786,#12787,#12788,#12789,#12790,#12791,#12792,#12793,#12794,
#12795,#12796,#12797,#12798,#12799,#12800,#12801,#12802,#12803,#12804,#12805,
#12806,#12807,#12808,#12809,#12810,#12811,#12812,#12813,#12814,#12815,#12816,
#12817,#12818,#12819,#12820,#12821,#12822,#12823,#12824,#12825,#12826,#12827,
#12828,#12829,#12830,#12831,#12832,#12833,#12834,#12835,#12836,#12837,#12838,
#12839,#12840,#12841,#12842,#12843,#12844,#12845,#12846,#12847));
#2048=EDGE_LOOP('',(#12848,#12849,#12850,#12851));
#2049=EDGE_LOOP('',(#12852,#12853,#12854,#12855));
#2050=EDGE_LOOP('',(#12856,#12857,#12858,#12859));
#2051=EDGE_LOOP('',(#12860,#12861,#12862,#12863));
#2052=EDGE_LOOP('',(#12864,#12865,#12866,#12867));
#2053=EDGE_LOOP('',(#12868,#12869,#12870,#12871));
#2054=EDGE_LOOP('',(#12872,#12873,#12874,#12875));
#2055=EDGE_LOOP('',(#12876,#12877,#12878,#12879,#12880,#12881));
#2056=EDGE_LOOP('',(#12882));
#2057=EDGE_LOOP('',(#12883,#12884,#12885,#12886));
#2058=EDGE_LOOP('',(#12887,#12888,#12889,#12890));
#2059=EDGE_LOOP('',(#12891));
#2060=EDGE_LOOP('',(#12892,#12893,#12894,#12895,#12896,#12897));
#2061=EDGE_LOOP('',(#12898));
#2327=CIRCLE('',#15617,2.942);
#2328=CIRCLE('',#15657,2.37175);
#2329=CIRCLE('',#15697,2.942);
#2330=CIRCLE('',#15698,2.);
#2331=CIRCLE('',#15700,2.37175);
#2332=CIRCLE('',#15710,5.);
#2333=CIRCLE('',#15712,5.);
#3227=B_SPLINE_CURVE_WITH_KNOTS('',3,(#59298,#59299,#59300,#59301,#59302,
#59303,#59304,#59305,#59306,#59307),.UNSPECIFIED.,.F.,.F.,(4,3,3,4),(-4.09293042013064,
-3.99986567308015,-2.99989925481011,-2.06863817490912),.UNSPECIFIED.);
#3228=B_SPLINE_CURVE_WITH_KNOTS('',3,(#59310,#59311,#59312,#59313,#59314,
#59315,#59316),.UNSPECIFIED.,.F.,.F.,(4,3,4),(0.,0.996270937794229,1.11730040836874),
 .UNSPECIFIED.);
#3229=B_SPLINE_CURVE_WITH_KNOTS('',3,(#59321,#59322,#59323,#59324,#59325,
#59326,#59327,#59328,#59329,#59330,#59331,#59332,#59333,#59334,#59335,#59336,
#59337,#59338,#59339,#59340,#59341,#59342),.UNSPECIFIED.,.F.,.F.,(4,3,3,
3,3,3,3,4),(-10.3761157273102,-9.99966418270038,-8.99969776443034,-7.9997313461603,
-6.99976492789026,-5.99979850962022,-4.99983209135019,-4.09293042013064),
 .UNSPECIFIED.);
#3230=B_SPLINE_CURVE_WITH_KNOTS('',3,(#59343,#59344,#59345,#59346,#59347,
#59348,#59349,#59350,#59351,#59352,#59353,#59354,#59355,#59356,#59357,#59358,
#59359,#59360,#59361,#59362,#59363,#59364),.UNSPECIFIED.,.F.,.F.,(4,3,3,
3,3,3,3,4),(1.11730040836874,1.99254187558847,2.98881281338272,3.98508375117696,
4.98135468897121,5.97762562676545,6.97389656455969,7.40048571554833),
 .UNSPECIFIED.);
#3231=B_SPLINE_CURVE_WITH_KNOTS('',3,(#59369,#59370,#59371,#59372,#59373,
#59374,#59375,#59376,#59377,#59378,#59379,#59380,#59381,#59382,#59383,#59384,
#59385,#59386,#59387,#59388,#59389,#59390),.UNSPECIFIED.,.F.,.F.,(4,3,3,
3,3,3,3,4),(-16.6593010344898,-15.9994626923206,-14.9994962740506,-13.9995298557805,
-12.9995634375105,-11.9995970192405,-10.9996306009704,-10.3761157273102),
 .UNSPECIFIED.);
#3232=B_SPLINE_CURVE_WITH_KNOTS('',3,(#59391,#59392,#59393,#59394,#59395,
#59396,#59397,#59398,#59399,#59400,#59401,#59402,#59403,#59404,#59405,#59406,
#59407,#59408,#59409,#59410,#59411,#59412),.UNSPECIFIED.,.F.,.F.,(4,3,3,
3,3,3,3,4),(7.40048571554833,7.97016750235394,8.96643844014818,9.96270937794242,
10.9589803157367,11.9552512535309,12.9515221913251,13.6836710227279),
 .UNSPECIFIED.);
#3233=B_SPLINE_CURVE_WITH_KNOTS('',3,(#59417,#59418,#59419,#59420,#59421,
#59422,#59423,#59424,#59425,#59426,#59427,#59428,#59429,#59430,#59431,#59432,
#59433,#59434,#59435,#59436,#59437,#59438),.UNSPECIFIED.,.F.,.F.,(4,3,3,
3,3,3,3,4),(-22.9424863416694,-21.9992612019408,-20.9992947836708,-19.9993283654008,
-18.9993619471307,-17.9993955288607,-16.9994291105906,-16.6593010344898),
 .UNSPECIFIED.);
#3234=B_SPLINE_CURVE_WITH_KNOTS('',3,(#59439,#59440,#59441,#59442,#59443,
#59444,#59445,#59446,#59447,#59448,#59449,#59450,#59451,#59452,#59453,#59454,
#59455,#59456,#59457,#59458,#59459,#59460,#59461,#59462,#59463),
 .UNSPECIFIED.,.F.,.F.,(4,3,3,3,3,3,3,3,4),(13.6836710227279,13.9477931291194,
14.9440640669136,15.9403350047079,16.9366059425021,17.9328768802963,18.9291478180906,
19.9254187558848,19.9668563299075),.UNSPECIFIED.);
#3235=B_SPLINE_CURVE_WITH_KNOTS('',3,(#59468,#59469,#59470,#59471,#59472,
#59473,#59474,#59475,#59476,#59477,#59478,#59479,#59480,#59481,#59482,#59483,
#59484,#59485,#59486,#59487,#59488,#59489,#59490,#59491,#59492),
 .UNSPECIFIED.,.F.,.F.,(4,3,3,3,3,3,3,3,4),(-29.225671648849,-28.9990261298311,
-27.9990597115611,-26.999093293291,-25.999126875021,-24.9991604567509,-23.9991940384809,
-22.9992276202109,-22.9424863416694),.UNSPECIFIED.);
#3236=B_SPLINE_CURVE_WITH_KNOTS('',3,(#59493,#59494,#59495,#59496,#59497,
#59498,#59499,#59500,#59501,#59502,#59503,#59504,#59505,#59506,#59507,#59508,
#59509,#59510,#59511,#59512,#59513,#59514),.UNSPECIFIED.,.F.,.F.,(4,3,3,
3,3,3,3,4),(19.9668563299075,20.9216896936791,21.9179606314733,22.9142315692675,
23.9105025070618,24.906773444856,25.9030443826502,26.2500416370871),
 .UNSPECIFIED.);
#3237=B_SPLINE_CURVE_WITH_KNOTS('',3,(#59519,#59520,#59521,#59522,#59523,
#59524,#59525,#59526,#59527,#59528,#59529,#59530,#59531,#59532,#59533,#59534,
#59535,#59536,#59537,#59538,#59539,#59540),.UNSPECIFIED.,.F.,.F.,(4,3,3,
3,3,3,3,4),(-35.5088569560286,-34.9988246394513,-33.9988582211813,-32.9988918029113,
-31.9989253846412,-30.9989589663712,-29.9989925481011,-29.225671648849),
 .UNSPECIFIED.);
#3238=B_SPLINE_CURVE_WITH_KNOTS('',3,(#59541,#59542,#59543,#59544,#59545,
#59546,#59547,#59548,#59549,#59550,#59551,#59552,#59553,#59554,#59555,#59556,
#59557,#59558,#59559,#59560,#59561,#59562),.UNSPECIFIED.,.F.,.F.,(4,3,3,
3,3,3,3,4),(26.2500416370871,26.8993153204445,27.8955862582387,28.891857196033,
29.8881281338272,30.8843990716215,31.8806700094157,32.5332269442667),
 .UNSPECIFIED.);
#3239=B_SPLINE_CURVE_WITH_KNOTS('',3,(#59567,#59568,#59569,#59570,#59571,
#59572,#59573,#59574,#59575,#59576,#59577,#59578,#59579,#59580,#59581,#59582,
#59583,#59584,#59585,#59586,#59587,#59588),.UNSPECIFIED.,.F.,.F.,(4,3,3,
3,3,3,3,4),(-41.7920422632082,-40.9986231490716,-39.9986567308015,-38.9986903125315,
-37.9987238942614,-36.9987574759914,-35.9987910577214,-35.5088569560286),
 .UNSPECIFIED.);
#3240=B_SPLINE_CURVE_WITH_KNOTS('',3,(#59589,#59590,#59591,#59592,#59593,
#59594,#59595,#59596,#59597,#59598,#59599,#59600,#59601,#59602,#59603,#59604,
#59605,#59606,#59607,#59608,#59609,#59610),.UNSPECIFIED.,.F.,.F.,(4,3,3,
3,3,3,3,4),(32.5332269442667,32.87694094721,33.8732118850042,34.8694828227984,
35.8657537605927,36.8620246983869,37.8582956361812,38.8164122514463),
 .UNSPECIFIED.);
#3241=B_SPLINE_CURVE_WITH_KNOTS('',3,(#59615,#59616,#59617,#59618,#59619,
#59620,#59621,#59622,#59623,#59624,#59625,#59626,#59627,#59628,#59629,#59630,
#59631,#59632,#59633,#59634,#59635,#59636,#59637,#59638,#59639),
 .UNSPECIFIED.,.F.,.F.,(4,3,3,3,3,3,3,3,4),(-48.0752275703878,-47.9983880769618,
-46.9984216586918,-45.9984552404217,-44.9984888221517,-43.9985224038817,
-42.9985559856116,-41.9985895673416,-41.7920422632082),.UNSPECIFIED.);
#3242=B_SPLINE_CURVE_WITH_KNOTS('',3,(#59640,#59641,#59642,#59643,#59644,
#59645,#59646,#59647,#59648,#59649,#59650,#59651,#59652,#59653,#59654,#59655,
#59656,#59657,#59658,#59659,#59660,#59661,#59662,#59663,#59664),
 .UNSPECIFIED.,.F.,.F.,(4,3,3,3,3,3,3,3,4),(38.8164122514463,38.8545665739754,
39.8508375117697,40.8471084495639,41.8433793873581,42.8396503251524,43.8359212629466,
44.8321922007408,45.0995975586259),.UNSPECIFIED.);
#3243=B_SPLINE_CURVE_WITH_KNOTS('',3,(#59669,#59670,#59671,#59672,#59673,
#59674,#59675,#59676,#59677,#59678,#59679,#59680,#59681,#59682,#59683,#59684,
#59685,#59686,#59687,#59688,#59689,#59690),.UNSPECIFIED.,.F.,.F.,(4,3,3,
3,3,3,3,4),(-54.3584128775673,-53.998186586582,-52.998220168312,-51.998253750042,
-50.9982873317719,-49.9983209135019,-48.9983544952319,-48.0752275703878),
 .UNSPECIFIED.);
#3244=B_SPLINE_CURVE_WITH_KNOTS('',3,(#59691,#59692,#59693,#59694,#59695,
#59696,#59697,#59698,#59699,#59700,#59701,#59702,#59703,#59704,#59705,#59706,
#59707,#59708,#59709,#59710,#59711,#59712),.UNSPECIFIED.,.F.,.F.,(4,3,3,
3,3,3,3,4),(45.0995975586259,45.8284631385351,46.8247340763293,47.8210050141236,
48.8172759519178,49.8135468897121,50.8098178275063,51.3827828658055),
 .UNSPECIFIED.);
#3245=B_SPLINE_CURVE_WITH_KNOTS('',3,(#59717,#59718,#59719,#59720,#59721,
#59722,#59723,#59724,#59725,#59726,#59727,#59728,#59729,#59730,#59731,#59732,
#59733,#59734,#59735,#59736,#59737,#59738),.UNSPECIFIED.,.F.,.F.,(4,3,3,
3,3,3,3,4),(-60.6415981847469,-59.9979850962023,-58.9980186779322,-57.9980522596622,
-56.9980858413922,-55.9981194231221,-54.9981530048521,-54.3584128775673),
 .UNSPECIFIED.);
#3246=B_SPLINE_CURVE_WITH_KNOTS('',3,(#59739,#59740,#59741,#59742,#59743,
#59744,#59745,#59746,#59747,#59748,#59749,#59750,#59751,#59752,#59753,#59754,
#59755,#59756,#59757,#59758,#59759,#59760),.UNSPECIFIED.,.F.,.F.,(4,3,3,
3,3,3,3,4),(51.3827828658055,51.8060887653006,52.8023597030948,53.798630640889,
54.7949015786833,55.7911725164775,56.7874434542717,57.665968172985),
 .UNSPECIFIED.);
#3247=B_SPLINE_CURVE_WITH_KNOTS('',3,(#59765,#59766,#59767,#59768,#59769,
#59770,#59771,#59772,#59773,#59774,#59775,#59776,#59777,#59778,#59779,#59780,
#59781,#59782,#59783,#59784,#59785,#59786),.UNSPECIFIED.,.F.,.F.,(4,3,3,
3,3,3,3,4),(-66.9247834919265,-65.9977836058225,-64.9978171875525,-63.9978507692824,
-62.9978843510124,-61.9979179327423,-60.9979515144723,-60.6415981847469),
 .UNSPECIFIED.);
#3248=B_SPLINE_CURVE_WITH_KNOTS('',3,(#59787,#59788,#59789,#59790,#59791,
#59792,#59793,#59794,#59795,#59796,#59797,#59798,#59799,#59800,#59801,#59802,
#59803,#59804,#59805,#59806,#59807,#59808,#59809,#59810,#59811),
 .UNSPECIFIED.,.F.,.F.,(4,3,3,3,3,3,3,3,4),(57.665968172985,57.783714392066,
58.7799853298602,59.7762562676544,60.7725272054487,61.7687981432429,62.7650690810372,
63.7613400188314,63.9491534801646),.UNSPECIFIED.);
#3249=B_SPLINE_CURVE_WITH_KNOTS('',3,(#59816,#59817,#59818,#59819,#59820,
#59821,#59822,#59823,#59824,#59825,#59826,#59827,#59828,#59829,#59830,#59831,
#59832,#59833,#59834,#59835,#59836,#59837,#59838,#59839,#59840),
 .UNSPECIFIED.,.F.,.F.,(4,3,3,3,3,3,3,3,4),(-73.2079687991061,-72.9975485337127,
-71.9975821154427,-70.9976156971727,-69.9976492789027,-68.9976828606326,
-67.9977164423626,-66.9977500240925,-66.9247834919265),.UNSPECIFIED.);
#3250=B_SPLINE_CURVE_WITH_KNOTS('',3,(#59841,#59842,#59843,#59844,#59845,
#59846,#59847,#59848,#59849,#59850,#59851,#59852,#59853,#59854,#59855,#59856,
#59857,#59858,#59859,#59860,#59861,#59862),.UNSPECIFIED.,.F.,.F.,(4,3,3,
3,3,3,3,4),(63.9491534801646,64.7576109566257,65.7538818944199,66.7501528322141,
67.7464237700084,68.7426947078026,69.7389656455968,70.2323387873442),
 .UNSPECIFIED.);
#3251=B_SPLINE_CURVE_WITH_KNOTS('',3,(#59867,#59868,#59869,#59870,#59871,
#59872,#59873,#59874,#59875,#59876,#59877,#59878,#59879,#59880,#59881,#59882,
#59883,#59884,#59885,#59886,#59887,#59888),.UNSPECIFIED.,.F.,.F.,(4,3,3,
3,3,3,3,4),(-79.4911541062857,-78.997347043333,-77.997380625063,-76.9974142067929,
-75.9974477885229,-74.9974813702528,-73.9975149519828,-73.2079687991061),
 .UNSPECIFIED.);
#3252=B_SPLINE_CURVE_WITH_KNOTS('',3,(#59889,#59890,#59891,#59892,#59893,
#59894,#59895,#59896,#59897,#59898,#59899,#59900,#59901,#59902,#59903,#59904,
#59905,#59906,#59907,#59908,#59909,#59910),.UNSPECIFIED.,.F.,.F.,(4,3,3,
3,3,3,3,4),(70.2323387873442,70.7352365833911,71.7315075211853,72.7277784589796,
73.7240493967738,74.7203203345681,75.7165912723623,76.5155240945238),
 .UNSPECIFIED.);
#3253=B_SPLINE_CURVE_WITH_KNOTS('',3,(#59915,#59916,#59917,#59918,#59919,
#59920,#59921,#59922,#59923,#59924,#59925,#59926,#59927,#59928,#59929,#59930,
#59931,#59932,#59933,#59934,#59935,#59936),.UNSPECIFIED.,.F.,.F.,(4,3,3,
3,3,3,3,4),(-85.7743394134653,-84.9971455529532,-83.9971791346832,-82.9972127164132,
-81.9972462981431,-80.9972798798731,-79.997313461603,-79.4911541062857),
 .UNSPECIFIED.);
#3254=B_SPLINE_CURVE_WITH_KNOTS('',3,(#59937,#59938,#59939,#59940,#59941,
#59942,#59943,#59944,#59945,#59946,#59947,#59948,#59949,#59950,#59951,#59952,
#59953,#59954,#59955,#59956,#59957,#59958,#59959,#59960,#59961),
 .UNSPECIFIED.,.F.,.F.,(4,3,3,3,3,3,3,3,4),(76.5155240945238,76.7128622101565,
77.7091331479508,78.705404085745,79.7016750235393,80.6979459613335,81.6942168991278,
82.690487836922,82.7987094017034),.UNSPECIFIED.);
#3255=B_SPLINE_CURVE_WITH_KNOTS('',3,(#59966,#59967,#59968,#59969,#59970,
#59971,#59972,#59973,#59974,#59975,#59976,#59977,#59978,#59979,#59980,#59981,
#59982,#59983,#59984,#59985,#59986,#59987,#59988,#59989,#59990),
 .UNSPECIFIED.,.F.,.F.,(4,3,3,3,3,3,3,3,4),(-92.0575247206449,-91.9969104808435,
-90.9969440625734,-89.9969776443034,-88.9970112260334,-87.9970448077633,
-86.9970783894933,-85.9971119712233,-85.7743394134653),.UNSPECIFIED.);
#3256=B_SPLINE_CURVE_WITH_KNOTS('',3,(#59991,#59992,#59993,#59994,#59995,
#59996,#59997,#59998,#59999,#60000,#60001,#60002,#60003,#60004,#60005,#60006,
#60007,#60008,#60009,#60010,#60011,#60012),.UNSPECIFIED.,.F.,.F.,(4,3,3,
3,3,3,3,4),(82.7987094017034,83.6867587747162,84.6830297125105,85.6793006503047,
86.675571588099,87.6718425258932,88.6681134636875,89.081894708883),
 .UNSPECIFIED.);
#3257=B_SPLINE_CURVE_WITH_KNOTS('',3,(#60017,#60018,#60019,#60020,#60021,
#60022,#60023,#60024,#60025,#60026,#60027,#60028,#60029,#60030,#60031,#60032,
#60033,#60034,#60035,#60036,#60037,#60038),.UNSPECIFIED.,.F.,.F.,(4,3,3,
3,3,3,3,4),(-98.3407100278245,-97.9967089904637,-96.9967425721937,-95.9967761539236,
-94.9968097356536,-93.9968433173836,-92.9968768991135,-92.0575247206449),
 .UNSPECIFIED.);
#3258=B_SPLINE_CURVE_WITH_KNOTS('',3,(#60039,#60040,#60041,#60042,#60043,
#60044,#60045,#60046,#60047,#60048,#60049,#60050,#60051,#60052,#60053,#60054,
#60055,#60056,#60057,#60058,#60059,#60060),.UNSPECIFIED.,.F.,.F.,(4,3,3,
3,3,3,3,4),(89.081894708883,89.6643844014817,90.6606553392759,91.6569262770702,
92.6531972148644,93.6494681526586,94.6457390904529,95.3650800160626),
 .UNSPECIFIED.);
#3259=B_SPLINE_CURVE_WITH_KNOTS('',3,(#60065,#60066,#60067,#60068,#60069,
#60070,#60071,#60072,#60073,#60074,#60075,#60076,#60077,#60078,#60079,#60080,
#60081,#60082,#60083,#60084,#60085,#60086),.UNSPECIFIED.,.F.,.F.,(4,3,3,
3,3,3,3,4),(-104.623895335004,-103.996507500084,-102.996541081814,-101.996574663544,
-100.996608245274,-99.9966418270038,-98.9966754087338,-98.3407100278245),
 .UNSPECIFIED.);
#3260=B_SPLINE_CURVE_WITH_KNOTS('',3,(#60087,#60088,#60089,#60090,#60091,
#60092,#60093,#60094,#60095,#60096,#60097,#60098,#60099,#60100,#60101,#60102,
#60103,#60104,#60105,#60106,#60107,#60108,#60109,#60110,#60111),
 .UNSPECIFIED.,.F.,.F.,(4,3,3,3,3,3,3,3,4),(95.3650800160626,95.6420100282471,
96.6382809660413,97.6345519038356,98.6308228416299,99.6270937794241,100.623364717218,
101.619635655013,101.648265323242),.UNSPECIFIED.);
#3261=B_SPLINE_CURVE_WITH_KNOTS('',3,(#60116,#60117,#60118,#60119,#60120,
#60121,#60122,#60123,#60124,#60125,#60126,#60127,#60128,#60129,#60130,#60131,
#60132,#60133,#60134,#60135,#60136,#60137),.UNSPECIFIED.,.F.,.F.,(4,3,3,
3,3,3,3,4),(-110.907080642184,-109.996306009704,-108.996339591434,-107.996373173164,
-106.996406754894,-105.996440336624,-104.996473918354,-104.623895335004),
 .UNSPECIFIED.);
#3262=B_SPLINE_CURVE_WITH_KNOTS('',3,(#60138,#60139,#60140,#60141,#60142,
#60143,#60144,#60145,#60146,#60147,#60148,#60149,#60150,#60151,#60152,#60153,
#60154,#60155,#60156,#60157,#60158,#60159),.UNSPECIFIED.,.F.,.F.,(4,3,3,
3,3,3,3,4),(101.648265323242,102.615906592807,103.612177530601,104.608448468395,
105.60471940619,106.600990343984,107.597261281778,107.931450630422),
 .UNSPECIFIED.);
#3263=B_SPLINE_CURVE_WITH_KNOTS('',3,(#60164,#60165,#60166,#60167,#60168,
#60169,#60170,#60171,#60172,#60173,#60174,#60175,#60176,#60177,#60178,#60179,
#60180,#60181,#60182,#60183,#60184,#60185,#60186,#60187,#60188),
 .UNSPECIFIED.,.F.,.F.,(4,3,3,3,3,3,3,3,4),(-117.190265949363,-116.996070937594,
-115.996104519324,-114.996138101054,-113.996171682784,-112.996205264514,
-111.996238846244,-110.996272427974,-110.907080642184),.UNSPECIFIED.);
#3264=B_SPLINE_CURVE_WITH_KNOTS('',3,(#60189,#60190,#60191,#60192,#60193,
#60194,#60195,#60196,#60197,#60198,#60199,#60200,#60201,#60202,#60203,#60204,
#60205,#60206,#60207,#60208,#60209,#60210),.UNSPECIFIED.,.F.,.F.,(4,3,3,
3,3,3,3,4),(107.931450630422,108.593532219572,109.589803157367,110.586074095161,
111.582345032955,112.578615970749,113.574886908543,114.214635937601),
 .UNSPECIFIED.);
#3265=B_SPLINE_CURVE_WITH_KNOTS('',3,(#60215,#60216,#60217,#60218,#60219,
#60220,#60221,#60222,#60223,#60224,#60225,#60226,#60227,#60228,#60229,#60230,
#60231,#60232,#60233,#60234,#60235,#60236),.UNSPECIFIED.,.F.,.F.,(4,3,3,
3,3,3,3,4),(-123.473451256543,-122.995869447215,-121.995903028945,-120.995936610675,
-119.995970192405,-118.996003774135,-117.996037355864,-117.190265949363),
 .UNSPECIFIED.);
#3266=B_SPLINE_CURVE_WITH_KNOTS('',3,(#60237,#60238,#60239,#60240,#60241,
#60242,#60243,#60244,#60245,#60246,#60247,#60248,#60249,#60250,#60251,#60252,
#60253,#60254,#60255,#60256,#60257,#60258),.UNSPECIFIED.,.F.,.F.,(4,3,3,
3,3,3,3,4),(114.214635937601,114.571157846338,115.567428784132,116.563699721926,
117.55997065972,118.556241597515,119.552512535309,120.497821244781),
 .UNSPECIFIED.);
#3267=B_SPLINE_CURVE_WITH_KNOTS('',3,(#60263,#60264,#60265,#60266,#60267,
#60268,#60269,#60270,#60271,#60272,#60273,#60274,#60275,#60276,#60277,#60278,
#60279,#60280,#60281,#60282,#60283,#60284),.UNSPECIFIED.,.F.,.F.,(4,3,3,
3,3,3,3,4),(-129.756636563722,-128.995667956835,-127.995701538565,-126.995735120295,
-125.995768702025,-124.995802283755,-123.995835865485,-123.473451256543),
 .UNSPECIFIED.);
#3268=B_SPLINE_CURVE_WITH_KNOTS('',3,(#60285,#60286,#60287,#60288,#60289,
#60290,#60291,#60292,#60293,#60294,#60295,#60296,#60297,#60298,#60299,#60300,
#60301,#60302,#60303,#60304,#60305,#60306,#60307,#60308,#60309),
 .UNSPECIFIED.,.F.,.F.,(4,3,3,3,3,3,3,3,4),(120.497821244781,120.548783473103,
121.545054410897,122.541325348692,123.537596286486,124.53386722428,125.530138162074,
126.526409099869,126.781006551961),.UNSPECIFIED.);
#3269=B_SPLINE_CURVE_WITH_KNOTS('',3,(#60314,#60315,#60316,#60317,#60318,
#60319,#60320,#60321,#60322,#60323,#60324,#60325,#60326,#60327,#60328,#60329,
#60330,#60331,#60332,#60333,#60334,#60335,#60336,#60337,#60338),
 .UNSPECIFIED.,.F.,.F.,(4,3,3,3,3,3,3,3,4),(-136.039821870902,-135.995432884725,
-134.995466466455,-133.995500048185,-132.995533629915,-131.995567211645,
-130.995600793375,-129.995634375105,-129.756636563722),.UNSPECIFIED.);
#3270=B_SPLINE_CURVE_WITH_KNOTS('',3,(#60339,#60340,#60341,#60342,#60343,
#60344,#60345,#60346,#60347,#60348,#60349,#60350,#60351,#60352,#60353,#60354,
#60355,#60356,#60357,#60358,#60359,#60360),.UNSPECIFIED.,.F.,.F.,(4,3,3,
3,3,3,3,4),(126.781006551961,127.522680037663,128.518950975457,129.515221913251,
130.511492851046,131.50776378884,132.504034726634,133.06419185914),
 .UNSPECIFIED.);
#3271=B_SPLINE_CURVE_WITH_KNOTS('',3,(#60365,#60366,#60367,#60368,#60369,
#60370,#60371,#60372,#60373,#60374,#60375,#60376,#60377,#60378,#60379,#60380,
#60381,#60382,#60383,#60384,#60385,#60386),.UNSPECIFIED.,.F.,.F.,(4,3,3,
3,3,3,3,4),(-142.323007178082,-141.995231394345,-140.995264976075,-139.995298557805,
-138.995332139535,-137.995365721265,-136.995399302995,-136.039821870902),
 .UNSPECIFIED.);
#3272=B_SPLINE_CURVE_WITH_KNOTS('',3,(#60387,#60388,#60389,#60390,#60391,
#60392,#60393,#60394,#60395,#60396,#60397,#60398,#60399,#60400,#60401,#60402,
#60403,#60404,#60405,#60406,#60407,#60408),.UNSPECIFIED.,.F.,.F.,(4,3,3,
3,3,3,3,4),(133.06419185914,133.500305664428,134.496576602223,135.492847540017,
136.489118477811,137.485389415605,138.481660353399,139.34737716632),
 .UNSPECIFIED.);
#3273=B_SPLINE_CURVE_WITH_KNOTS('',3,(#60413,#60414,#60415,#60416,#60417,
#60418,#60419,#60420,#60421,#60422,#60423,#60424,#60425,#60426,#60427,#60428,
#60429,#60430,#60431,#60432,#60433,#60434),.UNSPECIFIED.,.F.,.F.,(4,3,3,
3,3,3,3,4),(-148.606192485261,-147.995029903966,-146.995063485696,-145.995097067426,
-144.995130649155,-143.995164230885,-142.995197812615,-142.323007178082),
 .UNSPECIFIED.);
#3274=B_SPLINE_CURVE_WITH_KNOTS('',3,(#60435,#60436,#60437,#60438,#60439,
#60440,#60441,#60442,#60443,#60444,#60445,#60446,#60447,#60448,#60449,#60450,
#60451,#60452,#60453,#60454,#60455,#60456,#60457,#60458,#60459),
 .UNSPECIFIED.,.F.,.F.,(4,3,3,3,3,3,3,3,4),(139.34737716632,139.477931291194,
140.474202228988,141.470473166782,142.466744104576,143.463015042371,144.459285980165,
145.455556917959,145.630562473499),.UNSPECIFIED.);
#3275=B_SPLINE_CURVE_WITH_KNOTS('',3,(#60464,#60465,#60466,#60467,#60468,
#60469,#60470,#60471,#60472,#60473,#60474,#60475,#60476,#60477,#60478,#60479,
#60480,#60481,#60482,#60483,#60484,#60485),.UNSPECIFIED.,.F.,.F.,(4,3,3,
3,3,3,3,4),(-154.889377792441,-153.994828413586,-152.994861995316,-151.994895577046,
-150.994929158776,-149.994962740506,-148.994996322236,-148.606192485261),
 .UNSPECIFIED.);
#3276=B_SPLINE_CURVE_WITH_KNOTS('',3,(#60486,#60487,#60488,#60489,#60490,
#60491,#60492,#60493,#60494,#60495,#60496,#60497,#60498,#60499,#60500,#60501,
#60502,#60503,#60504,#60505,#60506,#60507),.UNSPECIFIED.,.F.,.F.,(4,3,3,
3,3,3,3,4),(145.630562473499,146.451827855753,147.448098793548,148.444369731342,
149.440640669136,150.43691160693,151.433182544725,151.913747780679),
 .UNSPECIFIED.);
#3277=B_SPLINE_CURVE_WITH_KNOTS('',3,(#60512,#60513,#60514,#60515,#60516,
#60517,#60518,#60519,#60520,#60521,#60522,#60523,#60524,#60525,#60526,#60527,
#60528,#60529,#60530,#60531,#60532,#60533,#60534,#60535,#60536),
 .UNSPECIFIED.,.F.,.F.,(4,3,3,3,3,3,3,3,4),(-161.17256309962,-160.994593341476,
-159.994626923206,-158.994660504936,-157.994694086666,-156.994727668396,
-155.994761250126,-154.994794831856,-154.889377792441),.UNSPECIFIED.);
#3278=B_SPLINE_CURVE_WITH_KNOTS('',3,(#60537,#60538,#60539,#60540,#60541,
#60542,#60543,#60544,#60545,#60546,#60547,#60548,#60549,#60550,#60551,#60552,
#60553,#60554,#60555,#60556,#60557,#60558),.UNSPECIFIED.,.F.,.F.,(4,3,3,
3,3,3,3,4),(151.913747780679,152.429453482519,153.425724420313,154.421995358107,
155.418266295902,156.414537233696,157.41080817149,158.196933087858),
 .UNSPECIFIED.);
#3279=B_SPLINE_CURVE_WITH_KNOTS('',3,(#60563,#60564,#60565,#60566,#60567,
#60568,#60569,#60570,#60571,#60572,#60573,#60574,#60575,#60576,#60577,#60578,
#60579,#60580,#60581,#60582,#60583,#60584),.UNSPECIFIED.,.F.,.F.,(4,3,3,
3,3,3,3,4),(-167.4557484068,-166.994391851096,-165.994425432826,-164.994459014556,
-163.994492596286,-162.994526178016,-161.994559759746,-161.17256309962),
 .UNSPECIFIED.);
#3280=B_SPLINE_CURVE_WITH_KNOTS('',3,(#60585,#60586,#60587,#60588,#60589,
#60590,#60591,#60592,#60593,#60594,#60595,#60596,#60597,#60598,#60599,#60600,
#60601,#60602,#60603,#60604,#60605,#60606,#60607,#60608,#60609),
 .UNSPECIFIED.,.F.,.F.,(4,3,3,3,3,3,3,3,4),(158.196933087858,158.407079109284,
159.403350047079,160.399620984873,161.395891922667,162.392162860461,163.388433798255,
164.38470473605,164.480118395038),.UNSPECIFIED.);
#3281=B_SPLINE_CURVE_WITH_KNOTS('',3,(#60614,#60615,#60616,#60617,#60618,
#60619,#60620,#60621,#60622,#60623,#60624,#60625,#60626,#60627,#60628,#60629,
#60630,#60631,#60632,#60633,#60634,#60635),.UNSPECIFIED.,.F.,.F.,(4,3,3,
3,3,3,3,4),(-173.738933713979,-172.994190360717,-171.994223942447,-170.994257524176,
-169.994291105906,-168.994324687636,-167.994358269366,-167.4557484068),
 .UNSPECIFIED.);
#3282=B_SPLINE_CURVE_WITH_KNOTS('',3,(#60636,#60637,#60638,#60639,#60640,
#60641,#60642,#60643,#60644,#60645,#60646,#60647,#60648,#60649,#60650,#60651,
#60652,#60653,#60654,#60655,#60656,#60657),.UNSPECIFIED.,.F.,.F.,(4,3,3,
3,3,3,3,4),(164.480118395038,165.380975673844,166.377246611638,167.373517549432,
168.369788487227,169.366059425021,170.362330362815,170.763303702218),
 .UNSPECIFIED.);
#3283=B_SPLINE_CURVE_WITH_KNOTS('',3,(#60662,#60663,#60664,#60665,#60666,
#60667,#60668,#60669,#60670,#60671,#60672,#60673,#60674,#60675,#60676,#60677,
#60678,#60679,#60680,#60681,#60682,#60683,#60684,#60685,#60686),
 .UNSPECIFIED.,.F.,.F.,(4,3,3,3,3,3,3,3,4),(-180.022119021159,-179.993955288607,
-178.993988870337,-177.994022452067,-176.994056033797,-175.994089615527,
-174.994123197257,-173.994156778987,-173.738933713979),.UNSPECIFIED.);
#3284=B_SPLINE_CURVE_WITH_KNOTS('',3,(#60687,#60688,#60689,#60690,#60691,
#60692,#60693,#60694,#60695,#60696,#60697,#60698,#60699,#60700,#60701,#60702,
#60703,#60704,#60705,#60706,#60707,#60708),.UNSPECIFIED.,.F.,.F.,(4,3,3,
3,3,3,3,4),(170.763303702218,171.358601300609,172.354872238404,173.351143176198,
174.347414113992,175.343685051786,176.339955989581,177.046489009397),
 .UNSPECIFIED.);
#3285=B_SPLINE_CURVE_WITH_KNOTS('',3,(#60713,#60714,#60715,#60716,#60717,
#60718,#60719,#60720,#60721,#60722,#60723,#60724,#60725,#60726,#60727,#60728,
#60729,#60730,#60731,#60732,#60733,#60734),.UNSPECIFIED.,.F.,.F.,(4,3,3,
3,3,3,3,4),(-186.305304328339,-185.993753798227,-184.993787379957,-183.993820961687,
-182.993854543417,-181.993888125147,-180.993921706877,-180.022119021159),
 .UNSPECIFIED.);
#3286=B_SPLINE_CURVE_WITH_KNOTS('',3,(#60735,#60736,#60737,#60738,#60739,
#60740,#60741,#60742,#60743,#60744,#60745,#60746,#60747,#60748,#60749,#60750,
#60751,#60752,#60753,#60754,#60755,#60756,#60757,#60758,#60759),
 .UNSPECIFIED.,.F.,.F.,(4,3,3,3,3,3,3,3,4),(177.046489009397,177.336226927375,
178.332497865169,179.328768802963,180.325039740758,181.321310678552,182.317581616346,
183.31385255414,183.329674316577),.UNSPECIFIED.);
#3287=B_SPLINE_CURVE_WITH_KNOTS('',3,(#60764,#60765,#60766,#60767,#60768,
#60769,#60770,#60771,#60772,#60773,#60774,#60775,#60776,#60777,#60778,#60779,
#60780,#60781,#60782,#60783,#60784,#60785),.UNSPECIFIED.,.F.,.F.,(4,3,3,
3,3,3,3,4),(-192.588489635518,-191.993552307847,-190.993585889577,-189.993619471307,
-188.993653053037,-187.993686634767,-186.993720216497,-186.305304328339),
 .UNSPECIFIED.);
#3288=B_SPLINE_CURVE_WITH_KNOTS('',3,(#60786,#60787,#60788,#60789,#60790,
#60791,#60792,#60793,#60794,#60795,#60796,#60797,#60798,#60799,#60800,#60801,
#60802,#60803,#60804,#60805,#60806,#60807),.UNSPECIFIED.,.F.,.F.,(4,3,3,
3,3,3,3,4),(183.329674316577,184.310123491935,185.306394429729,186.302665367523,
187.298936305317,188.295207243112,189.291478180906,189.612859623756),
 .UNSPECIFIED.);
#3289=B_SPLINE_CURVE_WITH_KNOTS('',3,(#60812,#60813,#60814,#60815,#60816,
#60817,#60818,#60819,#60820,#60821,#60822,#60823,#60824,#60825,#60826,#60827,
#60828,#60829,#60830,#60831,#60832,#60833),.UNSPECIFIED.,.F.,.F.,(4,3,3,
3,3,3,3,4),(-198.871674942698,-197.993350817467,-196.993384399197,-195.993417980927,
-194.993451562657,-193.993485144387,-192.993518726117,-192.588489635518),
 .UNSPECIFIED.);
#3290=B_SPLINE_CURVE_WITH_KNOTS('',3,(#60834,#60835,#60836,#60837,#60838,
#60839,#60840,#60841,#60842,#60843,#60844,#60845,#60846,#60847,#60848,#60849,
#60850,#60851,#60852,#60853,#60854,#60855),.UNSPECIFIED.,.F.,.F.,(4,3,3,
3,3,3,3,4),(189.612859623756,190.2877491187,191.284020056494,192.280290994288,
193.276561932083,194.272832869877,195.269103807671,195.896044930936),
 .UNSPECIFIED.);
#3291=B_SPLINE_CURVE_WITH_KNOTS('',3,(#60860,#60861,#60862,#60863,#60864,
#60865,#60866,#60867,#60868,#60869,#60870,#60871,#60872,#60873,#60874,#60875,
#60876,#60877,#60878,#60879,#60880,#60881,#60882,#60883,#60884),
 .UNSPECIFIED.,.F.,.F.,(4,3,3,3,3,3,3,3,4),(-205.154860249877,-204.993115745358,
-203.993149327088,-202.993182908818,-201.993216490548,-200.993250072278,
-199.993283654008,-198.993317235738,-198.871674942698),.UNSPECIFIED.);
#3292=B_SPLINE_CURVE_WITH_KNOTS('',3,(#60885,#60886,#60887,#60888,#60889,
#60890,#60891,#60892,#60893,#60894,#60895,#60896,#60897,#60898,#60899,#60900,
#60901,#60902,#60903,#60904,#60905,#60906),.UNSPECIFIED.,.F.,.F.,(4,3,3,
3,3,3,3,4),(195.896044930936,196.265374745465,197.26164568326,198.257916621054,
199.254187558848,200.250458496642,201.246729434437,202.179230238115),
 .UNSPECIFIED.);
#3293=B_SPLINE_CURVE_WITH_KNOTS('',3,(#60911,#60912,#60913,#60914,#60915,
#60916,#60917,#60918,#60919,#60920,#60921,#60922,#60923,#60924,#60925,#60926,
#60927,#60928,#60929,#60930,#60931,#60932),.UNSPECIFIED.,.F.,.F.,(4,3,3,
3,3,3,3,4),(-211.438045557057,-210.992914254978,-209.992947836708,-208.992981418438,
-207.993015000168,-206.993048581898,-205.993082163628,-205.154860249877),
 .UNSPECIFIED.);
#3294=B_SPLINE_CURVE_WITH_KNOTS('',3,(#60933,#60934,#60935,#60936,#60937,
#60938,#60939,#60940,#60941,#60942,#60943,#60944,#60945,#60946,#60947,#60948,
#60949,#60950,#60951,#60952,#60953,#60954,#60955,#60956,#60957),
 .UNSPECIFIED.,.F.,.F.,(4,3,3,3,3,3,3,3,4),(202.179230238115,202.243000372231,
203.239271310025,204.235542247819,205.231813185614,206.228084123408,207.224355061202,
208.220625998996,208.462415545295),.UNSPECIFIED.);
#3295=B_SPLINE_CURVE_WITH_KNOTS('',3,(#60962,#60963,#60964,#60965,#60966,
#60967,#60968,#60969,#60970,#60971,#60972,#60973,#60974,#60975,#60976,#60977,
#60978,#60979,#60980,#60981,#60982,#60983),.UNSPECIFIED.,.F.,.F.,(4,3,3,
3,3,3,3,4),(-217.721230864236,-216.992712764598,-215.992746346328,-214.992779928058,
-213.992813509788,-212.992847091518,-211.992880673248,-211.438045557057),
 .UNSPECIFIED.);
#3296=B_SPLINE_CURVE_WITH_KNOTS('',3,(#60984,#60985,#60986,#60987,#60988,
#60989,#60990,#60991,#60992,#60993,#60994,#60995,#60996,#60997,#60998,#60999,
#61000,#61001,#61002,#61003,#61004,#61005),.UNSPECIFIED.,.F.,.F.,(4,3,3,
3,3,3,3,4),(208.462415545295,209.216896936791,210.213167874585,211.209438812379,
212.205709750173,213.201980687968,214.198251625762,214.745600852474),
 .UNSPECIFIED.);
#3297=B_SPLINE_CURVE_WITH_KNOTS('',3,(#61010,#61011,#61012,#61013,#61014,
#61015,#61016,#61017,#61018,#61019,#61020,#61021,#61022,#61023,#61024,#61025,
#61026,#61027,#61028,#61029,#61030,#61031,#61032,#61033,#61034),
 .UNSPECIFIED.,.F.,.F.,(4,3,3,3,3,3,3,3,4),(-224.004416171416,-223.992477692488,
-222.992511274218,-221.992544855948,-220.992578437678,-219.992612019408,
-218.992645601138,-217.992679182868,-217.721230864236),.UNSPECIFIED.);
#3298=B_SPLINE_CURVE_WITH_KNOTS('',3,(#61035,#61036,#61037,#61038,#61039,
#61040,#61041,#61042,#61043,#61044,#61045,#61046,#61047,#61048,#61049,#61050,
#61051,#61052,#61053,#61054,#61055,#61056),.UNSPECIFIED.,.F.,.F.,(4,3,3,
3,3,3,3,4),(214.745600852474,215.194522563556,216.19079350135,217.187064439145,
218.183335376939,219.179606314733,220.175877252527,221.028786159654),
 .UNSPECIFIED.);
#3299=B_SPLINE_CURVE_WITH_KNOTS('',3,(#61061,#61062,#61063,#61064,#61065,
#61066,#61067,#61068,#61069,#61070,#61071,#61072,#61073,#61074,#61075,#61076,
#61077,#61078,#61079,#61080,#61081,#61082),.UNSPECIFIED.,.F.,.F.,(4,3,3,
3,3,3,3,4),(-230.287601478595,-229.992276202109,-228.992309783839,-227.992343365569,
-226.992376947299,-225.992410529029,-224.992444110759,-224.004416171416),
 .UNSPECIFIED.);
#3300=B_SPLINE_CURVE_WITH_KNOTS('',3,(#61083,#61084,#61085,#61086,#61087,
#61088,#61089,#61090,#61091,#61092,#61093,#61094,#61095,#61096,#61097,#61098,
#61099,#61100,#61101,#61102,#61103,#61104,#61105,#61106,#61107),
 .UNSPECIFIED.,.F.,.F.,(4,3,3,3,3,3,3,3,4),(221.028786159654,221.172148190321,
222.168419128116,223.16469006591,224.160961003704,225.157231941498,226.153502879293,
227.149773817087,227.311971466834),.UNSPECIFIED.);
#3301=B_SPLINE_CURVE_WITH_KNOTS('',3,(#61112,#61113,#61114,#61115,#61116,
#61117,#61118,#61119,#61120,#61121,#61122,#61123,#61124,#61125,#61126,#61127,
#61128,#61129,#61130,#61131,#61132,#61133),.UNSPECIFIED.,.F.,.F.,(4,3,3,
3,3,3,3,4),(-236.570786785775,-235.992074711729,-234.992108293459,-233.992141875189,
-232.992175456919,-231.992209038649,-230.992242620379,-230.287601478595),
 .UNSPECIFIED.);
#3302=B_SPLINE_CURVE_WITH_KNOTS('',3,(#61134,#61135,#61136,#61137,#61138,
#61139,#61140,#61141,#61142,#61143,#61144,#61145,#61146,#61147,#61148,#61149,
#61150,#61151,#61152,#61153,#61154,#61155),.UNSPECIFIED.,.F.,.F.,(4,3,3,
3,3,3,3,4),(227.311971466834,228.146044754881,229.142315692675,230.13858663047,
231.134857568264,232.131128506058,233.127399443852,233.595156774013),
 .UNSPECIFIED.);
#3303=B_SPLINE_CURVE_WITH_KNOTS('',3,(#61160,#61161,#61162,#61163,#61164,
#61165,#61166,#61167,#61168,#61169,#61170,#61171,#61172,#61173,#61174,#61175,
#61176,#61177,#61178,#61179,#61180,#61181),.UNSPECIFIED.,.F.,.F.,(4,3,3,
3,3,3,3,4),(-242.853972092955,-241.991873221349,-240.991906803079,-239.991940384809,
-238.991973966539,-237.992007548269,-236.992041129999,-236.570786785775),
 .UNSPECIFIED.);
#3304=B_SPLINE_CURVE_WITH_KNOTS('',3,(#61182,#61183,#61184,#61185,#61186,
#61187,#61188,#61189,#61190,#61191,#61192,#61193,#61194,#61195,#61196,#61197,
#61198,#61199,#61200,#61201,#61202,#61203),.UNSPECIFIED.,.F.,.F.,(4,3,3,
3,3,3,3,4),(233.595156774013,234.123670381647,235.119941319441,236.116212257235,
237.112483195029,238.108754132824,239.105025070618,239.878342081193),
 .UNSPECIFIED.);
#3305=B_SPLINE_CURVE_WITH_KNOTS('',3,(#61209,#61210,#61211,#61212,#61213,
#61214,#61215,#61216,#61217,#61218),.UNSPECIFIED.,.F.,.F.,(4,1,1,1,1,1,
1,4),(254.469004940773,254.606872487438,255.606838905708,256.606805323978,
257.606771742248,258.606738160518,259.606704578788,260.606670997058),
 .UNSPECIFIED.);
#3306=B_SPLINE_CURVE_WITH_KNOTS('',3,(#61221,#61222,#61223,#61224,#61225,
#61226,#61227,#61228),.UNSPECIFIED.,.F.,.F.,(4,1,1,1,1,4),(254.469004940773,
255.382670125373,256.378941063167,257.375212000962,258.371482938756,259.36775387655),
 .UNSPECIFIED.);
#3307=B_SPLINE_CURVE_WITH_KNOTS('',3,(#61233,#61234,#61235,#61236,#61237,
#61238,#61239,#61240,#61241,#61242),.UNSPECIFIED.,.F.,.F.,(4,1,1,1,1,1,
1,4),(248.185819633594,248.607073977818,249.607040396088,250.607006814358,
251.606973232628,252.606939650898,253.606906069168,254.469004940773),
 .UNSPECIFIED.);
#3308=B_SPLINE_CURVE_WITH_KNOTS('',3,(#61243,#61244,#61245,#61246,#61247,
#61248,#61249,#61250,#61251,#61252,#61253),.UNSPECIFIED.,.F.,.F.,(4,1,1,
1,1,1,1,1,4),(248.185819633594,248.408773560813,249.405044498608,250.401315436402,
251.397586374196,252.39385731199,253.390128249785,254.386399187579,254.469004940773),
 .UNSPECIFIED.);
#3309=B_SPLINE_CURVE_WITH_KNOTS('',3,(#61258,#61259,#61260,#61261,#61262,
#61263,#61264,#61265,#61266,#61267),.UNSPECIFIED.,.F.,.F.,(4,1,1,1,1,1,
1,4),(241.902634326414,242.607275468197,243.607241886467,244.607208304738,
245.607174723008,246.607141141278,247.607107559548,248.185819633594),
 .UNSPECIFIED.);
#3310=B_SPLINE_CURVE_WITH_KNOTS('',3,(#61268,#61269,#61270,#61271,#61272,
#61273,#61274,#61275,#61276,#61277),.UNSPECIFIED.,.F.,.F.,(4,1,1,1,1,1,
1,4),(241.902634326414,242.431147934048,243.427418871842,244.423689809636,
245.419960747431,246.416231685225,247.412502623019,248.185819633594),
 .UNSPECIFIED.);
#3311=B_SPLINE_CURVE_WITH_KNOTS('',3,(#61282,#61283,#61284,#61285,#61286,
#61287,#61288,#61289,#61290,#61291),.UNSPECIFIED.,.F.,.F.,(4,1,1,1,1,1,
1,4),(235.619449019234,236.607476958577,237.607443376847,238.607409795117,
239.607376213387,240.607342631657,241.607309049927,241.902634326414),
 .UNSPECIFIED.);
#3312=B_SPLINE_CURVE_WITH_KNOTS('',3,(#61292,#61293,#61294,#61295,#61296,
#61297,#61298,#61299,#61300,#61301),.UNSPECIFIED.,.F.,.F.,(4,1,1,1,1,1,
1,4),(235.619449019235,236.453522307283,237.449793245077,238.446064182871,
239.442335120665,240.438606058459,241.434876996254,241.902634326414),
 .UNSPECIFIED.);
#3313=B_SPLINE_CURVE_WITH_KNOTS('',3,(#61306,#61307,#61308,#61309,#61310,
#61311,#61312,#61313,#61314,#61315,#61316),.UNSPECIFIED.,.F.,.F.,(4,1,1,
1,1,1,1,1,4),(229.336263712055,229.607712030687,230.607678448957,231.607644867227,
232.607611285497,233.607577703767,234.607544122037,235.607510540307,235.619449019234),
 .UNSPECIFIED.);
#3314=B_SPLINE_CURVE_WITH_KNOTS('',3,(#61317,#61318,#61319,#61320,#61321,
#61322,#61323,#61324,#61325,#61326,#61327),.UNSPECIFIED.,.F.,.F.,(4,1,1,
1,1,1,1,1,4),(229.336263712055,229.479625742723,230.475896680517,231.472167618311,
232.468438556106,233.4647094939,234.460980431694,235.457251369488,235.619449019235),
 .UNSPECIFIED.);
#3315=B_SPLINE_CURVE_WITH_KNOTS('',3,(#61332,#61333,#61334,#61335,#61336,
#61337,#61338,#61339,#61340,#61341),.UNSPECIFIED.,.F.,.F.,(4,1,1,1,1,1,
1,4),(223.053078404875,223.607913521067,224.607879939337,225.607846357607,
226.607812775877,227.607779194147,228.607745612417,229.336263712055),
 .UNSPECIFIED.);
#3316=B_SPLINE_CURVE_WITH_KNOTS('',3,(#61342,#61343,#61344,#61345,#61346,
#61347,#61348,#61349,#61350,#61351),.UNSPECIFIED.,.F.,.F.,(4,1,1,1,1,1,
1,4),(223.053078404875,223.502000115957,224.498271053752,225.494541991546,
226.49081292934,227.487083867134,228.483354804929,229.336263712055),
 .UNSPECIFIED.);
#3317=B_SPLINE_CURVE_WITH_KNOTS('',3,(#61356,#61357,#61358,#61359,#61360,
#61361,#61362,#61363,#61364,#61365),.UNSPECIFIED.,.F.,.F.,(4,1,1,1,1,1,
1,4),(216.769893097696,217.608115011447,218.608081429717,219.608047847987,
220.608014266257,221.607980684527,222.607947102797,223.053078404875),
 .UNSPECIFIED.);
#3318=B_SPLINE_CURVE_WITH_KNOTS('',3,(#61366,#61367,#61368,#61369,#61370,
#61371,#61372,#61373,#61374,#61375),.UNSPECIFIED.,.F.,.F.,(4,1,1,1,1,1,
1,4),(216.769893097696,217.524374489192,218.520645426986,219.51691636478,
220.513187302575,221.509458240369,222.505729178163,223.053078404875),
 .UNSPECIFIED.);
#3319=B_SPLINE_CURVE_WITH_KNOTS('',3,(#61380,#61381,#61382,#61383,#61384,
#61385,#61386,#61387,#61388,#61389,#61390),.UNSPECIFIED.,.F.,.F.,(4,1,1,
1,1,1,1,1,4),(210.486707790516,210.608350083556,211.608316501826,212.608282920096,
213.608249338366,214.608215756636,215.608182174906,216.608148593176,216.769893097696),
 .UNSPECIFIED.);
#3320=B_SPLINE_CURVE_WITH_KNOTS('',3,(#61391,#61392,#61393,#61394,#61395,
#61396,#61397,#61398,#61399,#61400,#61401),.UNSPECIFIED.,.F.,.F.,(4,1,1,
1,1,1,1,1,4),(210.486707790516,210.550477924632,211.546748862427,212.543019800221,
213.539290738015,214.535561675809,215.531832613603,216.528103551398,216.769893097696),
 .UNSPECIFIED.);
#3321=B_SPLINE_CURVE_WITH_KNOTS('',3,(#61406,#61407,#61408,#61409,#61410,
#61411,#61412,#61413,#61414,#61415),.UNSPECIFIED.,.F.,.F.,(4,1,1,1,1,1,
1,4),(204.203522483337,204.608551573936,205.608517992206,206.608484410476,
207.608450828746,208.608417247016,209.608383665286,210.486707790516),
 .UNSPECIFIED.);
#3322=B_SPLINE_CURVE_WITH_KNOTS('',3,(#61416,#61417,#61418,#61419,#61420,
#61421,#61422,#61423,#61424,#61425),.UNSPECIFIED.,.F.,.F.,(4,1,1,1,1,1,
1,4),(204.203522483337,204.572852297867,205.569123235661,206.565394173455,
207.56166511125,208.557936049044,209.554206986838,210.486707790516),
 .UNSPECIFIED.);
#3323=B_SPLINE_CURVE_WITH_KNOTS('',3,(#61430,#61431,#61432,#61433,#61434,
#61435,#61436,#61437,#61438,#61439),.UNSPECIFIED.,.F.,.F.,(4,1,1,1,1,1,
1,4),(197.920337176157,198.608753064316,199.608719482586,200.608685900856,
201.608652319126,202.608618737396,203.608585155666,204.203522483337),
 .UNSPECIFIED.);
#3324=B_SPLINE_CURVE_WITH_KNOTS('',3,(#61440,#61441,#61442,#61443,#61444,
#61445,#61446,#61447,#61448,#61449),.UNSPECIFIED.,.F.,.F.,(4,1,1,1,1,1,
1,4),(197.920337176157,198.595226671101,199.591497608896,200.58776854669,
201.584039484484,202.580310422278,203.576581360073,204.203522483337),
 .UNSPECIFIED.);
#3325=B_SPLINE_CURVE_WITH_KNOTS('',3,(#61454,#61455,#61456,#61457,#61458,
#61459,#61460,#61461,#61462,#61463),.UNSPECIFIED.,.F.,.F.,(4,1,1,1,1,1,
1,4),(191.637151868977,192.608954554696,193.608920972966,194.608887391236,
195.608853809506,196.608820227776,197.608786646046,197.920337176157),
 .UNSPECIFIED.);
#3326=B_SPLINE_CURVE_WITH_KNOTS('',3,(#61464,#61465,#61466,#61467,#61468,
#61469,#61470,#61471,#61472,#61473),.UNSPECIFIED.,.F.,.F.,(4,1,1,1,1,1,
1,4),(191.637151868978,192.617601044336,193.61387198213,194.610142919924,
195.606413857719,196.602684795513,197.598955733307,197.920337176157),
 .UNSPECIFIED.);
#3327=B_SPLINE_CURVE_WITH_KNOTS('',3,(#61478,#61479,#61480,#61481,#61482,
#61483,#61484,#61485,#61486,#61487,#61488),.UNSPECIFIED.,.F.,.F.,(4,1,1,
1,1,1,1,1,4),(185.353966561798,185.609189626805,186.609156045075,187.609122463345,
188.609088881615,189.609055299885,190.609021718155,191.608988136425,191.637151868977),
 .UNSPECIFIED.);
#3328=B_SPLINE_CURVE_WITH_KNOTS('',3,(#61489,#61490,#61491,#61492,#61493,
#61494,#61495,#61496,#61497,#61498,#61499),.UNSPECIFIED.,.F.,.F.,(4,1,1,
1,1,1,1,1,4),(185.353966561798,185.643704479776,186.63997541757,187.636246355365,
188.632517293159,189.628788230953,190.625059168747,191.621330106542,191.637151868978),
 .UNSPECIFIED.);
#3329=B_SPLINE_CURVE_WITH_KNOTS('',3,(#61504,#61505,#61506,#61507,#61508,
#61509,#61510,#61511,#61512,#61513),.UNSPECIFIED.,.F.,.F.,(4,1,1,1,1,1,
1,4),(179.070781254618,179.609391117185,180.609357535455,181.609323953725,
182.609290371995,183.609256790265,184.609223208535,185.353966561798),
 .UNSPECIFIED.);
#3330=B_SPLINE_CURVE_WITH_KNOTS('',3,(#61514,#61515,#61516,#61517,#61518,
#61519,#61520,#61521,#61522,#61523),.UNSPECIFIED.,.F.,.F.,(4,1,1,1,1,1,
1,4),(179.070781254618,179.666078853011,180.662349790805,181.658620728599,
182.654891666394,183.651162604188,184.647433541982,185.353966561798),
 .UNSPECIFIED.);
#3331=B_SPLINE_CURVE_WITH_KNOTS('',3,(#61528,#61529,#61530,#61531,#61532,
#61533,#61534,#61535,#61536,#61537),.UNSPECIFIED.,.F.,.F.,(4,1,1,1,1,1,
1,4),(172.787595947439,173.609592607565,174.609559025835,175.609525444105,
176.609491862375,177.609458280645,178.609424698915,179.070781254618),
 .UNSPECIFIED.);
#3332=B_SPLINE_CURVE_WITH_KNOTS('',3,(#61538,#61539,#61540,#61541,#61542,
#61543,#61544,#61545,#61546,#61547),.UNSPECIFIED.,.F.,.F.,(4,1,1,1,1,1,
1,4),(172.787595947439,173.688453226245,174.68472416404,175.680995101834,
176.677266039628,177.673536977422,178.669807915217,179.070781254618),
 .UNSPECIFIED.);
#3333=B_SPLINE_CURVE_WITH_KNOTS('',3,(#61552,#61553,#61554,#61555,#61556,
#61557,#61558,#61559,#61560,#61561,#61562),.UNSPECIFIED.,.F.,.F.,(4,1,1,
1,1,1,1,1,4),(166.504410640259,166.609827679675,167.609794097945,168.609760516215,
169.609726934485,170.609693352755,171.609659771025,172.609626189295,172.787595947439),
 .UNSPECIFIED.);
#3334=B_SPLINE_CURVE_WITH_KNOTS('',3,(#61563,#61564,#61565,#61566,#61567,
#61568,#61569,#61570,#61571,#61572,#61573),.UNSPECIFIED.,.F.,.F.,(4,1,1,
1,1,1,1,1,4),(166.504410640259,166.714556661686,167.71082759948,168.707098537274,
169.703369475068,170.699640412863,171.695911350657,172.692182288451,172.787595947439),
 .UNSPECIFIED.);
#3335=B_SPLINE_CURVE_WITH_KNOTS('',3,(#61578,#61579,#61580,#61581,#61582,
#61583,#61584,#61585,#61586,#61587),.UNSPECIFIED.,.F.,.F.,(4,1,1,1,1,1,
1,4),(160.22122533308,160.610029170054,161.609995588324,162.609962006594,
163.609928424864,164.609894843134,165.609861261405,166.504410640259),
 .UNSPECIFIED.);
#3336=B_SPLINE_CURVE_WITH_KNOTS('',3,(#61588,#61589,#61590,#61591,#61592,
#61593,#61594,#61595,#61596,#61597),.UNSPECIFIED.,.F.,.F.,(4,1,1,1,1,1,
1,4),(160.22122533308,160.73693103492,161.733201972714,162.729472910509,
163.725743848303,164.722014786097,165.718285723891,166.504410640259),
 .UNSPECIFIED.);
#3337=B_SPLINE_CURVE_WITH_KNOTS('',3,(#61602,#61603,#61604,#61605,#61606,
#61607,#61608,#61609,#61610,#61611),.UNSPECIFIED.,.F.,.F.,(4,1,1,1,1,1,
1,4),(153.9380400259,154.610230660434,155.610197078704,156.610163496974,
157.610129915244,158.610096333514,159.610062751784,160.22122533308),
 .UNSPECIFIED.);
#3338=B_SPLINE_CURVE_WITH_KNOTS('',3,(#61612,#61613,#61614,#61615,#61616,
#61617,#61618,#61619,#61620,#61621),.UNSPECIFIED.,.F.,.F.,(4,1,1,1,1,1,
1,4),(153.9380400259,154.759305408155,155.755576345949,156.751847283743,
157.748118221538,158.744389159332,159.740660097126,160.22122533308),
 .UNSPECIFIED.);
#3339=B_SPLINE_CURVE_WITH_KNOTS('',3,(#61626,#61627,#61628,#61629,#61630,
#61631,#61632,#61633,#61634,#61635),.UNSPECIFIED.,.F.,.F.,(4,1,1,1,1,1,
1,4),(147.654854718721,148.610432150814,149.610398569084,150.610364987354,
151.610331405624,152.610297823894,153.610264242164,153.9380400259),
 .UNSPECIFIED.);
#3340=B_SPLINE_CURVE_WITH_KNOTS('',3,(#61636,#61637,#61638,#61639,#61640,
#61641,#61642,#61643,#61644,#61645,#61646),.UNSPECIFIED.,.F.,.F.,(4,1,1,
1,1,1,1,1,4),(147.654854718721,147.785408843595,148.781679781389,149.777950719184,
150.774221656978,151.770492594772,152.766763532566,153.763034470361,153.9380400259),
 .UNSPECIFIED.);
#3341=B_SPLINE_CURVE_WITH_KNOTS('',3,(#61651,#61652,#61653,#61654,#61655,
#61656,#61657,#61658,#61659,#61660,#61661),.UNSPECIFIED.,.F.,.F.,(4,1,1,
1,1,1,1,1,4),(141.371669411541,141.610667222924,142.610633641194,143.610600059464,
144.610566477734,145.610532896004,146.610499314274,147.610465732544,147.654854718721),
 .UNSPECIFIED.);
#3342=B_SPLINE_CURVE_WITH_KNOTS('',3,(#61662,#61663,#61664,#61665,#61666,
#61667,#61668,#61669,#61670,#61671),.UNSPECIFIED.,.F.,.F.,(4,1,1,1,1,1,
1,4),(141.371669411541,141.80778321683,142.804054154624,143.800325092418,
144.796596030212,145.792866968007,146.789137905801,147.654854718721),
 .UNSPECIFIED.);
#3343=B_SPLINE_CURVE_WITH_KNOTS('',3,(#61676,#61677,#61678,#61679,#61680,
#61681,#61682,#61683,#61684,#61685),.UNSPECIFIED.,.F.,.F.,(4,1,1,1,1,1,
1,4),(135.088484104361,135.610868713303,136.610835131573,137.610801549843,
138.610767968113,139.610734386384,140.610700804654,141.371669411541),
 .UNSPECIFIED.);
#3344=B_SPLINE_CURVE_WITH_KNOTS('',3,(#61686,#61687,#61688,#61689,#61690,
#61691,#61692,#61693,#61694,#61695),.UNSPECIFIED.,.F.,.F.,(4,1,1,1,1,1,
1,4),(135.088484104361,135.830157590064,136.826428527858,137.822699465653,
138.818970403447,139.815241341241,140.811512279035,141.371669411541),
 .UNSPECIFIED.);
#3345=B_SPLINE_CURVE_WITH_KNOTS('',3,(#61700,#61701,#61702,#61703,#61704,
#61705,#61706,#61707,#61708,#61709),.UNSPECIFIED.,.F.,.F.,(4,1,1,1,1,1,
1,4),(128.805298797182,129.611070203683,130.611036621953,131.611003040223,
132.610969458493,133.610935876763,134.610902295033,135.088484104361),
 .UNSPECIFIED.);
#3346=B_SPLINE_CURVE_WITH_KNOTS('',3,(#61710,#61711,#61712,#61713,#61714,
#61715,#61716,#61717,#61718,#61719,#61720),.UNSPECIFIED.,.F.,.F.,(4,1,1,
1,1,1,1,1,4),(128.805298797182,128.856261025505,129.852531963299,130.848802901093,
131.845073838887,132.841344776681,133.837615714476,134.83388665227,135.088484104361),
 .UNSPECIFIED.);
#3347=B_SPLINE_CURVE_WITH_KNOTS('',3,(#61725,#61726,#61727,#61728,#61729,
#61730,#61731,#61732,#61733,#61734,#61735),.UNSPECIFIED.,.F.,.F.,(4,1,1,
1,1,1,1,1,4),(122.522113490002,122.611305275793,123.611271694063,124.611238112333,
125.611204530603,126.611170948873,127.611137367143,128.611103785413,128.805298797182),
 .UNSPECIFIED.);
#3348=B_SPLINE_CURVE_WITH_KNOTS('',3,(#61736,#61737,#61738,#61739,#61740,
#61741,#61742,#61743,#61744,#61745),.UNSPECIFIED.,.F.,.F.,(4,1,1,1,1,1,
1,4),(122.522113490002,122.878635398739,123.874906336533,124.871177274328,
125.867448212122,126.863719149916,127.85999008771,128.805298797182),
 .UNSPECIFIED.);
#3349=B_SPLINE_CURVE_WITH_KNOTS('',3,(#61750,#61751,#61752,#61753,#61754,
#61755,#61756,#61757,#61758,#61759),.UNSPECIFIED.,.F.,.F.,(4,1,1,1,1,1,
1,4),(116.238928182823,116.611506766173,117.611473184443,118.611439602713,
119.611406020983,120.611372439253,121.611338857523,122.522113490002),
 .UNSPECIFIED.);
#3350=B_SPLINE_CURVE_WITH_KNOTS('',3,(#61760,#61761,#61762,#61763,#61764,
#61765,#61766,#61767,#61768,#61769),.UNSPECIFIED.,.F.,.F.,(4,1,1,1,1,1,
1,4),(116.238928182823,116.901009771974,117.897280709768,118.893551647562,
119.889822585356,120.886093523151,121.882364460945,122.522113490002),
 .UNSPECIFIED.);
#3351=B_SPLINE_CURVE_WITH_KNOTS('',3,(#61774,#61775,#61776,#61777,#61778,
#61779,#61780,#61781,#61782,#61783),.UNSPECIFIED.,.F.,.F.,(4,1,1,1,1,1,
1,4),(109.955742875643,110.611708256552,111.611674674822,112.611641093093,
113.611607511363,114.611573929633,115.611540347903,116.238928182823),
 .UNSPECIFIED.);
#3352=B_SPLINE_CURVE_WITH_KNOTS('',3,(#61784,#61785,#61786,#61787,#61788,
#61789,#61790,#61791,#61792,#61793),.UNSPECIFIED.,.F.,.F.,(4,1,1,1,1,1,
1,4),(109.955742875643,110.923384145208,111.919655083002,112.915926020797,
113.912196958591,114.908467896385,115.904738834179,116.238928182823),
 .UNSPECIFIED.);
#3353=B_SPLINE_CURVE_WITH_KNOTS('',3,(#61798,#61799,#61800,#61801,#61802,
#61803,#61804,#61805,#61806,#61807),.UNSPECIFIED.,.F.,.F.,(4,1,1,1,1,1,
1,4),(103.672557568463,104.611909746932,105.611876165202,106.611842583472,
107.611809001742,108.611775420012,109.611741838282,109.955742875643),
 .UNSPECIFIED.);
#3354=B_SPLINE_CURVE_WITH_KNOTS('',3,(#61808,#61809,#61810,#61811,#61812,
#61813,#61814,#61815,#61816,#61817,#61818),.UNSPECIFIED.,.F.,.F.,(4,1,1,
1,1,1,1,1,4),(103.672557568464,103.949487580649,104.945758518443,105.942029456237,
106.938300394031,107.934571331825,108.93084226962,109.927113207414,109.955742875643),
 .UNSPECIFIED.);
#3355=B_SPLINE_CURVE_WITH_KNOTS('',3,(#61823,#61824,#61825,#61826,#61827,
#61828,#61829,#61830,#61831,#61832,#61833),.UNSPECIFIED.,.F.,.F.,(4,1,1,
1,1,1,1,1,4),(97.3893722612839,97.612144819042,98.612111237312,99.612077655582,
100.612044073852,101.612010492122,102.611976910392,103.611943328662,103.672557568463),
 .UNSPECIFIED.);
#3356=B_SPLINE_CURVE_WITH_KNOTS('',3,(#61834,#61835,#61836,#61837,#61838,
#61839,#61840,#61841,#61842,#61843),.UNSPECIFIED.,.F.,.F.,(4,1,1,1,1,1,
1,4),(97.389372261284,97.9718619538831,98.9681328916773,99.9644038294716,
100.960674767266,101.95694570506,102.953216642854,103.672557568464),
 .UNSPECIFIED.);
#3357=B_SPLINE_CURVE_WITH_KNOTS('',3,(#61848,#61849,#61850,#61851,#61852,
#61853,#61854,#61855,#61856,#61857),.UNSPECIFIED.,.F.,.F.,(4,1,1,1,1,1,
1,4),(91.1061869541042,91.6123463094217,92.6123127276918,93.6122791459618,
94.6122455642318,95.6122119825019,96.6121784007719,97.3893722612839),
 .UNSPECIFIED.);
#3358=B_SPLINE_CURVE_WITH_KNOTS('',3,(#61858,#61859,#61860,#61861,#61862,
#61863,#61864,#61865,#61866,#61867),.UNSPECIFIED.,.F.,.F.,(4,1,1,1,1,1,
1,4),(91.1061869541043,91.9942363271176,92.9905072649119,93.9867782027061,
94.9830491405003,95.9793200782946,96.9755910160888,97.389372261284),
 .UNSPECIFIED.);
#3359=B_SPLINE_CURVE_WITH_KNOTS('',3,(#61872,#61873,#61874,#61875,#61876,
#61877,#61878,#61879,#61880,#61881),.UNSPECIFIED.,.F.,.F.,(4,1,1,1,1,1,
1,4),(84.8230016469247,85.6125477998015,86.6125142180715,87.6124806363416,
88.6124470546116,89.6124134728817,90.6123798911517,91.1061869541042),
 .UNSPECIFIED.);
#3360=B_SPLINE_CURVE_WITH_KNOTS('',3,(#61882,#61883,#61884,#61885,#61886,
#61887,#61888,#61889,#61890,#61891,#61892),.UNSPECIFIED.,.F.,.F.,(4,1,1,
1,1,1,1,1,4),(84.8230016469248,85.0203397625579,86.0166107003522,87.0128816381464,
88.0091525759407,89.0054235137349,90.0016944515291,90.9979653893234,91.1061869541043),
 .UNSPECIFIED.);
#3361=B_SPLINE_CURVE_WITH_KNOTS('',3,(#61897,#61898,#61899,#61900,#61901,
#61902,#61903,#61904,#61905,#61906,#61907),.UNSPECIFIED.,.F.,.F.,(4,1,1,
1,1,1,1,1,4),(78.5398163397451,78.6127828719112,79.6127492901813,80.6127157084513,
81.6126821267214,82.6126485449914,83.6126149632614,84.6125813815315,84.8230016469247),
 .UNSPECIFIED.);
#3362=B_SPLINE_CURVE_WITH_KNOTS('',3,(#61908,#61909,#61910,#61911,#61912,
#61913,#61914,#61915,#61916,#61917),.UNSPECIFIED.,.F.,.F.,(4,1,1,1,1,1,
1,4),(78.5398163397452,79.0427141357925,80.0389850735867,81.035256011381,
82.0315269491752,83.0277978869695,84.0240688247637,84.8230016469248),
 .UNSPECIFIED.);
#3363=B_SPLINE_CURVE_WITH_KNOTS('',3,(#61922,#61923,#61924,#61925,#61926,
#61927,#61928,#61929,#61930,#61931),.UNSPECIFIED.,.F.,.F.,(4,1,1,1,1,1,
1,4),(72.2566310325655,72.612984362291,73.612950780561,74.6129171988311,
75.6128836171011,76.6128500353712,77.6128164536412,78.5398163397451),
 .UNSPECIFIED.);
#3364=B_SPLINE_CURVE_WITH_KNOTS('',3,(#61932,#61933,#61934,#61935,#61936,
#61937,#61938,#61939,#61940,#61941),.UNSPECIFIED.,.F.,.F.,(4,1,1,1,1,1,
1,4),(72.2566310325656,73.065088509027,74.0613594468213,75.0576303846155,
76.0539013224098,77.050172260204,78.0464431979982,78.5398163397452),
 .UNSPECIFIED.);
#3365=B_SPLINE_CURVE_WITH_KNOTS('',3,(#61946,#61947,#61948,#61949,#61950,
#61951,#61952,#61953,#61954,#61955),.UNSPECIFIED.,.F.,.F.,(4,1,1,1,1,1,
1,4),(65.9734457253859,66.6131858526708,67.6131522709408,68.6131186892109,
69.6130851074809,70.6130515257509,71.613017944021,72.2566310325655),
 .UNSPECIFIED.);
#3366=B_SPLINE_CURVE_WITH_KNOTS('',3,(#61956,#61957,#61958,#61959,#61960,
#61961,#61962,#61963,#61964,#61965,#61966),.UNSPECIFIED.,.F.,.F.,(4,1,1,
1,1,1,1,1,4),(65.973445725386,66.0911919444674,67.0874628822616,68.0837338200558,
69.0800047578501,70.0762756956443,71.0725466334385,72.0688175712328,72.2566310325656),
 .UNSPECIFIED.);
#3367=B_SPLINE_CURVE_WITH_KNOTS('',3,(#61971,#61972,#61973,#61974,#61975,
#61976,#61977,#61978,#61979,#61980),.UNSPECIFIED.,.F.,.F.,(4,1,1,1,1,1,
1,4),(59.6902604182063,60.6133873430505,61.6133537613206,62.6133201795906,
63.6132865978607,64.6132530161307,65.6132194344007,65.9734457253859),
 .UNSPECIFIED.);
#3368=B_SPLINE_CURVE_WITH_KNOTS('',3,(#61981,#61982,#61983,#61984,#61985,
#61986,#61987,#61988,#61989,#61990),.UNSPECIFIED.,.F.,.F.,(4,1,1,1,1,1,
1,4),(59.6902604182064,60.1135663177019,61.1098372554961,62.1061081932904,
63.1023791310846,64.0986500688789,65.0949210066731,65.973445725386),
 .UNSPECIFIED.);
#3369=B_SPLINE_CURVE_WITH_KNOTS('',3,(#61995,#61996,#61997,#61998,#61999,
#62000,#62001,#62002,#62003,#62004,#62005),.UNSPECIFIED.,.F.,.F.,(4,1,1,
1,1,1,1,1,4),(53.4070751110267,53.6136224151603,54.6135888334303,55.6135552517004,
56.6135216699704,57.6134880882404,58.6134545065105,59.6134209247805,59.6902604182063),
 .UNSPECIFIED.);
#3370=B_SPLINE_CURVE_WITH_KNOTS('',3,(#62006,#62007,#62008,#62009,#62010,
#62011,#62012,#62013,#62014,#62015),.UNSPECIFIED.,.F.,.F.,(4,1,1,1,1,1,
1,4),(53.4070751110268,54.1359406909365,55.1322116287307,56.1284825665249,
57.1247535043192,58.1210244421134,59.1172953799077,59.6902604182064),
 .UNSPECIFIED.);
#3371=B_SPLINE_CURVE_WITH_KNOTS('',3,(#62020,#62021,#62022,#62023,#62024,
#62025,#62026,#62027,#62028,#62029),.UNSPECIFIED.,.F.,.F.,(4,1,1,1,1,1,
1,4),(47.1238898038471,47.6138239055401,48.6137903238101,49.6137567420801,
50.6137231603502,51.6136895786202,52.6136559968902,53.4070751110267),
 .UNSPECIFIED.);
#3372=B_SPLINE_CURVE_WITH_KNOTS('',3,(#62030,#62031,#62032,#62033,#62034,
#62035,#62036,#62037,#62038,#62039,#62040),.UNSPECIFIED.,.F.,.F.,(4,1,1,
1,1,1,1,1,4),(47.1238898038472,47.1620441263768,48.158315064171,49.1545860019653,
50.1508569397595,51.1471278775537,52.143398815348,53.1396697531422,53.4070751110268),
 .UNSPECIFIED.);
#3373=B_SPLINE_CURVE_WITH_KNOTS('',3,(#62045,#62046,#62047,#62048,#62049,
#62050,#62051,#62052,#62053,#62054),.UNSPECIFIED.,.F.,.F.,(4,1,1,1,1,1,
1,4),(40.8407044966675,41.6140253959198,42.6139918141899,43.6139582324599,
44.6139246507299,45.613891069,46.61385748727,47.1238898038471),
 .UNSPECIFIED.);
#3374=B_SPLINE_CURVE_WITH_KNOTS('',3,(#62055,#62056,#62057,#62058,#62059,
#62060,#62061,#62062,#62063,#62064),.UNSPECIFIED.,.F.,.F.,(4,1,1,1,1,1,
1,4),(40.8407044966676,41.1844184996113,42.1806894374056,43.1769603751998,
44.1732313129941,45.1695022507883,46.1657731885825,47.1238898038472),
 .UNSPECIFIED.);
#3375=B_SPLINE_CURVE_WITH_KNOTS('',3,(#62069,#62070,#62071,#62072,#62073,
#62074,#62075,#62076,#62077,#62078,#62079),.UNSPECIFIED.,.F.,.F.,(4,1,1,
1,1,1,1,1,4),(34.5575191894879,34.6142604680296,35.6142268862996,36.6141933045696,
37.6141597228397,38.6141261411097,39.6140925593798,40.6140589776498,40.8407044966675),
 .UNSPECIFIED.);
#3376=B_SPLINE_CURVE_WITH_KNOTS('',3,(#62080,#62081,#62082,#62083,#62084,
#62085,#62086,#62087,#62088,#62089),.UNSPECIFIED.,.F.,.F.,(4,1,1,1,1,1,
1,4),(34.557519189488,35.2067928728459,36.2030638106401,37.1993347484344,
38.1956056862286,39.1918766240228,40.1881475618171,40.8407044966676),
 .UNSPECIFIED.);
#3377=B_SPLINE_CURVE_WITH_KNOTS('',3,(#62094,#62095,#62096,#62097,#62098,
#62099,#62100,#62101,#62102,#62103),.UNSPECIFIED.,.F.,.F.,(4,1,1,1,1,1,
1,4),(28.2743338823083,28.6144619584093,29.6144283766794,30.6143947949494,
31.6143612132194,32.6143276314895,33.6142940497595,34.5575191894879),
 .UNSPECIFIED.);
#3378=B_SPLINE_CURVE_WITH_KNOTS('',3,(#62104,#62105,#62106,#62107,#62108,
#62109,#62110,#62111,#62112,#62113),.UNSPECIFIED.,.F.,.F.,(4,1,1,1,1,1,
1,4),(28.2743338823084,29.2291672460804,30.2254381838747,31.2217091216689,
32.2179800594632,33.2142509972574,34.2105219350516,34.557519189488),
 .UNSPECIFIED.);
#3379=B_SPLINE_CURVE_WITH_KNOTS('',3,(#62118,#62119,#62120,#62121,#62122,
#62123,#62124,#62125,#62126,#62127),.UNSPECIFIED.,.F.,.F.,(4,1,1,1,1,1,
1,4),(21.9911485751287,22.6146634487891,23.6146298670591,24.6145962853292,
25.6145627035992,26.6145291218693,27.6144955401393,28.2743338823083),
 .UNSPECIFIED.);
#3380=B_SPLINE_CURVE_WITH_KNOTS('',3,(#62128,#62129,#62130,#62131,#62132,
#62133,#62134,#62135,#62136,#62137,#62138),.UNSPECIFIED.,.F.,.F.,(4,1,1,
1,1,1,1,1,4),(21.9911485751289,22.2552706815207,23.251541619315,24.2478125571092,
25.2440834949035,26.2403544326977,27.236625370492,28.2328963082862,28.2743338823084),
 .UNSPECIFIED.);
#3381=B_SPLINE_CURVE_WITH_KNOTS('',3,(#62143,#62144,#62145,#62146,#62147,
#62148,#62149,#62150,#62151,#62152),.UNSPECIFIED.,.F.,.F.,(4,1,1,1,1,1,
1,4),(15.7079632679492,16.6148649391689,17.6148313574389,18.614797775709,
19.614764193979,20.614730612249,21.6146970305191,21.9911485751287),
 .UNSPECIFIED.);
#3382=B_SPLINE_CURVE_WITH_KNOTS('',3,(#62153,#62154,#62155,#62156,#62157,
#62158,#62159,#62160,#62161,#62162),.UNSPECIFIED.,.F.,.F.,(4,1,1,1,1,1,
1,4),(15.7079632679493,16.2776450547553,17.2739159925495,18.2701869303438,
19.266457868138,20.2627288059323,21.2589997437265,21.9911485751289),
 .UNSPECIFIED.);
#3383=B_SPLINE_CURVE_WITH_KNOTS('',3,(#62165,#62166,#62167,#62168,#62169,
#62170,#62171,#62172,#62173,#62174,#62175,#62176,#62177,#62178,#62179,#62180,
#62181,#62182,#62183,#62184,#62185,#62186,#62187,#62188,#62189,#62190,#62191,
#62192,#62193,#62194,#62195,#62196,#62197,#62198,#62199,#62200,#62201,#62202,
#62203,#62204,#62205,#62206,#62207,#62208,#62209,#62210,#62211,#62212,#62213,
#62214,#62215,#62216,#62217,#62218,#62219,#62220,#62221,#62222,#62223,#62224,
#62225,#62226,#62227,#62228,#62229,#62230,#62231,#62232,#62233,#62234,#62235,
#62236,#62237,#62238,#62239,#62240,#62241,#62242,#62243,#62244,#62245,#62246,
#62247,#62248,#62249,#62250,#62251,#62252,#62253,#62254,#62255,#62256,#62257,
#62258,#62259,#62260,#62261,#62262,#62263,#62264,#62265,#62266,#62267,#62268,
#62269,#62270,#62271,#62272,#62273,#62274,#62275,#62276,#62277,#62278,#62279,
#62280,#62281,#62282,#62283,#62284,#62285,#62286,#62287,#62288,#62289,#62290,
#62291,#62292,#62293,#62294,#62295,#62296,#62297,#62298,#62299,#62300,#62301,
#62302,#62303,#62304,#62305,#62306,#62307,#62308,#62309,#62310,#62311,#62312,
#62313,#62314,#62315,#62316,#62317,#62318,#62319,#62320,#62321,#62322,#62323,
#62324,#62325,#62326,#62327,#62328,#62329,#62330,#62331,#62332,#62333,#62334,
#62335,#62336,#62337,#62338,#62339,#62340,#62341,#62342,#62343,#62344,#62345,
#62346,#62347,#62348,#62349,#62350,#62351,#62352,#62353,#62354,#62355,#62356,
#62357,#62358,#62359,#62360,#62361,#62362,#62363,#62364,#62365,#62366,#62367,
#62368,#62369,#62370,#62371,#62372,#62373,#62374,#62375,#62376,#62377,#62378,
#62379,#62380,#62381,#62382,#62383,#62384,#62385,#62386,#62387,#62388,#62389,
#62390),.UNSPECIFIED.,.F.,.F.,(4,3,3,3,3,3,3,3,3,3,3,3,3,3,3,3,3,3,3,3,
3,3,3,3,3,3,3,3,3,3,3,3,3,3,3,3,3,3,3,3,3,3,3,3,3,3,3,3,3,3,3,3,3,3,3,3,
3,3,3,3,3,3,3,3,3,3,3,3,3,3,3,3,3,3,3,4),(-1.5115530493712,-1.48679646988231,
-1.46138327157041,-1.44931403653187,-1.44201521738479,-1.4372364069369,
-1.41130073666512,-1.3851364793294,-1.36882167524197,-1.36489335463821,
-1.33844118737752,-1.31212405971847,-1.29019978533613,-1.27923764814496,
-1.27341919949145,-1.26903466137048,-1.26827551095379,-1.24293973226305,
-1.21686129007046,-1.19161648481995,-1.18057188252285,-1.17415589095891,
-1.17024744553752,-1.14344439633044,-1.11634682592921,-1.0909858314635,
-1.08147545853886,-1.07621433222182,-1.07212128966627,-1.04351206886633,
-1.0165509628589,-1.01490284806638,-0.988030199407108,-0.977552081199909,
-0.973437277723626,-0.945726987414166,-0.918214262331309,-0.890537857808272,
-0.880398328972147,-0.87237005911237,-0.867956987444107,-0.838906479395067,
-0.811044859415748,-0.783625034708112,-0.772915569760388,-0.768645334133187,
-0.764137890402299,-0.751754955247948,-0.724693670921933,-0.696925419694083,
-0.669642708112985,-0.663192181598675,-0.658947817948324,-0.630700019923219,
-0.602103353566958,-0.573605985023947,-0.561738202776617,-0.556716888407782,
-0.552057825803808,-0.523179250890329,-0.494755452697743,-0.478663727045304,
-0.462934741526935,-0.451680956559048,-0.447722787491454,-0.419466033709138,
-0.390586852248759,-0.36140366189149,-0.344603198998977,-0.339184578268993,
-0.335360215694789,-0.305911623051275,-0.276431237914502,-0.247572950493138,
-0.22699995875139,-0.219677966287888),.UNSPECIFIED.);
#3384=B_SPLINE_CURVE_WITH_KNOTS('',3,(#62392,#62393,#62394,#62395,#62396,
#62397,#62398,#62399,#62400,#62401,#62402,#62403,#62404,#62405,#62406,#62407,
#62408,#62409,#62410,#62411,#62412,#62413,#62414,#62415,#62416,#62417,#62418,
#62419,#62420,#62421,#62422,#62423,#62424,#62425,#62426,#62427,#62428,#62429,
#62430,#62431,#62432,#62433,#62434,#62435,#62436,#62437,#62438,#62439,#62440,
#62441,#62442,#62443,#62444,#62445,#62446,#62447,#62448,#62449,#62450,#62451,
#62452,#62453,#62454,#62455),.UNSPECIFIED.,.F.,.F.,(4,3,3,3,3,3,3,3,3,3,
3,3,3,3,3,3,3,3,3,3,3,4),(-0.410648750432358,-0.381299282375245,-0.351451987365484,
-0.32338277226279,-0.31441918992071,-0.307886057995154,-0.302748807341755,
-0.275195476204274,-0.2619101023362,-0.23366962500355,-0.204460921878106,
-0.199264215741705,-0.195568173418504,-0.168370897549803,-0.141281081328714,
-0.114654976955625,-0.100323104836172,-0.0960558144650962,-0.0702818786829607,
-0.044890002900036,-0.02024436392036,0.),.UNSPECIFIED.);
#3385=B_SPLINE_CURVE_WITH_KNOTS('',3,(#62458,#62459,#62460,#62461,#62462,
#62463,#62464,#62465,#62466,#62467,#62468,#62469,#62470,#62471,#62472,#62473,
#62474,#62475,#62476,#62477,#62478,#62479,#62480,#62481,#62482,#62483,#62484,
#62485,#62486,#62487,#62488),.UNSPECIFIED.,.F.,.F.,(4,3,3,3,3,3,3,3,3,3,
4),(-0.219677966287888,-0.195864471024291,-0.166952662475248,-0.137468548387315,
-0.120284979838901,-0.114251963704818,-0.109988263453048,-0.080302546936133,
-0.0502597344232586,-0.0203206940376301,0.),.UNSPECIFIED.);
#3386=B_SPLINE_CURVE_WITH_KNOTS('',3,(#63501,#63502,#63503,#63504,#63505,
#63506,#63507,#63508),.UNSPECIFIED.,.F.,.F.,(4,1,1,1,1,4),(11.6150328478187,
12.6149992660887,13.6149656843588,14.6149321026288,15.6148985208988,15.7079632679492),
 .UNSPECIFIED.);
#3387=B_SPLINE_CURVE_WITH_KNOTS('',3,(#63509,#63510,#63511,#63512,#63513,
#63514,#63515,#63516,#63517,#63518,#63519,#63520,#63521,#63522,#63523,#63524,
#63525,#63526,#63527,#63528,#63529,#63530,#63531,#63532,#63533,#63534,#63535,
#63536,#63537,#63538,#63539,#63540,#63541,#63542,#63543,#63544,#63545,#63546,
#63547,#63548,#63549,#63550,#63551,#63552,#63553,#63554,#63555,#63556,#63557,
#63558,#63559,#63560,#63561,#63562,#63563,#63564,#63565,#63566,#63567,#63568,
#63569,#63570,#63571,#63572,#63573,#63574,#63575,#63576,#63577,#63578,#63579,
#63580,#63581,#63582,#63583,#63584,#63585,#63586,#63587,#63588,#63589,#63590,
#63591,#63592,#63593,#63594,#63595,#63596,#63597,#63598,#63599,#63600,#63601,
#63602),.UNSPECIFIED.,.F.,.F.,(4,3,3,3,3,3,3,3,3,3,3,3,3,3,3,3,3,3,3,3,
3,3,3,3,3,3,3,3,3,3,3,4),(-0.552745378375066,-0.53257041253064,-0.503209833963106,
-0.487569744740098,-0.475817235384553,-0.470703937755808,-0.441646149367916,
-0.418061431496298,-0.407743117427465,-0.402003725693741,-0.397456462704961,
-0.369148821319412,-0.340103717588302,-0.312985901936444,-0.297779959016177,
-0.291309037186587,-0.264507979745426,-0.252968406394974,-0.225608178960633,
-0.197407156590554,-0.192288000083304,-0.188202033999832,-0.161559009732277,
-0.134959874297392,-0.108788470827791,-0.0997870868716052,-0.094523571416419,
-0.0902265394264102,-0.064682595398749,-0.0395411867789222,-0.0151843303020833,
0.),.UNSPECIFIED.);
#3388=B_SPLINE_CURVE_WITH_KNOTS('',3,(#63603,#63604,#63605,#63606,#63607,
#63608,#63609,#63610,#63611,#63612,#63613,#63614,#63615,#63616,#63617,#63618,
#63619,#63620,#63621),.UNSPECIFIED.,.F.,.F.,(4,3,3,3,3,3,4),(-247.477289902729,
-246.991705312699,-245.991738894429,-244.991772476159,-243.991806057889,
-242.991839639619,-242.853972092955),.UNSPECIFIED.);
#3389=B_SPLINE_CURVE_WITH_KNOTS('',3,(#63624,#63625,#63626,#63627,#63628,
#63629,#63630,#63631,#63632),.UNSPECIFIED.,.F.,.F.,(4,1,1,1,1,1,4),(10.3761157273106,
11.2962903657841,12.2925613035783,13.2888322413726,14.2851031791668,15.2813741169611,
15.7079632679493),.UNSPECIFIED.);
#3390=B_SPLINE_CURVE_WITH_KNOTS('',3,(#64654,#64655,#64656,#64657,#64658,
#64659,#64660,#64661,#64662,#64663,#64664,#64665,#64666,#64667,#64668,#64669,
#64670,#64671,#64672,#64673,#64674,#64675),.UNSPECIFIED.,.F.,.F.,(4,3,3,
3,3,3,3,4),(239.878342081193,240.101296008412,241.097566946206,242.093837884001,
243.090108821795,244.086379759589,245.082650697383,245.40865172782),
 .UNSPECIFIED.);
#3391=B_SPLINE_CURVE_WITH_KNOTS('',3,(#64676,#64677,#64678,#64679,#64680,
#64681,#64682,#64683,#64684,#64685,#64686,#64687,#64688,#64689,#64690,#64691,
#64692,#64693,#64694,#64695,#64696,#64697,#64698,#64699,#64700,#64701,#64702,
#64703,#64704,#64705,#64706,#64707,#64708,#64709,#64710,#64711,#64712,#64713,
#64714,#64715,#64716,#64717,#64718,#64719,#64720,#64721,#64722,#64723,#64724,
#64725,#64726,#64727,#64728,#64729,#64730,#64731,#64732,#64733,#64734,#64735,
#64736,#64737,#64738,#64739,#64740,#64741,#64742,#64743,#64744,#64745,#64746,
#64747,#64748,#64749,#64750,#64751,#64752,#64753,#64754,#64755,#64756,#64757,
#64758,#64759,#64760,#64761,#64762,#64763,#64764,#64765,#64766),
 .UNSPECIFIED.,.F.,.F.,(4,3,3,3,3,3,3,3,3,3,3,3,3,3,3,3,3,3,3,3,3,3,3,3,
3,3,3,3,3,3,4),(-0.555272788399356,-0.536933533817927,-0.512218003438917,
-0.497827681018193,-0.492206798870043,-0.487869646287534,-0.462091513356309,
-0.439576679775185,-0.428764166378627,-0.422010894528083,-0.395425506675213,
-0.367062341183239,-0.345789967064259,-0.329835686475024,-0.325431154183988,
-0.320888849595204,-0.292973404720077,-0.281972844707319,-0.255027785728263,
-0.227542539987006,-0.221779606338387,-0.218030423923514,-0.190105025722723,
-0.161634029602592,-0.13290803371308,-0.116294529498945,-0.111891296080701,
-0.0824377575584239,-0.0528856925172319,-0.0238818739582312,0.),
 .UNSPECIFIED.);
#4190=LINE('',#59296,#5038);
#4191=LINE('',#59320,#5039);
#4192=LINE('',#59368,#5040);
#4193=LINE('',#59416,#5041);
#4194=LINE('',#59467,#5042);
#4195=LINE('',#59518,#5043);
#4196=LINE('',#59566,#5044);
#4197=LINE('',#59614,#5045);
#4198=LINE('',#59668,#5046);
#4199=LINE('',#59716,#5047);
#4200=LINE('',#59764,#5048);
#4201=LINE('',#59815,#5049);
#4202=LINE('',#59866,#5050);
#4203=LINE('',#59914,#5051);
#4204=LINE('',#59965,#5052);
#4205=LINE('',#60016,#5053);
#4206=LINE('',#60064,#5054);
#4207=LINE('',#60115,#5055);
#4208=LINE('',#60163,#5056);
#4209=LINE('',#60214,#5057);
#4210=LINE('',#60262,#5058);
#4211=LINE('',#60313,#5059);
#4212=LINE('',#60364,#5060);
#4213=LINE('',#60412,#5061);
#4214=LINE('',#60463,#5062);
#4215=LINE('',#60511,#5063);
#4216=LINE('',#60562,#5064);
#4217=LINE('',#60613,#5065);
#4218=LINE('',#60661,#5066);
#4219=LINE('',#60712,#5067);
#4220=LINE('',#60763,#5068);
#4221=LINE('',#60811,#5069);
#4222=LINE('',#60859,#5070);
#4223=LINE('',#60910,#5071);
#4224=LINE('',#60961,#5072);
#4225=LINE('',#61009,#5073);
#4226=LINE('',#61060,#5074);
#4227=LINE('',#61111,#5075);
#4228=LINE('',#61159,#5076);
#4229=LINE('',#61207,#5077);
#4230=LINE('',#61232,#5078);
#4231=LINE('',#61257,#5079);
#4232=LINE('',#61281,#5080);
#4233=LINE('',#61305,#5081);
#4234=LINE('',#61331,#5082);
#4235=LINE('',#61355,#5083);
#4236=LINE('',#61379,#5084);
#4237=LINE('',#61405,#5085);
#4238=LINE('',#61429,#5086);
#4239=LINE('',#61453,#5087);
#4240=LINE('',#61477,#5088);
#4241=LINE('',#61503,#5089);
#4242=LINE('',#61527,#5090);
#4243=LINE('',#61551,#5091);
#4244=LINE('',#61577,#5092);
#4245=LINE('',#61601,#5093);
#4246=LINE('',#61625,#5094);
#4247=LINE('',#61650,#5095);
#4248=LINE('',#61675,#5096);
#4249=LINE('',#61699,#5097);
#4250=LINE('',#61724,#5098);
#4251=LINE('',#61749,#5099);
#4252=LINE('',#61773,#5100);
#4253=LINE('',#61797,#5101);
#4254=LINE('',#61822,#5102);
#4255=LINE('',#61847,#5103);
#4256=LINE('',#61871,#5104);
#4257=LINE('',#61896,#5105);
#4258=LINE('',#61921,#5106);
#4259=LINE('',#61945,#5107);
#4260=LINE('',#61970,#5108);
#4261=LINE('',#61994,#5109);
#4262=LINE('',#62019,#5110);
#4263=LINE('',#62044,#5111);
#4264=LINE('',#62068,#5112);
#4265=LINE('',#62093,#5113);
#4266=LINE('',#62117,#5114);
#4267=LINE('',#62142,#5115);
#4268=LINE('',#62490,#5116);
#4269=LINE('',#64771,#5117);
#4270=LINE('',#64773,#5118);
#4271=LINE('',#64775,#5119);
#4272=LINE('',#64776,#5120);
#4273=LINE('',#64779,#5121);
#4274=LINE('',#64781,#5122);
#4275=LINE('',#64782,#5123);
#4276=LINE('',#64785,#5124);
#4277=LINE('',#64787,#5125);
#4278=LINE('',#64788,#5126);
#4279=LINE('',#64791,#5127);
#4280=LINE('',#64793,#5128);
#4281=LINE('',#64794,#5129);
#4282=LINE('',#64797,#5130);
#4283=LINE('',#64799,#5131);
#4284=LINE('',#64800,#5132);
#4285=LINE('',#64802,#5133);
#4286=LINE('',#64803,#5134);
#4287=LINE('',#64810,#5135);
#5038=VECTOR('',#18032,3.);
#5039=VECTOR('',#18037,3.);
#5040=VECTOR('',#18040,3.);
#5041=VECTOR('',#18043,3.);
#5042=VECTOR('',#18046,3.);
#5043=VECTOR('',#18049,3.);
#5044=VECTOR('',#18052,3.);
#5045=VECTOR('',#18055,3.);
#5046=VECTOR('',#18058,3.);
#5047=VECTOR('',#18061,3.);
#5048=VECTOR('',#18064,3.);
#5049=VECTOR('',#18067,3.);
#5050=VECTOR('',#18070,3.);
#5051=VECTOR('',#18073,3.);
#5052=VECTOR('',#18076,3.);
#5053=VECTOR('',#18079,3.);
#5054=VECTOR('',#18082,3.);
#5055=VECTOR('',#18085,3.);
#5056=VECTOR('',#18088,3.);
#5057=VECTOR('',#18091,3.);
#5058=VECTOR('',#18094,3.);
#5059=VECTOR('',#18097,3.);
#5060=VECTOR('',#18100,3.);
#5061=VECTOR('',#18103,3.);
#5062=VECTOR('',#18106,3.);
#5063=VECTOR('',#18109,3.);
#5064=VECTOR('',#18112,3.);
#5065=VECTOR('',#18115,3.);
#5066=VECTOR('',#18118,3.);
#5067=VECTOR('',#18121,3.);
#5068=VECTOR('',#18124,3.);
#5069=VECTOR('',#18127,3.);
#5070=VECTOR('',#18130,3.);
#5071=VECTOR('',#18133,3.);
#5072=VECTOR('',#18136,3.);
#5073=VECTOR('',#18139,3.);
#5074=VECTOR('',#18142,3.);
#5075=VECTOR('',#18145,3.);
#5076=VECTOR('',#18148,3.);
#5077=VECTOR('',#18151,2.37175);
#5078=VECTOR('',#18156,2.37175);
#5079=VECTOR('',#18159,2.37175);
#5080=VECTOR('',#18162,2.37175);
#5081=VECTOR('',#18165,2.37175);
#5082=VECTOR('',#18168,2.37175);
#5083=VECTOR('',#18171,2.37175);
#5084=VECTOR('',#18174,2.37175);
#5085=VECTOR('',#18177,2.37175);
#5086=VECTOR('',#18180,2.37175);
#5087=VECTOR('',#18183,2.37175);
#5088=VECTOR('',#18186,2.37175);
#5089=VECTOR('',#18189,2.37175);
#5090=VECTOR('',#18192,2.37175);
#5091=VECTOR('',#18195,2.37175);
#5092=VECTOR('',#18198,2.37175);
#5093=VECTOR('',#18201,2.37175);
#5094=VECTOR('',#18204,2.37175);
#5095=VECTOR('',#18207,2.37175);
#5096=VECTOR('',#18210,2.37175);
#5097=VECTOR('',#18213,2.37175);
#5098=VECTOR('',#18216,2.37175);
#5099=VECTOR('',#18219,2.37175);
#5100=VECTOR('',#18222,2.37175);
#5101=VECTOR('',#18225,2.37175);
#5102=VECTOR('',#18228,2.37175);
#5103=VECTOR('',#18231,2.37175);
#5104=VECTOR('',#18234,2.37175);
#5105=VECTOR('',#18237,2.37175);
#5106=VECTOR('',#18240,2.37175);
#5107=VECTOR('',#18243,2.37175);
#5108=VECTOR('',#18246,2.37175);
#5109=VECTOR('',#18249,2.37175);
#5110=VECTOR('',#18252,2.37175);
#5111=VECTOR('',#18255,2.37175);
#5112=VECTOR('',#18258,2.37175);
#5113=VECTOR('',#18261,2.37175);
#5114=VECTOR('',#18264,2.37175);
#5115=VECTOR('',#18267,2.37175);
#5116=VECTOR('',#18272,2.5);
#5117=VECTOR('',#18283,10.);
#5118=VECTOR('',#18284,10.);
#5119=VECTOR('',#18285,10.);
#5120=VECTOR('',#18286,10.);
#5121=VECTOR('',#18289,10.);
#5122=VECTOR('',#18290,10.);
#5123=VECTOR('',#18291,10.);
#5124=VECTOR('',#18294,10.);
#5125=VECTOR('',#18295,10.);
#5126=VECTOR('',#18296,10.);
#5127=VECTOR('',#18299,10.);
#5128=VECTOR('',#18300,10.);
#5129=VECTOR('',#18301,10.);
#5130=VECTOR('',#18304,10.);
#5131=VECTOR('',#18305,10.);
#5132=VECTOR('',#18306,10.);
#5133=VECTOR('',#18309,10.);
#5134=VECTOR('',#18310,10.);
#5135=VECTOR('',#18319,5.);
#6361=VERTEX_POINT('',#59294);
#6362=VERTEX_POINT('',#59295);
#6363=VERTEX_POINT('',#59297);
#6364=VERTEX_POINT('',#59308);
#6365=VERTEX_POINT('',#59318);
#6366=VERTEX_POINT('',#59319);
#6367=VERTEX_POINT('',#59366);
#6368=VERTEX_POINT('',#59367);
#6369=VERTEX_POINT('',#59414);
#6370=VERTEX_POINT('',#59415);
#6371=VERTEX_POINT('',#59465);
#6372=VERTEX_POINT('',#59466);
#6373=VERTEX_POINT('',#59516);
#6374=VERTEX_POINT('',#59517);
#6375=VERTEX_POINT('',#59564);
#6376=VERTEX_POINT('',#59565);
#6377=VERTEX_POINT('',#59612);
#6378=VERTEX_POINT('',#59613);
#6379=VERTEX_POINT('',#59666);
#6380=VERTEX_POINT('',#59667);
#6381=VERTEX_POINT('',#59714);
#6382=VERTEX_POINT('',#59715);
#6383=VERTEX_POINT('',#59762);
#6384=VERTEX_POINT('',#59763);
#6385=VERTEX_POINT('',#59813);
#6386=VERTEX_POINT('',#59814);
#6387=VERTEX_POINT('',#59864);
#6388=VERTEX_POINT('',#59865);
#6389=VERTEX_POINT('',#59912);
#6390=VERTEX_POINT('',#59913);
#6391=VERTEX_POINT('',#59963);
#6392=VERTEX_POINT('',#59964);
#6393=VERTEX_POINT('',#60014);
#6394=VERTEX_POINT('',#60015);
#6395=VERTEX_POINT('',#60062);
#6396=VERTEX_POINT('',#60063);
#6397=VERTEX_POINT('',#60113);
#6398=VERTEX_POINT('',#60114);
#6399=VERTEX_POINT('',#60161);
#6400=VERTEX_POINT('',#60162);
#6401=VERTEX_POINT('',#60212);
#6402=VERTEX_POINT('',#60213);
#6403=VERTEX_POINT('',#60260);
#6404=VERTEX_POINT('',#60261);
#6405=VERTEX_POINT('',#60311);
#6406=VERTEX_POINT('',#60312);
#6407=VERTEX_POINT('',#60362);
#6408=VERTEX_POINT('',#60363);
#6409=VERTEX_POINT('',#60410);
#6410=VERTEX_POINT('',#60411);
#6411=VERTEX_POINT('',#60461);
#6412=VERTEX_POINT('',#60462);
#6413=VERTEX_POINT('',#60509);
#6414=VERTEX_POINT('',#60510);
#6415=VERTEX_POINT('',#60560);
#6416=VERTEX_POINT('',#60561);
#6417=VERTEX_POINT('',#60611);
#6418=VERTEX_POINT('',#60612);
#6419=VERTEX_POINT('',#60659);
#6420=VERTEX_POINT('',#60660);
#6421=VERTEX_POINT('',#60710);
#6422=VERTEX_POINT('',#60711);
#6423=VERTEX_POINT('',#60761);
#6424=VERTEX_POINT('',#60762);
#6425=VERTEX_POINT('',#60809);
#6426=VERTEX_POINT('',#60810);
#6427=VERTEX_POINT('',#60857);
#6428=VERTEX_POINT('',#60858);
#6429=VERTEX_POINT('',#60908);
#6430=VERTEX_POINT('',#60909);
#6431=VERTEX_POINT('',#60959);
#6432=VERTEX_POINT('',#60960);
#6433=VERTEX_POINT('',#61007);
#6434=VERTEX_POINT('',#61008);
#6435=VERTEX_POINT('',#61058);
#6436=VERTEX_POINT('',#61059);
#6437=VERTEX_POINT('',#61109);
#6438=VERTEX_POINT('',#61110);
#6439=VERTEX_POINT('',#61157);
#6440=VERTEX_POINT('',#61158);
#6441=VERTEX_POINT('',#61205);
#6442=VERTEX_POINT('',#61206);
#6443=VERTEX_POINT('',#61208);
#6444=VERTEX_POINT('',#61219);
#6445=VERTEX_POINT('',#61230);
#6446=VERTEX_POINT('',#61231);
#6447=VERTEX_POINT('',#61255);
#6448=VERTEX_POINT('',#61256);
#6449=VERTEX_POINT('',#61279);
#6450=VERTEX_POINT('',#61280);
#6451=VERTEX_POINT('',#61303);
#6452=VERTEX_POINT('',#61304);
#6453=VERTEX_POINT('',#61329);
#6454=VERTEX_POINT('',#61330);
#6455=VERTEX_POINT('',#61353);
#6456=VERTEX_POINT('',#61354);
#6457=VERTEX_POINT('',#61377);
#6458=VERTEX_POINT('',#61378);
#6459=VERTEX_POINT('',#61403);
#6460=VERTEX_POINT('',#61404);
#6461=VERTEX_POINT('',#61427);
#6462=VERTEX_POINT('',#61428);
#6463=VERTEX_POINT('',#61451);
#6464=VERTEX_POINT('',#61452);
#6465=VERTEX_POINT('',#61475);
#6466=VERTEX_POINT('',#61476);
#6467=VERTEX_POINT('',#61501);
#6468=VERTEX_POINT('',#61502);
#6469=VERTEX_POINT('',#61525);
#6470=VERTEX_POINT('',#61526);
#6471=VERTEX_POINT('',#61549);
#6472=VERTEX_POINT('',#61550);
#6473=VERTEX_POINT('',#61575);
#6474=VERTEX_POINT('',#61576);
#6475=VERTEX_POINT('',#61599);
#6476=VERTEX_POINT('',#61600);
#6477=VERTEX_POINT('',#61623);
#6478=VERTEX_POINT('',#61624);
#6479=VERTEX_POINT('',#61648);
#6480=VERTEX_POINT('',#61649);
#6481=VERTEX_POINT('',#61673);
#6482=VERTEX_POINT('',#61674);
#6483=VERTEX_POINT('',#61697);
#6484=VERTEX_POINT('',#61698);
#6485=VERTEX_POINT('',#61722);
#6486=VERTEX_POINT('',#61723);
#6487=VERTEX_POINT('',#61747);
#6488=VERTEX_POINT('',#61748);
#6489=VERTEX_POINT('',#61771);
#6490=VERTEX_POINT('',#61772);
#6491=VERTEX_POINT('',#61795);
#6492=VERTEX_POINT('',#61796);
#6493=VERTEX_POINT('',#61820);
#6494=VERTEX_POINT('',#61821);
#6495=VERTEX_POINT('',#61845);
#6496=VERTEX_POINT('',#61846);
#6497=VERTEX_POINT('',#61869);
#6498=VERTEX_POINT('',#61870);
#6499=VERTEX_POINT('',#61894);
#6500=VERTEX_POINT('',#61895);
#6501=VERTEX_POINT('',#61919);
#6502=VERTEX_POINT('',#61920);
#6503=VERTEX_POINT('',#61943);
#6504=VERTEX_POINT('',#61944);
#6505=VERTEX_POINT('',#61968);
#6506=VERTEX_POINT('',#61969);
#6507=VERTEX_POINT('',#61992);
#6508=VERTEX_POINT('',#61993);
#6509=VERTEX_POINT('',#62017);
#6510=VERTEX_POINT('',#62018);
#6511=VERTEX_POINT('',#62042);
#6512=VERTEX_POINT('',#62043);
#6513=VERTEX_POINT('',#62066);
#6514=VERTEX_POINT('',#62067);
#6515=VERTEX_POINT('',#62091);
#6516=VERTEX_POINT('',#62092);
#6517=VERTEX_POINT('',#62115);
#6518=VERTEX_POINT('',#62116);
#6519=VERTEX_POINT('',#62140);
#6520=VERTEX_POINT('',#62141);
#6521=VERTEX_POINT('',#62164);
#6522=VERTEX_POINT('',#62391);
#6523=VERTEX_POINT('',#62456);
#6524=VERTEX_POINT('',#62489);
#6525=VERTEX_POINT('',#63500);
#6526=VERTEX_POINT('',#63623);
#6527=VERTEX_POINT('',#64769);
#6528=VERTEX_POINT('',#64770);
#6529=VERTEX_POINT('',#64772);
#6530=VERTEX_POINT('',#64774);
#6531=VERTEX_POINT('',#64778);
#6532=VERTEX_POINT('',#64780);
#6533=VERTEX_POINT('',#64784);
#6534=VERTEX_POINT('',#64786);
#6535=VERTEX_POINT('',#64790);
#6536=VERTEX_POINT('',#64792);
#6537=VERTEX_POINT('',#64796);
#6538=VERTEX_POINT('',#64798);
#6539=VERTEX_POINT('',#64806);
#6540=VERTEX_POINT('',#64809);
#8416=EDGE_CURVE('',#6361,#6362,#4190,.T.);
#8417=EDGE_CURVE('',#6361,#6363,#3227,.T.);
#8418=EDGE_CURVE('',#6363,#6364,#2327,.F.);
#8419=EDGE_CURVE('',#6364,#6362,#3228,.T.);
#8420=EDGE_CURVE('',#6365,#6366,#4191,.T.);
#8421=EDGE_CURVE('',#6365,#6361,#3229,.T.);
#8422=EDGE_CURVE('',#6362,#6366,#3230,.T.);
#8423=EDGE_CURVE('',#6367,#6368,#4192,.T.);
#8424=EDGE_CURVE('',#6367,#6365,#3231,.T.);
#8425=EDGE_CURVE('',#6366,#6368,#3232,.T.);
#8426=EDGE_CURVE('',#6369,#6370,#4193,.T.);
#8427=EDGE_CURVE('',#6369,#6367,#3233,.T.);
#8428=EDGE_CURVE('',#6368,#6370,#3234,.T.);
#8429=EDGE_CURVE('',#6371,#6372,#4194,.T.);
#8430=EDGE_CURVE('',#6371,#6369,#3235,.T.);
#8431=EDGE_CURVE('',#6370,#6372,#3236,.T.);
#8432=EDGE_CURVE('',#6373,#6374,#4195,.T.);
#8433=EDGE_CURVE('',#6373,#6371,#3237,.T.);
#8434=EDGE_CURVE('',#6372,#6374,#3238,.T.);
#8435=EDGE_CURVE('',#6375,#6376,#4196,.T.);
#8436=EDGE_CURVE('',#6375,#6373,#3239,.T.);
#8437=EDGE_CURVE('',#6374,#6376,#3240,.T.);
#8438=EDGE_CURVE('',#6377,#6378,#4197,.T.);
#8439=EDGE_CURVE('',#6377,#6375,#3241,.T.);
#8440=EDGE_CURVE('',#6376,#6378,#3242,.T.);
#8441=EDGE_CURVE('',#6379,#6380,#4198,.T.);
#8442=EDGE_CURVE('',#6379,#6377,#3243,.T.);
#8443=EDGE_CURVE('',#6378,#6380,#3244,.T.);
#8444=EDGE_CURVE('',#6381,#6382,#4199,.T.);
#8445=EDGE_CURVE('',#6381,#6379,#3245,.T.);
#8446=EDGE_CURVE('',#6380,#6382,#3246,.T.);
#8447=EDGE_CURVE('',#6383,#6384,#4200,.T.);
#8448=EDGE_CURVE('',#6383,#6381,#3247,.T.);
#8449=EDGE_CURVE('',#6382,#6384,#3248,.T.);
#8450=EDGE_CURVE('',#6385,#6386,#4201,.T.);
#8451=EDGE_CURVE('',#6385,#6383,#3249,.T.);
#8452=EDGE_CURVE('',#6384,#6386,#3250,.T.);
#8453=EDGE_CURVE('',#6387,#6388,#4202,.T.);
#8454=EDGE_CURVE('',#6387,#6385,#3251,.T.);
#8455=EDGE_CURVE('',#6386,#6388,#3252,.T.);
#8456=EDGE_CURVE('',#6389,#6390,#4203,.T.);
#8457=EDGE_CURVE('',#6389,#6387,#3253,.T.);
#8458=EDGE_CURVE('',#6388,#6390,#3254,.T.);
#8459=EDGE_CURVE('',#6391,#6392,#4204,.T.);
#8460=EDGE_CURVE('',#6391,#6389,#3255,.T.);
#8461=EDGE_CURVE('',#6390,#6392,#3256,.T.);
#8462=EDGE_CURVE('',#6393,#6394,#4205,.T.);
#8463=EDGE_CURVE('',#6393,#6391,#3257,.T.);
#8464=EDGE_CURVE('',#6392,#6394,#3258,.T.);
#8465=EDGE_CURVE('',#6395,#6396,#4206,.T.);
#8466=EDGE_CURVE('',#6395,#6393,#3259,.T.);
#8467=EDGE_CURVE('',#6394,#6396,#3260,.T.);
#8468=EDGE_CURVE('',#6397,#6398,#4207,.T.);
#8469=EDGE_CURVE('',#6397,#6395,#3261,.T.);
#8470=EDGE_CURVE('',#6396,#6398,#3262,.T.);
#8471=EDGE_CURVE('',#6399,#6400,#4208,.T.);
#8472=EDGE_CURVE('',#6399,#6397,#3263,.T.);
#8473=EDGE_CURVE('',#6398,#6400,#3264,.T.);
#8474=EDGE_CURVE('',#6401,#6402,#4209,.T.);
#8475=EDGE_CURVE('',#6401,#6399,#3265,.T.);
#8476=EDGE_CURVE('',#6400,#6402,#3266,.T.);
#8477=EDGE_CURVE('',#6403,#6404,#4210,.T.);
#8478=EDGE_CURVE('',#6403,#6401,#3267,.T.);
#8479=EDGE_CURVE('',#6402,#6404,#3268,.T.);
#8480=EDGE_CURVE('',#6405,#6406,#4211,.T.);
#8481=EDGE_CURVE('',#6405,#6403,#3269,.T.);
#8482=EDGE_CURVE('',#6404,#6406,#3270,.T.);
#8483=EDGE_CURVE('',#6407,#6408,#4212,.T.);
#8484=EDGE_CURVE('',#6407,#6405,#3271,.T.);
#8485=EDGE_CURVE('',#6406,#6408,#3272,.T.);
#8486=EDGE_CURVE('',#6409,#6410,#4213,.T.);
#8487=EDGE_CURVE('',#6409,#6407,#3273,.T.);
#8488=EDGE_CURVE('',#6408,#6410,#3274,.T.);
#8489=EDGE_CURVE('',#6411,#6412,#4214,.T.);
#8490=EDGE_CURVE('',#6411,#6409,#3275,.T.);
#8491=EDGE_CURVE('',#6410,#6412,#3276,.T.);
#8492=EDGE_CURVE('',#6413,#6414,#4215,.T.);
#8493=EDGE_CURVE('',#6413,#6411,#3277,.T.);
#8494=EDGE_CURVE('',#6412,#6414,#3278,.T.);
#8495=EDGE_CURVE('',#6415,#6416,#4216,.T.);
#8496=EDGE_CURVE('',#6415,#6413,#3279,.T.);
#8497=EDGE_CURVE('',#6414,#6416,#3280,.T.);
#8498=EDGE_CURVE('',#6417,#6418,#4217,.T.);
#8499=EDGE_CURVE('',#6417,#6415,#3281,.T.);
#8500=EDGE_CURVE('',#6416,#6418,#3282,.T.);
#8501=EDGE_CURVE('',#6419,#6420,#4218,.T.);
#8502=EDGE_CURVE('',#6419,#6417,#3283,.T.);
#8503=EDGE_CURVE('',#6418,#6420,#3284,.T.);
#8504=EDGE_CURVE('',#6421,#6422,#4219,.T.);
#8505=EDGE_CURVE('',#6421,#6419,#3285,.T.);
#8506=EDGE_CURVE('',#6420,#6422,#3286,.T.);
#8507=EDGE_CURVE('',#6423,#6424,#4220,.T.);
#8508=EDGE_CURVE('',#6423,#6421,#3287,.T.);
#8509=EDGE_CURVE('',#6422,#6424,#3288,.T.);
#8510=EDGE_CURVE('',#6425,#6426,#4221,.T.);
#8511=EDGE_CURVE('',#6425,#6423,#3289,.T.);
#8512=EDGE_CURVE('',#6424,#6426,#3290,.T.);
#8513=EDGE_CURVE('',#6427,#6428,#4222,.T.);
#8514=EDGE_CURVE('',#6427,#6425,#3291,.T.);
#8515=EDGE_CURVE('',#6426,#6428,#3292,.T.);
#8516=EDGE_CURVE('',#6429,#6430,#4223,.T.);
#8517=EDGE_CURVE('',#6429,#6427,#3293,.T.);
#8518=EDGE_CURVE('',#6428,#6430,#3294,.T.);
#8519=EDGE_CURVE('',#6431,#6432,#4224,.T.);
#8520=EDGE_CURVE('',#6431,#6429,#3295,.T.);
#8521=EDGE_CURVE('',#6430,#6432,#3296,.T.);
#8522=EDGE_CURVE('',#6433,#6434,#4225,.T.);
#8523=EDGE_CURVE('',#6433,#6431,#3297,.T.);
#8524=EDGE_CURVE('',#6432,#6434,#3298,.T.);
#8525=EDGE_CURVE('',#6435,#6436,#4226,.T.);
#8526=EDGE_CURVE('',#6435,#6433,#3299,.T.);
#8527=EDGE_CURVE('',#6434,#6436,#3300,.T.);
#8528=EDGE_CURVE('',#6437,#6438,#4227,.T.);
#8529=EDGE_CURVE('',#6437,#6435,#3301,.T.);
#8530=EDGE_CURVE('',#6436,#6438,#3302,.T.);
#8531=EDGE_CURVE('',#6439,#6440,#4228,.T.);
#8532=EDGE_CURVE('',#6439,#6437,#3303,.T.);
#8533=EDGE_CURVE('',#6438,#6440,#3304,.T.);
#8534=EDGE_CURVE('',#6441,#6442,#4229,.T.);
#8535=EDGE_CURVE('',#6441,#6443,#3305,.T.);
#8536=EDGE_CURVE('',#6443,#6444,#2328,.T.);
#8537=EDGE_CURVE('',#6442,#6444,#3306,.T.);
#8538=EDGE_CURVE('',#6445,#6446,#4230,.T.);
#8539=EDGE_CURVE('',#6445,#6441,#3307,.T.);
#8540=EDGE_CURVE('',#6446,#6442,#3308,.T.);
#8541=EDGE_CURVE('',#6447,#6448,#4231,.T.);
#8542=EDGE_CURVE('',#6447,#6445,#3309,.T.);
#8543=EDGE_CURVE('',#6448,#6446,#3310,.T.);
#8544=EDGE_CURVE('',#6449,#6450,#4232,.T.);
#8545=EDGE_CURVE('',#6449,#6447,#3311,.T.);
#8546=EDGE_CURVE('',#6450,#6448,#3312,.T.);
#8547=EDGE_CURVE('',#6451,#6452,#4233,.T.);
#8548=EDGE_CURVE('',#6451,#6449,#3313,.T.);
#8549=EDGE_CURVE('',#6452,#6450,#3314,.T.);
#8550=EDGE_CURVE('',#6453,#6454,#4234,.T.);
#8551=EDGE_CURVE('',#6453,#6451,#3315,.T.);
#8552=EDGE_CURVE('',#6454,#6452,#3316,.T.);
#8553=EDGE_CURVE('',#6455,#6456,#4235,.T.);
#8554=EDGE_CURVE('',#6455,#6453,#3317,.T.);
#8555=EDGE_CURVE('',#6456,#6454,#3318,.T.);
#8556=EDGE_CURVE('',#6457,#6458,#4236,.T.);
#8557=EDGE_CURVE('',#6457,#6455,#3319,.T.);
#8558=EDGE_CURVE('',#6458,#6456,#3320,.T.);
#8559=EDGE_CURVE('',#6459,#6460,#4237,.T.);
#8560=EDGE_CURVE('',#6459,#6457,#3321,.T.);
#8561=EDGE_CURVE('',#6460,#6458,#3322,.T.);
#8562=EDGE_CURVE('',#6461,#6462,#4238,.T.);
#8563=EDGE_CURVE('',#6461,#6459,#3323,.T.);
#8564=EDGE_CURVE('',#6462,#6460,#3324,.T.);
#8565=EDGE_CURVE('',#6463,#6464,#4239,.T.);
#8566=EDGE_CURVE('',#6463,#6461,#3325,.T.);
#8567=EDGE_CURVE('',#6464,#6462,#3326,.T.);
#8568=EDGE_CURVE('',#6465,#6466,#4240,.T.);
#8569=EDGE_CURVE('',#6465,#6463,#3327,.T.);
#8570=EDGE_CURVE('',#6466,#6464,#3328,.T.);
#8571=EDGE_CURVE('',#6467,#6468,#4241,.T.);
#8572=EDGE_CURVE('',#6467,#6465,#3329,.T.);
#8573=EDGE_CURVE('',#6468,#6466,#3330,.T.);
#8574=EDGE_CURVE('',#6469,#6470,#4242,.T.);
#8575=EDGE_CURVE('',#6469,#6467,#3331,.T.);
#8576=EDGE_CURVE('',#6470,#6468,#3332,.T.);
#8577=EDGE_CURVE('',#6471,#6472,#4243,.T.);
#8578=EDGE_CURVE('',#6471,#6469,#3333,.T.);
#8579=EDGE_CURVE('',#6472,#6470,#3334,.T.);
#8580=EDGE_CURVE('',#6473,#6474,#4244,.T.);
#8581=EDGE_CURVE('',#6473,#6471,#3335,.T.);
#8582=EDGE_CURVE('',#6474,#6472,#3336,.T.);
#8583=EDGE_CURVE('',#6475,#6476,#4245,.T.);
#8584=EDGE_CURVE('',#6475,#6473,#3337,.T.);
#8585=EDGE_CURVE('',#6476,#6474,#3338,.T.);
#8586=EDGE_CURVE('',#6477,#6478,#4246,.T.);
#8587=EDGE_CURVE('',#6477,#6475,#3339,.T.);
#8588=EDGE_CURVE('',#6478,#6476,#3340,.T.);
#8589=EDGE_CURVE('',#6479,#6480,#4247,.T.);
#8590=EDGE_CURVE('',#6479,#6477,#3341,.T.);
#8591=EDGE_CURVE('',#6480,#6478,#3342,.T.);
#8592=EDGE_CURVE('',#6481,#6482,#4248,.T.);
#8593=EDGE_CURVE('',#6481,#6479,#3343,.T.);
#8594=EDGE_CURVE('',#6482,#6480,#3344,.T.);
#8595=EDGE_CURVE('',#6483,#6484,#4249,.T.);
#8596=EDGE_CURVE('',#6483,#6481,#3345,.T.);
#8597=EDGE_CURVE('',#6484,#6482,#3346,.T.);
#8598=EDGE_CURVE('',#6485,#6486,#4250,.T.);
#8599=EDGE_CURVE('',#6485,#6483,#3347,.T.);
#8600=EDGE_CURVE('',#6486,#6484,#3348,.T.);
#8601=EDGE_CURVE('',#6487,#6488,#4251,.T.);
#8602=EDGE_CURVE('',#6487,#6485,#3349,.T.);
#8603=EDGE_CURVE('',#6488,#6486,#3350,.T.);
#8604=EDGE_CURVE('',#6489,#6490,#4252,.T.);
#8605=EDGE_CURVE('',#6489,#6487,#3351,.T.);
#8606=EDGE_CURVE('',#6490,#6488,#3352,.T.);
#8607=EDGE_CURVE('',#6491,#6492,#4253,.T.);
#8608=EDGE_CURVE('',#6491,#6489,#3353,.T.);
#8609=EDGE_CURVE('',#6492,#6490,#3354,.T.);
#8610=EDGE_CURVE('',#6493,#6494,#4254,.T.);
#8611=EDGE_CURVE('',#6493,#6491,#3355,.T.);
#8612=EDGE_CURVE('',#6494,#6492,#3356,.T.);
#8613=EDGE_CURVE('',#6495,#6496,#4255,.T.);
#8614=EDGE_CURVE('',#6495,#6493,#3357,.T.);
#8615=EDGE_CURVE('',#6496,#6494,#3358,.T.);
#8616=EDGE_CURVE('',#6497,#6498,#4256,.T.);
#8617=EDGE_CURVE('',#6497,#6495,#3359,.T.);
#8618=EDGE_CURVE('',#6498,#6496,#3360,.T.);
#8619=EDGE_CURVE('',#6499,#6500,#4257,.T.);
#8620=EDGE_CURVE('',#6499,#6497,#3361,.T.);
#8621=EDGE_CURVE('',#6500,#6498,#3362,.T.);
#8622=EDGE_CURVE('',#6501,#6502,#4258,.T.);
#8623=EDGE_CURVE('',#6501,#6499,#3363,.T.);
#8624=EDGE_CURVE('',#6502,#6500,#3364,.T.);
#8625=EDGE_CURVE('',#6503,#6504,#4259,.T.);
#8626=EDGE_CURVE('',#6503,#6501,#3365,.T.);
#8627=EDGE_CURVE('',#6504,#6502,#3366,.T.);
#8628=EDGE_CURVE('',#6505,#6506,#4260,.T.);
#8629=EDGE_CURVE('',#6505,#6503,#3367,.T.);
#8630=EDGE_CURVE('',#6506,#6504,#3368,.T.);
#8631=EDGE_CURVE('',#6507,#6508,#4261,.T.);
#8632=EDGE_CURVE('',#6507,#6505,#3369,.T.);
#8633=EDGE_CURVE('',#6508,#6506,#3370,.T.);
#8634=EDGE_CURVE('',#6509,#6510,#4262,.T.);
#8635=EDGE_CURVE('',#6509,#6507,#3371,.T.);
#8636=EDGE_CURVE('',#6510,#6508,#3372,.T.);
#8637=EDGE_CURVE('',#6511,#6512,#4263,.T.);
#8638=EDGE_CURVE('',#6511,#6509,#3373,.T.);
#8639=EDGE_CURVE('',#6512,#6510,#3374,.T.);
#8640=EDGE_CURVE('',#6513,#6514,#4264,.T.);
#8641=EDGE_CURVE('',#6513,#6511,#3375,.T.);
#8642=EDGE_CURVE('',#6514,#6512,#3376,.T.);
#8643=EDGE_CURVE('',#6515,#6516,#4265,.T.);
#8644=EDGE_CURVE('',#6515,#6513,#3377,.T.);
#8645=EDGE_CURVE('',#6516,#6514,#3378,.T.);
#8646=EDGE_CURVE('',#6517,#6518,#4266,.T.);
#8647=EDGE_CURVE('',#6517,#6515,#3379,.T.);
#8648=EDGE_CURVE('',#6518,#6516,#3380,.T.);
#8649=EDGE_CURVE('',#6519,#6520,#4267,.T.);
#8650=EDGE_CURVE('',#6519,#6517,#3381,.T.);
#8651=EDGE_CURVE('',#6520,#6518,#3382,.T.);
#8652=EDGE_CURVE('',#6444,#6521,#3383,.T.);
#8653=EDGE_CURVE('',#6522,#6443,#3384,.T.);
#8654=EDGE_CURVE('',#6523,#6522,#2329,.T.);
#8655=EDGE_CURVE('',#6521,#6523,#3385,.T.);
#8656=EDGE_CURVE('',#6521,#6524,#4268,.T.);
#8657=EDGE_CURVE('',#6524,#6524,#2330,.T.);
#8658=EDGE_CURVE('',#6525,#6519,#3386,.T.);
#8659=EDGE_CURVE('',#6363,#6525,#3387,.T.);
#8660=EDGE_CURVE('',#6522,#6439,#3388,.T.);
#8661=EDGE_CURVE('',#6526,#6520,#3389,.T.);
#8662=EDGE_CURVE('',#6525,#6526,#2331,.T.);
#8663=EDGE_CURVE('',#6440,#6523,#3390,.T.);
#8664=EDGE_CURVE('',#6526,#6364,#3391,.T.);
#8665=EDGE_CURVE('',#6527,#6528,#4269,.T.);
#8666=EDGE_CURVE('',#6527,#6529,#4270,.T.);
#8667=EDGE_CURVE('',#6529,#6530,#4271,.T.);
#8668=EDGE_CURVE('',#6528,#6530,#4272,.T.);
#8669=EDGE_CURVE('',#6531,#6527,#4273,.T.);
#8670=EDGE_CURVE('',#6531,#6532,#4274,.T.);
#8671=EDGE_CURVE('',#6532,#6529,#4275,.T.);
#8672=EDGE_CURVE('',#6533,#6531,#4276,.T.);
#8673=EDGE_CURVE('',#6533,#6534,#4277,.T.);
#8674=EDGE_CURVE('',#6534,#6532,#4278,.T.);
#8675=EDGE_CURVE('',#6535,#6533,#4279,.T.);
#8676=EDGE_CURVE('',#6535,#6536,#4280,.T.);
#8677=EDGE_CURVE('',#6536,#6534,#4281,.T.);
#8678=EDGE_CURVE('',#6537,#6535,#4282,.T.);
#8679=EDGE_CURVE('',#6537,#6538,#4283,.T.);
#8680=EDGE_CURVE('',#6538,#6536,#4284,.T.);
#8681=EDGE_CURVE('',#6528,#6537,#4285,.T.);
#8682=EDGE_CURVE('',#6530,#6538,#4286,.T.);
#8683=EDGE_CURVE('',#6539,#6539,#2332,.T.);
#8684=EDGE_CURVE('',#6539,#6540,#4287,.T.);
#8685=EDGE_CURVE('',#6540,#6540,#2333,.T.);
#12359=ORIENTED_EDGE('',*,*,#8416,.F.);
#12360=ORIENTED_EDGE('',*,*,#8417,.T.);
#12361=ORIENTED_EDGE('',*,*,#8418,.T.);
#12362=ORIENTED_EDGE('',*,*,#8419,.T.);
#12363=ORIENTED_EDGE('',*,*,#8420,.F.);
#12364=ORIENTED_EDGE('',*,*,#8421,.T.);
#12365=ORIENTED_EDGE('',*,*,#8416,.T.);
#12366=ORIENTED_EDGE('',*,*,#8422,.T.);
#12367=ORIENTED_EDGE('',*,*,#8423,.F.);
#12368=ORIENTED_EDGE('',*,*,#8424,.T.);
#12369=ORIENTED_EDGE('',*,*,#8420,.T.);
#12370=ORIENTED_EDGE('',*,*,#8425,.T.);
#12371=ORIENTED_EDGE('',*,*,#8426,.F.);
#12372=ORIENTED_EDGE('',*,*,#8427,.T.);
#12373=ORIENTED_EDGE('',*,*,#8423,.T.);
#12374=ORIENTED_EDGE('',*,*,#8428,.T.);
#12375=ORIENTED_EDGE('',*,*,#8429,.F.);
#12376=ORIENTED_EDGE('',*,*,#8430,.T.);
#12377=ORIENTED_EDGE('',*,*,#8426,.T.);
#12378=ORIENTED_EDGE('',*,*,#8431,.T.);
#12379=ORIENTED_EDGE('',*,*,#8432,.F.);
#12380=ORIENTED_EDGE('',*,*,#8433,.T.);
#12381=ORIENTED_EDGE('',*,*,#8429,.T.);
#12382=ORIENTED_EDGE('',*,*,#8434,.T.);
#12383=ORIENTED_EDGE('',*,*,#8435,.F.);
#12384=ORIENTED_EDGE('',*,*,#8436,.T.);
#12385=ORIENTED_EDGE('',*,*,#8432,.T.);
#12386=ORIENTED_EDGE('',*,*,#8437,.T.);
#12387=ORIENTED_EDGE('',*,*,#8438,.F.);
#12388=ORIENTED_EDGE('',*,*,#8439,.T.);
#12389=ORIENTED_EDGE('',*,*,#8435,.T.);
#12390=ORIENTED_EDGE('',*,*,#8440,.T.);
#12391=ORIENTED_EDGE('',*,*,#8441,.F.);
#12392=ORIENTED_EDGE('',*,*,#8442,.T.);
#12393=ORIENTED_EDGE('',*,*,#8438,.T.);
#12394=ORIENTED_EDGE('',*,*,#8443,.T.);
#12395=ORIENTED_EDGE('',*,*,#8444,.F.);
#12396=ORIENTED_EDGE('',*,*,#8445,.T.);
#12397=ORIENTED_EDGE('',*,*,#8441,.T.);
#12398=ORIENTED_EDGE('',*,*,#8446,.T.);
#12399=ORIENTED_EDGE('',*,*,#8447,.F.);
#12400=ORIENTED_EDGE('',*,*,#8448,.T.);
#12401=ORIENTED_EDGE('',*,*,#8444,.T.);
#12402=ORIENTED_EDGE('',*,*,#8449,.T.);
#12403=ORIENTED_EDGE('',*,*,#8450,.F.);
#12404=ORIENTED_EDGE('',*,*,#8451,.T.);
#12405=ORIENTED_EDGE('',*,*,#8447,.T.);
#12406=ORIENTED_EDGE('',*,*,#8452,.T.);
#12407=ORIENTED_EDGE('',*,*,#8453,.F.);
#12408=ORIENTED_EDGE('',*,*,#8454,.T.);
#12409=ORIENTED_EDGE('',*,*,#8450,.T.);
#12410=ORIENTED_EDGE('',*,*,#8455,.T.);
#12411=ORIENTED_EDGE('',*,*,#8456,.F.);
#12412=ORIENTED_EDGE('',*,*,#8457,.T.);
#12413=ORIENTED_EDGE('',*,*,#8453,.T.);
#12414=ORIENTED_EDGE('',*,*,#8458,.T.);
#12415=ORIENTED_EDGE('',*,*,#8459,.F.);
#12416=ORIENTED_EDGE('',*,*,#8460,.T.);
#12417=ORIENTED_EDGE('',*,*,#8456,.T.);
#12418=ORIENTED_EDGE('',*,*,#8461,.T.);
#12419=ORIENTED_EDGE('',*,*,#8462,.F.);
#12420=ORIENTED_EDGE('',*,*,#8463,.T.);
#12421=ORIENTED_EDGE('',*,*,#8459,.T.);
#12422=ORIENTED_EDGE('',*,*,#8464,.T.);
#12423=ORIENTED_EDGE('',*,*,#8465,.F.);
#12424=ORIENTED_EDGE('',*,*,#8466,.T.);
#12425=ORIENTED_EDGE('',*,*,#8462,.T.);
#12426=ORIENTED_EDGE('',*,*,#8467,.T.);
#12427=ORIENTED_EDGE('',*,*,#8468,.F.);
#12428=ORIENTED_EDGE('',*,*,#8469,.T.);
#12429=ORIENTED_EDGE('',*,*,#8465,.T.);
#12430=ORIENTED_EDGE('',*,*,#8470,.T.);
#12431=ORIENTED_EDGE('',*,*,#8471,.F.);
#12432=ORIENTED_EDGE('',*,*,#8472,.T.);
#12433=ORIENTED_EDGE('',*,*,#8468,.T.);
#12434=ORIENTED_EDGE('',*,*,#8473,.T.);
#12435=ORIENTED_EDGE('',*,*,#8474,.F.);
#12436=ORIENTED_EDGE('',*,*,#8475,.T.);
#12437=ORIENTED_EDGE('',*,*,#8471,.T.);
#12438=ORIENTED_EDGE('',*,*,#8476,.T.);
#12439=ORIENTED_EDGE('',*,*,#8477,.F.);
#12440=ORIENTED_EDGE('',*,*,#8478,.T.);
#12441=ORIENTED_EDGE('',*,*,#8474,.T.);
#12442=ORIENTED_EDGE('',*,*,#8479,.T.);
#12443=ORIENTED_EDGE('',*,*,#8480,.F.);
#12444=ORIENTED_EDGE('',*,*,#8481,.T.);
#12445=ORIENTED_EDGE('',*,*,#8477,.T.);
#12446=ORIENTED_EDGE('',*,*,#8482,.T.);
#12447=ORIENTED_EDGE('',*,*,#8483,.F.);
#12448=ORIENTED_EDGE('',*,*,#8484,.T.);
#12449=ORIENTED_EDGE('',*,*,#8480,.T.);
#12450=ORIENTED_EDGE('',*,*,#8485,.T.);
#12451=ORIENTED_EDGE('',*,*,#8486,.F.);
#12452=ORIENTED_EDGE('',*,*,#8487,.T.);
#12453=ORIENTED_EDGE('',*,*,#8483,.T.);
#12454=ORIENTED_EDGE('',*,*,#8488,.T.);
#12455=ORIENTED_EDGE('',*,*,#8489,.F.);
#12456=ORIENTED_EDGE('',*,*,#8490,.T.);
#12457=ORIENTED_EDGE('',*,*,#8486,.T.);
#12458=ORIENTED_EDGE('',*,*,#8491,.T.);
#12459=ORIENTED_EDGE('',*,*,#8492,.F.);
#12460=ORIENTED_EDGE('',*,*,#8493,.T.);
#12461=ORIENTED_EDGE('',*,*,#8489,.T.);
#12462=ORIENTED_EDGE('',*,*,#8494,.T.);
#12463=ORIENTED_EDGE('',*,*,#8495,.F.);
#12464=ORIENTED_EDGE('',*,*,#8496,.T.);
#12465=ORIENTED_EDGE('',*,*,#8492,.T.);
#12466=ORIENTED_EDGE('',*,*,#8497,.T.);
#12467=ORIENTED_EDGE('',*,*,#8498,.F.);
#12468=ORIENTED_EDGE('',*,*,#8499,.T.);
#12469=ORIENTED_EDGE('',*,*,#8495,.T.);
#12470=ORIENTED_EDGE('',*,*,#8500,.T.);
#12471=ORIENTED_EDGE('',*,*,#8501,.F.);
#12472=ORIENTED_EDGE('',*,*,#8502,.T.);
#12473=ORIENTED_EDGE('',*,*,#8498,.T.);
#12474=ORIENTED_EDGE('',*,*,#8503,.T.);
#12475=ORIENTED_EDGE('',*,*,#8504,.F.);
#12476=ORIENTED_EDGE('',*,*,#8505,.T.);
#12477=ORIENTED_EDGE('',*,*,#8501,.T.);
#12478=ORIENTED_EDGE('',*,*,#8506,.T.);
#12479=ORIENTED_EDGE('',*,*,#8507,.F.);
#12480=ORIENTED_EDGE('',*,*,#8508,.T.);
#12481=ORIENTED_EDGE('',*,*,#8504,.T.);
#12482=ORIENTED_EDGE('',*,*,#8509,.T.);
#12483=ORIENTED_EDGE('',*,*,#8510,.F.);
#12484=ORIENTED_EDGE('',*,*,#8511,.T.);
#12485=ORIENTED_EDGE('',*,*,#8507,.T.);
#12486=ORIENTED_EDGE('',*,*,#8512,.T.);
#12487=ORIENTED_EDGE('',*,*,#8513,.F.);
#12488=ORIENTED_EDGE('',*,*,#8514,.T.);
#12489=ORIENTED_EDGE('',*,*,#8510,.T.);
#12490=ORIENTED_EDGE('',*,*,#8515,.T.);
#12491=ORIENTED_EDGE('',*,*,#8516,.F.);
#12492=ORIENTED_EDGE('',*,*,#8517,.T.);
#12493=ORIENTED_EDGE('',*,*,#8513,.T.);
#12494=ORIENTED_EDGE('',*,*,#8518,.T.);
#12495=ORIENTED_EDGE('',*,*,#8519,.F.);
#12496=ORIENTED_EDGE('',*,*,#8520,.T.);
#12497=ORIENTED_EDGE('',*,*,#8516,.T.);
#12498=ORIENTED_EDGE('',*,*,#8521,.T.);
#12499=ORIENTED_EDGE('',*,*,#8522,.F.);
#12500=ORIENTED_EDGE('',*,*,#8523,.T.);
#12501=ORIENTED_EDGE('',*,*,#8519,.T.);
#12502=ORIENTED_EDGE('',*,*,#8524,.T.);
#12503=ORIENTED_EDGE('',*,*,#8525,.F.);
#12504=ORIENTED_EDGE('',*,*,#8526,.T.);
#12505=ORIENTED_EDGE('',*,*,#8522,.T.);
#12506=ORIENTED_EDGE('',*,*,#8527,.T.);
#12507=ORIENTED_EDGE('',*,*,#8528,.F.);
#12508=ORIENTED_EDGE('',*,*,#8529,.T.);
#12509=ORIENTED_EDGE('',*,*,#8525,.T.);
#12510=ORIENTED_EDGE('',*,*,#8530,.T.);
#12511=ORIENTED_EDGE('',*,*,#8531,.F.);
#12512=ORIENTED_EDGE('',*,*,#8532,.T.);
#12513=ORIENTED_EDGE('',*,*,#8528,.T.);
#12514=ORIENTED_EDGE('',*,*,#8533,.T.);
#12515=ORIENTED_EDGE('',*,*,#8534,.F.);
#12516=ORIENTED_EDGE('',*,*,#8535,.T.);
#12517=ORIENTED_EDGE('',*,*,#8536,.T.);
#12518=ORIENTED_EDGE('',*,*,#8537,.F.);
#12519=ORIENTED_EDGE('',*,*,#8538,.F.);
#12520=ORIENTED_EDGE('',*,*,#8539,.T.);
#12521=ORIENTED_EDGE('',*,*,#8534,.T.);
#12522=ORIENTED_EDGE('',*,*,#8540,.F.);
#12523=ORIENTED_EDGE('',*,*,#8541,.F.);
#12524=ORIENTED_EDGE('',*,*,#8542,.T.);
#12525=ORIENTED_EDGE('',*,*,#8538,.T.);
#12526=ORIENTED_EDGE('',*,*,#8543,.F.);
#12527=ORIENTED_EDGE('',*,*,#8544,.F.);
#12528=ORIENTED_EDGE('',*,*,#8545,.T.);
#12529=ORIENTED_EDGE('',*,*,#8541,.T.);
#12530=ORIENTED_EDGE('',*,*,#8546,.F.);
#12531=ORIENTED_EDGE('',*,*,#8547,.F.);
#12532=ORIENTED_EDGE('',*,*,#8548,.T.);
#12533=ORIENTED_EDGE('',*,*,#8544,.T.);
#12534=ORIENTED_EDGE('',*,*,#8549,.F.);
#12535=ORIENTED_EDGE('',*,*,#8550,.F.);
#12536=ORIENTED_EDGE('',*,*,#8551,.T.);
#12537=ORIENTED_EDGE('',*,*,#8547,.T.);
#12538=ORIENTED_EDGE('',*,*,#8552,.F.);
#12539=ORIENTED_EDGE('',*,*,#8553,.F.);
#12540=ORIENTED_EDGE('',*,*,#8554,.T.);
#12541=ORIENTED_EDGE('',*,*,#8550,.T.);
#12542=ORIENTED_EDGE('',*,*,#8555,.F.);
#12543=ORIENTED_EDGE('',*,*,#8556,.F.);
#12544=ORIENTED_EDGE('',*,*,#8557,.T.);
#12545=ORIENTED_EDGE('',*,*,#8553,.T.);
#12546=ORIENTED_EDGE('',*,*,#8558,.F.);
#12547=ORIENTED_EDGE('',*,*,#8559,.F.);
#12548=ORIENTED_EDGE('',*,*,#8560,.T.);
#12549=ORIENTED_EDGE('',*,*,#8556,.T.);
#12550=ORIENTED_EDGE('',*,*,#8561,.F.);
#12551=ORIENTED_EDGE('',*,*,#8562,.F.);
#12552=ORIENTED_EDGE('',*,*,#8563,.T.);
#12553=ORIENTED_EDGE('',*,*,#8559,.T.);
#12554=ORIENTED_EDGE('',*,*,#8564,.F.);
#12555=ORIENTED_EDGE('',*,*,#8565,.F.);
#12556=ORIENTED_EDGE('',*,*,#8566,.T.);
#12557=ORIENTED_EDGE('',*,*,#8562,.T.);
#12558=ORIENTED_EDGE('',*,*,#8567,.F.);
#12559=ORIENTED_EDGE('',*,*,#8568,.F.);
#12560=ORIENTED_EDGE('',*,*,#8569,.T.);
#12561=ORIENTED_EDGE('',*,*,#8565,.T.);
#12562=ORIENTED_EDGE('',*,*,#8570,.F.);
#12563=ORIENTED_EDGE('',*,*,#8571,.F.);
#12564=ORIENTED_EDGE('',*,*,#8572,.T.);
#12565=ORIENTED_EDGE('',*,*,#8568,.T.);
#12566=ORIENTED_EDGE('',*,*,#8573,.F.);
#12567=ORIENTED_EDGE('',*,*,#8574,.F.);
#12568=ORIENTED_EDGE('',*,*,#8575,.T.);
#12569=ORIENTED_EDGE('',*,*,#8571,.T.);
#12570=ORIENTED_EDGE('',*,*,#8576,.F.);
#12571=ORIENTED_EDGE('',*,*,#8577,.F.);
#12572=ORIENTED_EDGE('',*,*,#8578,.T.);
#12573=ORIENTED_EDGE('',*,*,#8574,.T.);
#12574=ORIENTED_EDGE('',*,*,#8579,.F.);
#12575=ORIENTED_EDGE('',*,*,#8580,.F.);
#12576=ORIENTED_EDGE('',*,*,#8581,.T.);
#12577=ORIENTED_EDGE('',*,*,#8577,.T.);
#12578=ORIENTED_EDGE('',*,*,#8582,.F.);
#12579=ORIENTED_EDGE('',*,*,#8583,.F.);
#12580=ORIENTED_EDGE('',*,*,#8584,.T.);
#12581=ORIENTED_EDGE('',*,*,#8580,.T.);
#12582=ORIENTED_EDGE('',*,*,#8585,.F.);
#12583=ORIENTED_EDGE('',*,*,#8586,.F.);
#12584=ORIENTED_EDGE('',*,*,#8587,.T.);
#12585=ORIENTED_EDGE('',*,*,#8583,.T.);
#12586=ORIENTED_EDGE('',*,*,#8588,.F.);
#12587=ORIENTED_EDGE('',*,*,#8589,.F.);
#12588=ORIENTED_EDGE('',*,*,#8590,.T.);
#12589=ORIENTED_EDGE('',*,*,#8586,.T.);
#12590=ORIENTED_EDGE('',*,*,#8591,.F.);
#12591=ORIENTED_EDGE('',*,*,#8592,.F.);
#12592=ORIENTED_EDGE('',*,*,#8593,.T.);
#12593=ORIENTED_EDGE('',*,*,#8589,.T.);
#12594=ORIENTED_EDGE('',*,*,#8594,.F.);
#12595=ORIENTED_EDGE('',*,*,#8595,.F.);
#12596=ORIENTED_EDGE('',*,*,#8596,.T.);
#12597=ORIENTED_EDGE('',*,*,#8592,.T.);
#12598=ORIENTED_EDGE('',*,*,#8597,.F.);
#12599=ORIENTED_EDGE('',*,*,#8598,.F.);
#12600=ORIENTED_EDGE('',*,*,#8599,.T.);
#12601=ORIENTED_EDGE('',*,*,#8595,.T.);
#12602=ORIENTED_EDGE('',*,*,#8600,.F.);
#12603=ORIENTED_EDGE('',*,*,#8601,.F.);
#12604=ORIENTED_EDGE('',*,*,#8602,.T.);
#12605=ORIENTED_EDGE('',*,*,#8598,.T.);
#12606=ORIENTED_EDGE('',*,*,#8603,.F.);
#12607=ORIENTED_EDGE('',*,*,#8604,.F.);
#12608=ORIENTED_EDGE('',*,*,#8605,.T.);
#12609=ORIENTED_EDGE('',*,*,#8601,.T.);
#12610=ORIENTED_EDGE('',*,*,#8606,.F.);
#12611=ORIENTED_EDGE('',*,*,#8607,.F.);
#12612=ORIENTED_EDGE('',*,*,#8608,.T.);
#12613=ORIENTED_EDGE('',*,*,#8604,.T.);
#12614=ORIENTED_EDGE('',*,*,#8609,.F.);
#12615=ORIENTED_EDGE('',*,*,#8610,.F.);
#12616=ORIENTED_EDGE('',*,*,#8611,.T.);
#12617=ORIENTED_EDGE('',*,*,#8607,.T.);
#12618=ORIENTED_EDGE('',*,*,#8612,.F.);
#12619=ORIENTED_EDGE('',*,*,#8613,.F.);
#12620=ORIENTED_EDGE('',*,*,#8614,.T.);
#12621=ORIENTED_EDGE('',*,*,#8610,.T.);
#12622=ORIENTED_EDGE('',*,*,#8615,.F.);
#12623=ORIENTED_EDGE('',*,*,#8616,.F.);
#12624=ORIENTED_EDGE('',*,*,#8617,.T.);
#12625=ORIENTED_EDGE('',*,*,#8613,.T.);
#12626=ORIENTED_EDGE('',*,*,#8618,.F.);
#12627=ORIENTED_EDGE('',*,*,#8619,.F.);
#12628=ORIENTED_EDGE('',*,*,#8620,.T.);
#12629=ORIENTED_EDGE('',*,*,#8616,.T.);
#12630=ORIENTED_EDGE('',*,*,#8621,.F.);
#12631=ORIENTED_EDGE('',*,*,#8622,.F.);
#12632=ORIENTED_EDGE('',*,*,#8623,.T.);
#12633=ORIENTED_EDGE('',*,*,#8619,.T.);
#12634=ORIENTED_EDGE('',*,*,#8624,.F.);
#12635=ORIENTED_EDGE('',*,*,#8625,.F.);
#12636=ORIENTED_EDGE('',*,*,#8626,.T.);
#12637=ORIENTED_EDGE('',*,*,#8622,.T.);
#12638=ORIENTED_EDGE('',*,*,#8627,.F.);
#12639=ORIENTED_EDGE('',*,*,#8628,.F.);
#12640=ORIENTED_EDGE('',*,*,#8629,.T.);
#12641=ORIENTED_EDGE('',*,*,#8625,.T.);
#12642=ORIENTED_EDGE('',*,*,#8630,.F.);
#12643=ORIENTED_EDGE('',*,*,#8631,.F.);
#12644=ORIENTED_EDGE('',*,*,#8632,.T.);
#12645=ORIENTED_EDGE('',*,*,#8628,.T.);
#12646=ORIENTED_EDGE('',*,*,#8633,.F.);
#12647=ORIENTED_EDGE('',*,*,#8634,.F.);
#12648=ORIENTED_EDGE('',*,*,#8635,.T.);
#12649=ORIENTED_EDGE('',*,*,#8631,.T.);
#12650=ORIENTED_EDGE('',*,*,#8636,.F.);
#12651=ORIENTED_EDGE('',*,*,#8637,.F.);
#12652=ORIENTED_EDGE('',*,*,#8638,.T.);
#12653=ORIENTED_EDGE('',*,*,#8634,.T.);
#12654=ORIENTED_EDGE('',*,*,#8639,.F.);
#12655=ORIENTED_EDGE('',*,*,#8640,.F.);
#12656=ORIENTED_EDGE('',*,*,#8641,.T.);
#12657=ORIENTED_EDGE('',*,*,#8637,.T.);
#12658=ORIENTED_EDGE('',*,*,#8642,.F.);
#12659=ORIENTED_EDGE('',*,*,#8643,.F.);
#12660=ORIENTED_EDGE('',*,*,#8644,.T.);
#12661=ORIENTED_EDGE('',*,*,#8640,.T.);
#12662=ORIENTED_EDGE('',*,*,#8645,.F.);
#12663=ORIENTED_EDGE('',*,*,#8646,.F.);
#12664=ORIENTED_EDGE('',*,*,#8647,.T.);
#12665=ORIENTED_EDGE('',*,*,#8643,.T.);
#12666=ORIENTED_EDGE('',*,*,#8648,.F.);
#12667=ORIENTED_EDGE('',*,*,#8649,.F.);
#12668=ORIENTED_EDGE('',*,*,#8650,.T.);
#12669=ORIENTED_EDGE('',*,*,#8646,.T.);
#12670=ORIENTED_EDGE('',*,*,#8651,.F.);
#12671=ORIENTED_EDGE('',*,*,#8652,.F.);
#12672=ORIENTED_EDGE('',*,*,#8536,.F.);
#12673=ORIENTED_EDGE('',*,*,#8653,.F.);
#12674=ORIENTED_EDGE('',*,*,#8654,.F.);
#12675=ORIENTED_EDGE('',*,*,#8655,.F.);
#12676=ORIENTED_EDGE('',*,*,#8656,.T.);
#12677=ORIENTED_EDGE('',*,*,#8657,.F.);
#12678=ORIENTED_EDGE('',*,*,#8656,.F.);
#12679=ORIENTED_EDGE('',*,*,#8653,.T.);
#12680=ORIENTED_EDGE('',*,*,#8535,.F.);
#12681=ORIENTED_EDGE('',*,*,#8539,.F.);
#12682=ORIENTED_EDGE('',*,*,#8542,.F.);
#12683=ORIENTED_EDGE('',*,*,#8545,.F.);
#12684=ORIENTED_EDGE('',*,*,#8548,.F.);
#12685=ORIENTED_EDGE('',*,*,#8551,.F.);
#12686=ORIENTED_EDGE('',*,*,#8554,.F.);
#12687=ORIENTED_EDGE('',*,*,#8557,.F.);
#12688=ORIENTED_EDGE('',*,*,#8560,.F.);
#12689=ORIENTED_EDGE('',*,*,#8563,.F.);
#12690=ORIENTED_EDGE('',*,*,#8566,.F.);
#12691=ORIENTED_EDGE('',*,*,#8569,.F.);
#12692=ORIENTED_EDGE('',*,*,#8572,.F.);
#12693=ORIENTED_EDGE('',*,*,#8575,.F.);
#12694=ORIENTED_EDGE('',*,*,#8578,.F.);
#12695=ORIENTED_EDGE('',*,*,#8581,.F.);
#12696=ORIENTED_EDGE('',*,*,#8584,.F.);
#12697=ORIENTED_EDGE('',*,*,#8587,.F.);
#12698=ORIENTED_EDGE('',*,*,#8590,.F.);
#12699=ORIENTED_EDGE('',*,*,#8593,.F.);
#12700=ORIENTED_EDGE('',*,*,#8596,.F.);
#12701=ORIENTED_EDGE('',*,*,#8599,.F.);
#12702=ORIENTED_EDGE('',*,*,#8602,.F.);
#12703=ORIENTED_EDGE('',*,*,#8605,.F.);
#12704=ORIENTED_EDGE('',*,*,#8608,.F.);
#12705=ORIENTED_EDGE('',*,*,#8611,.F.);
#12706=ORIENTED_EDGE('',*,*,#8614,.F.);
#12707=ORIENTED_EDGE('',*,*,#8617,.F.);
#12708=ORIENTED_EDGE('',*,*,#8620,.F.);
#12709=ORIENTED_EDGE('',*,*,#8623,.F.);
#12710=ORIENTED_EDGE('',*,*,#8626,.F.);
#12711=ORIENTED_EDGE('',*,*,#8629,.F.);
#12712=ORIENTED_EDGE('',*,*,#8632,.F.);
#12713=ORIENTED_EDGE('',*,*,#8635,.F.);
#12714=ORIENTED_EDGE('',*,*,#8638,.F.);
#12715=ORIENTED_EDGE('',*,*,#8641,.F.);
#12716=ORIENTED_EDGE('',*,*,#8644,.F.);
#12717=ORIENTED_EDGE('',*,*,#8647,.F.);
#12718=ORIENTED_EDGE('',*,*,#8650,.F.);
#12719=ORIENTED_EDGE('',*,*,#8658,.F.);
#12720=ORIENTED_EDGE('',*,*,#8659,.F.);
#12721=ORIENTED_EDGE('',*,*,#8417,.F.);
#12722=ORIENTED_EDGE('',*,*,#8421,.F.);
#12723=ORIENTED_EDGE('',*,*,#8424,.F.);
#12724=ORIENTED_EDGE('',*,*,#8427,.F.);
#12725=ORIENTED_EDGE('',*,*,#8430,.F.);
#12726=ORIENTED_EDGE('',*,*,#8433,.F.);
#12727=ORIENTED_EDGE('',*,*,#8436,.F.);
#12728=ORIENTED_EDGE('',*,*,#8439,.F.);
#12729=ORIENTED_EDGE('',*,*,#8442,.F.);
#12730=ORIENTED_EDGE('',*,*,#8445,.F.);
#12731=ORIENTED_EDGE('',*,*,#8448,.F.);
#12732=ORIENTED_EDGE('',*,*,#8451,.F.);
#12733=ORIENTED_EDGE('',*,*,#8454,.F.);
#12734=ORIENTED_EDGE('',*,*,#8457,.F.);
#12735=ORIENTED_EDGE('',*,*,#8460,.F.);
#12736=ORIENTED_EDGE('',*,*,#8463,.F.);
#12737=ORIENTED_EDGE('',*,*,#8466,.F.);
#12738=ORIENTED_EDGE('',*,*,#8469,.F.);
#12739=ORIENTED_EDGE('',*,*,#8472,.F.);
#12740=ORIENTED_EDGE('',*,*,#8475,.F.);
#12741=ORIENTED_EDGE('',*,*,#8478,.F.);
#12742=ORIENTED_EDGE('',*,*,#8481,.F.);
#12743=ORIENTED_EDGE('',*,*,#8484,.F.);
#12744=ORIENTED_EDGE('',*,*,#8487,.F.);
#12745=ORIENTED_EDGE('',*,*,#8490,.F.);
#12746=ORIENTED_EDGE('',*,*,#8493,.F.);
#12747=ORIENTED_EDGE('',*,*,#8496,.F.);
#12748=ORIENTED_EDGE('',*,*,#8499,.F.);
#12749=ORIENTED_EDGE('',*,*,#8502,.F.);
#12750=ORIENTED_EDGE('',*,*,#8505,.F.);
#12751=ORIENTED_EDGE('',*,*,#8508,.F.);
#12752=ORIENTED_EDGE('',*,*,#8511,.F.);
#12753=ORIENTED_EDGE('',*,*,#8514,.F.);
#12754=ORIENTED_EDGE('',*,*,#8517,.F.);
#12755=ORIENTED_EDGE('',*,*,#8520,.F.);
#12756=ORIENTED_EDGE('',*,*,#8523,.F.);
#12757=ORIENTED_EDGE('',*,*,#8526,.F.);
#12758=ORIENTED_EDGE('',*,*,#8529,.F.);
#12759=ORIENTED_EDGE('',*,*,#8532,.F.);
#12760=ORIENTED_EDGE('',*,*,#8660,.F.);
#12761=ORIENTED_EDGE('',*,*,#8649,.T.);
#12762=ORIENTED_EDGE('',*,*,#8661,.F.);
#12763=ORIENTED_EDGE('',*,*,#8662,.F.);
#12764=ORIENTED_EDGE('',*,*,#8658,.T.);
#12765=ORIENTED_EDGE('',*,*,#8652,.T.);
#12766=ORIENTED_EDGE('',*,*,#8655,.T.);
#12767=ORIENTED_EDGE('',*,*,#8663,.F.);
#12768=ORIENTED_EDGE('',*,*,#8533,.F.);
#12769=ORIENTED_EDGE('',*,*,#8530,.F.);
#12770=ORIENTED_EDGE('',*,*,#8527,.F.);
#12771=ORIENTED_EDGE('',*,*,#8524,.F.);
#12772=ORIENTED_EDGE('',*,*,#8521,.F.);
#12773=ORIENTED_EDGE('',*,*,#8518,.F.);
#12774=ORIENTED_EDGE('',*,*,#8515,.F.);
#12775=ORIENTED_EDGE('',*,*,#8512,.F.);
#12776=ORIENTED_EDGE('',*,*,#8509,.F.);
#12777=ORIENTED_EDGE('',*,*,#8506,.F.);
#12778=ORIENTED_EDGE('',*,*,#8503,.F.);
#12779=ORIENTED_EDGE('',*,*,#8500,.F.);
#12780=ORIENTED_EDGE('',*,*,#8497,.F.);
#12781=ORIENTED_EDGE('',*,*,#8494,.F.);
#12782=ORIENTED_EDGE('',*,*,#8491,.F.);
#12783=ORIENTED_EDGE('',*,*,#8488,.F.);
#12784=ORIENTED_EDGE('',*,*,#8485,.F.);
#12785=ORIENTED_EDGE('',*,*,#8482,.F.);
#12786=ORIENTED_EDGE('',*,*,#8479,.F.);
#12787=ORIENTED_EDGE('',*,*,#8476,.F.);
#12788=ORIENTED_EDGE('',*,*,#8473,.F.);
#12789=ORIENTED_EDGE('',*,*,#8470,.F.);
#12790=ORIENTED_EDGE('',*,*,#8467,.F.);
#12791=ORIENTED_EDGE('',*,*,#8464,.F.);
#12792=ORIENTED_EDGE('',*,*,#8461,.F.);
#12793=ORIENTED_EDGE('',*,*,#8458,.F.);
#12794=ORIENTED_EDGE('',*,*,#8455,.F.);
#12795=ORIENTED_EDGE('',*,*,#8452,.F.);
#12796=ORIENTED_EDGE('',*,*,#8449,.F.);
#12797=ORIENTED_EDGE('',*,*,#8446,.F.);
#12798=ORIENTED_EDGE('',*,*,#8443,.F.);
#12799=ORIENTED_EDGE('',*,*,#8440,.F.);
#12800=ORIENTED_EDGE('',*,*,#8437,.F.);
#12801=ORIENTED_EDGE('',*,*,#8434,.F.);
#12802=ORIENTED_EDGE('',*,*,#8431,.F.);
#12803=ORIENTED_EDGE('',*,*,#8428,.F.);
#12804=ORIENTED_EDGE('',*,*,#8425,.F.);
#12805=ORIENTED_EDGE('',*,*,#8422,.F.);
#12806=ORIENTED_EDGE('',*,*,#8419,.F.);
#12807=ORIENTED_EDGE('',*,*,#8664,.F.);
#12808=ORIENTED_EDGE('',*,*,#8661,.T.);
#12809=ORIENTED_EDGE('',*,*,#8651,.T.);
#12810=ORIENTED_EDGE('',*,*,#8648,.T.);
#12811=ORIENTED_EDGE('',*,*,#8645,.T.);
#12812=ORIENTED_EDGE('',*,*,#8642,.T.);
#12813=ORIENTED_EDGE('',*,*,#8639,.T.);
#12814=ORIENTED_EDGE('',*,*,#8636,.T.);
#12815=ORIENTED_EDGE('',*,*,#8633,.T.);
#12816=ORIENTED_EDGE('',*,*,#8630,.T.);
#12817=ORIENTED_EDGE('',*,*,#8627,.T.);
#12818=ORIENTED_EDGE('',*,*,#8624,.T.);
#12819=ORIENTED_EDGE('',*,*,#8621,.T.);
#12820=ORIENTED_EDGE('',*,*,#8618,.T.);
#12821=ORIENTED_EDGE('',*,*,#8615,.T.);
#12822=ORIENTED_EDGE('',*,*,#8612,.T.);
#12823=ORIENTED_EDGE('',*,*,#8609,.T.);
#12824=ORIENTED_EDGE('',*,*,#8606,.T.);
#12825=ORIENTED_EDGE('',*,*,#8603,.T.);
#12826=ORIENTED_EDGE('',*,*,#8600,.T.);
#12827=ORIENTED_EDGE('',*,*,#8597,.T.);
#12828=ORIENTED_EDGE('',*,*,#8594,.T.);
#12829=ORIENTED_EDGE('',*,*,#8591,.T.);
#12830=ORIENTED_EDGE('',*,*,#8588,.T.);
#12831=ORIENTED_EDGE('',*,*,#8585,.T.);
#12832=ORIENTED_EDGE('',*,*,#8582,.T.);
#12833=ORIENTED_EDGE('',*,*,#8579,.T.);
#12834=ORIENTED_EDGE('',*,*,#8576,.T.);
#12835=ORIENTED_EDGE('',*,*,#8573,.T.);
#12836=ORIENTED_EDGE('',*,*,#8570,.T.);
#12837=ORIENTED_EDGE('',*,*,#8567,.T.);
#12838=ORIENTED_EDGE('',*,*,#8564,.T.);
#12839=ORIENTED_EDGE('',*,*,#8561,.T.);
#12840=ORIENTED_EDGE('',*,*,#8558,.T.);
#12841=ORIENTED_EDGE('',*,*,#8555,.T.);
#12842=ORIENTED_EDGE('',*,*,#8552,.T.);
#12843=ORIENTED_EDGE('',*,*,#8549,.T.);
#12844=ORIENTED_EDGE('',*,*,#8546,.T.);
#12845=ORIENTED_EDGE('',*,*,#8543,.T.);
#12846=ORIENTED_EDGE('',*,*,#8540,.T.);
#12847=ORIENTED_EDGE('',*,*,#8537,.T.);
#12848=ORIENTED_EDGE('',*,*,#8531,.T.);
#12849=ORIENTED_EDGE('',*,*,#8663,.T.);
#12850=ORIENTED_EDGE('',*,*,#8654,.T.);
#12851=ORIENTED_EDGE('',*,*,#8660,.T.);
#12852=ORIENTED_EDGE('',*,*,#8665,.F.);
#12853=ORIENTED_EDGE('',*,*,#8666,.T.);
#12854=ORIENTED_EDGE('',*,*,#8667,.T.);
#12855=ORIENTED_EDGE('',*,*,#8668,.F.);
#12856=ORIENTED_EDGE('',*,*,#8669,.F.);
#12857=ORIENTED_EDGE('',*,*,#8670,.T.);
#12858=ORIENTED_EDGE('',*,*,#8671,.T.);
#12859=ORIENTED_EDGE('',*,*,#8666,.F.);
#12860=ORIENTED_EDGE('',*,*,#8672,.F.);
#12861=ORIENTED_EDGE('',*,*,#8673,.T.);
#12862=ORIENTED_EDGE('',*,*,#8674,.T.);
#12863=ORIENTED_EDGE('',*,*,#8670,.F.);
#12864=ORIENTED_EDGE('',*,*,#8675,.F.);
#12865=ORIENTED_EDGE('',*,*,#8676,.T.);
#12866=ORIENTED_EDGE('',*,*,#8677,.T.);
#12867=ORIENTED_EDGE('',*,*,#8673,.F.);
#12868=ORIENTED_EDGE('',*,*,#8678,.F.);
#12869=ORIENTED_EDGE('',*,*,#8679,.T.);
#12870=ORIENTED_EDGE('',*,*,#8680,.T.);
#12871=ORIENTED_EDGE('',*,*,#8676,.F.);
#12872=ORIENTED_EDGE('',*,*,#8681,.F.);
#12873=ORIENTED_EDGE('',*,*,#8668,.T.);
#12874=ORIENTED_EDGE('',*,*,#8682,.T.);
#12875=ORIENTED_EDGE('',*,*,#8679,.F.);
#12876=ORIENTED_EDGE('',*,*,#8682,.F.);
#12877=ORIENTED_EDGE('',*,*,#8667,.F.);
#12878=ORIENTED_EDGE('',*,*,#8671,.F.);
#12879=ORIENTED_EDGE('',*,*,#8674,.F.);
#12880=ORIENTED_EDGE('',*,*,#8677,.F.);
#12881=ORIENTED_EDGE('',*,*,#8680,.F.);
#12882=ORIENTED_EDGE('',*,*,#8683,.T.);
#12883=ORIENTED_EDGE('',*,*,#8659,.T.);
#12884=ORIENTED_EDGE('',*,*,#8662,.T.);
#12885=ORIENTED_EDGE('',*,*,#8664,.T.);
#12886=ORIENTED_EDGE('',*,*,#8418,.F.);
#12887=ORIENTED_EDGE('',*,*,#8683,.F.);
#12888=ORIENTED_EDGE('',*,*,#8684,.T.);
#12889=ORIENTED_EDGE('',*,*,#8685,.T.);
#12890=ORIENTED_EDGE('',*,*,#8684,.F.);
#12891=ORIENTED_EDGE('',*,*,#8685,.F.);
#12892=ORIENTED_EDGE('',*,*,#8665,.T.);
#12893=ORIENTED_EDGE('',*,*,#8681,.T.);
#12894=ORIENTED_EDGE('',*,*,#8678,.T.);
#12895=ORIENTED_EDGE('',*,*,#8675,.T.);
#12896=ORIENTED_EDGE('',*,*,#8672,.T.);
#12897=ORIENTED_EDGE('',*,*,#8669,.T.);
#12898=ORIENTED_EDGE('',*,*,#8657,.T.);
#13800=CYLINDRICAL_SURFACE('',#15616,2.942);
#13801=CYLINDRICAL_SURFACE('',#15618,2.942);
#13802=CYLINDRICAL_SURFACE('',#15619,2.942);
#13803=CYLINDRICAL_SURFACE('',#15620,2.942);
#13804=CYLINDRICAL_SURFACE('',#15621,2.942);
#13805=CYLINDRICAL_SURFACE('',#15622,2.942);
#13806=CYLINDRICAL_SURFACE('',#15623,2.942);
#13807=CYLINDRICAL_SURFACE('',#15624,2.942);
#13808=CYLINDRICAL_SURFACE('',#15625,2.942);
#13809=CYLINDRICAL_SURFACE('',#15626,2.942);
#13810=CYLINDRICAL_SURFACE('',#15627,2.942);
#13811=CYLINDRICAL_SURFACE('',#15628,2.942);
#13812=CYLINDRICAL_SURFACE('',#15629,2.942);
#13813=CYLINDRICAL_SURFACE('',#15630,2.942);
#13814=CYLINDRICAL_SURFACE('',#15631,2.942);
#13815=CYLINDRICAL_SURFACE('',#15632,2.942);
#13816=CYLINDRICAL_SURFACE('',#15633,2.942);
#13817=CYLINDRICAL_SURFACE('',#15634,2.942);
#13818=CYLINDRICAL_SURFACE('',#15635,2.942);
#13819=CYLINDRICAL_SURFACE('',#15636,2.942);
#13820=CYLINDRICAL_SURFACE('',#15637,2.942);
#13821=CYLINDRICAL_SURFACE('',#15638,2.942);
#13822=CYLINDRICAL_SURFACE('',#15639,2.942);
#13823=CYLINDRICAL_SURFACE('',#15640,2.942);
#13824=CYLINDRICAL_SURFACE('',#15641,2.942);
#13825=CYLINDRICAL_SURFACE('',#15642,2.942);
#13826=CYLINDRICAL_SURFACE('',#15643,2.942);
#13827=CYLINDRICAL_SURFACE('',#15644,2.942);
#13828=CYLINDRICAL_SURFACE('',#15645,2.942);
#13829=CYLINDRICAL_SURFACE('',#15646,2.942);
#13830=CYLINDRICAL_SURFACE('',#15647,2.942);
#13831=CYLINDRICAL_SURFACE('',#15648,2.942);
#13832=CYLINDRICAL_SURFACE('',#15649,2.942);
#13833=CYLINDRICAL_SURFACE('',#15650,2.942);
#13834=CYLINDRICAL_SURFACE('',#15651,2.942);
#13835=CYLINDRICAL_SURFACE('',#15652,2.942);
#13836=CYLINDRICAL_SURFACE('',#15653,2.942);
#13837=CYLINDRICAL_SURFACE('',#15654,2.942);
#13838=CYLINDRICAL_SURFACE('',#15655,2.942);
#13839=CYLINDRICAL_SURFACE('',#15656,2.37175);
#13840=CYLINDRICAL_SURFACE('',#15658,2.37175);
#13841=CYLINDRICAL_SURFACE('',#15659,2.37175);
#13842=CYLINDRICAL_SURFACE('',#15660,2.37175);
#13843=CYLINDRICAL_SURFACE('',#15661,2.37175);
#13844=CYLINDRICAL_SURFACE('',#15662,2.37175);
#13845=CYLINDRICAL_SURFACE('',#15663,2.37175);
#13846=CYLINDRICAL_SURFACE('',#15664,2.37175);
#13847=CYLINDRICAL_SURFACE('',#15665,2.37175);
#13848=CYLINDRICAL_SURFACE('',#15666,2.37175);
#13849=CYLINDRICAL_SURFACE('',#15667,2.37175);
#13850=CYLINDRICAL_SURFACE('',#15668,2.37175);
#13851=CYLINDRICAL_SURFACE('',#15669,2.37175);
#13852=CYLINDRICAL_SURFACE('',#15670,2.37175);
#13853=CYLINDRICAL_SURFACE('',#15671,2.37175);
#13854=CYLINDRICAL_SURFACE('',#15672,2.37175);
#13855=CYLINDRICAL_SURFACE('',#15673,2.37175);
#13856=CYLINDRICAL_SURFACE('',#15674,2.37175);
#13857=CYLINDRICAL_SURFACE('',#15675,2.37175);
#13858=CYLINDRICAL_SURFACE('',#15676,2.37175);
#13859=CYLINDRICAL_SURFACE('',#15677,2.37175);
#13860=CYLINDRICAL_SURFACE('',#15678,2.37175);
#13861=CYLINDRICAL_SURFACE('',#15679,2.37175);
#13862=CYLINDRICAL_SURFACE('',#15680,2.37175);
#13863=CYLINDRICAL_SURFACE('',#15681,2.37175);
#13864=CYLINDRICAL_SURFACE('',#15682,2.37175);
#13865=CYLINDRICAL_SURFACE('',#15683,2.37175);
#13866=CYLINDRICAL_SURFACE('',#15684,2.37175);
#13867=CYLINDRICAL_SURFACE('',#15685,2.37175);
#13868=CYLINDRICAL_SURFACE('',#15686,2.37175);
#13869=CYLINDRICAL_SURFACE('',#15687,2.37175);
#13870=CYLINDRICAL_SURFACE('',#15688,2.37175);
#13871=CYLINDRICAL_SURFACE('',#15689,2.37175);
#13872=CYLINDRICAL_SURFACE('',#15690,2.37175);
#13873=CYLINDRICAL_SURFACE('',#15691,2.37175);
#13874=CYLINDRICAL_SURFACE('',#15692,2.37175);
#13875=CYLINDRICAL_SURFACE('',#15693,2.37175);
#13876=CYLINDRICAL_SURFACE('',#15694,2.37175);
#13877=CYLINDRICAL_SURFACE('',#15695,2.37175);
#13878=CYLINDRICAL_SURFACE('',#15699,2.37175);
#13879=CYLINDRICAL_SURFACE('',#15701,2.942);
#13880=CYLINDRICAL_SURFACE('',#15711,5.);
#14552=ADVANCED_FACE('',(#1124),#13800,.T.);
#14553=ADVANCED_FACE('',(#1125),#13801,.T.);
#14554=ADVANCED_FACE('',(#1126),#13802,.T.);
#14555=ADVANCED_FACE('',(#1127),#13803,.T.);
#14556=ADVANCED_FACE('',(#1128),#13804,.T.);
#14557=ADVANCED_FACE('',(#1129),#13805,.T.);
#14558=ADVANCED_FACE('',(#1130),#13806,.T.);
#14559=ADVANCED_FACE('',(#1131),#13807,.T.);
#14560=ADVANCED_FACE('',(#1132),#13808,.T.);
#14561=ADVANCED_FACE('',(#1133),#13809,.T.);
#14562=ADVANCED_FACE('',(#1134),#13810,.T.);
#14563=ADVANCED_FACE('',(#1135),#13811,.T.);
#14564=ADVANCED_FACE('',(#1136),#13812,.T.);
#14565=ADVANCED_FACE('',(#1137),#13813,.T.);
#14566=ADVANCED_FACE('',(#1138),#13814,.T.);
#14567=ADVANCED_FACE('',(#1139),#13815,.T.);
#14568=ADVANCED_FACE('',(#1140),#13816,.T.);
#14569=ADVANCED_FACE('',(#1141),#13817,.T.);
#14570=ADVANCED_FACE('',(#1142),#13818,.T.);
#14571=ADVANCED_FACE('',(#1143),#13819,.T.);
#14572=ADVANCED_FACE('',(#1144),#13820,.T.);
#14573=ADVANCED_FACE('',(#1145),#13821,.T.);
#14574=ADVANCED_FACE('',(#1146),#13822,.T.);
#14575=ADVANCED_FACE('',(#1147),#13823,.T.);
#14576=ADVANCED_FACE('',(#1148),#13824,.T.);
#14577=ADVANCED_FACE('',(#1149),#13825,.T.);
#14578=ADVANCED_FACE('',(#1150),#13826,.T.);
#14579=ADVANCED_FACE('',(#1151),#13827,.T.);
#14580=ADVANCED_FACE('',(#1152),#13828,.T.);
#14581=ADVANCED_FACE('',(#1153),#13829,.T.);
#14582=ADVANCED_FACE('',(#1154),#13830,.T.);
#14583=ADVANCED_FACE('',(#1155),#13831,.T.);
#14584=ADVANCED_FACE('',(#1156),#13832,.T.);
#14585=ADVANCED_FACE('',(#1157),#13833,.T.);
#14586=ADVANCED_FACE('',(#1158),#13834,.T.);
#14587=ADVANCED_FACE('',(#1159),#13835,.T.);
#14588=ADVANCED_FACE('',(#1160),#13836,.T.);
#14589=ADVANCED_FACE('',(#1161),#13837,.T.);
#14590=ADVANCED_FACE('',(#1162),#13838,.T.);
#14591=ADVANCED_FACE('',(#1163),#13839,.T.);
#14592=ADVANCED_FACE('',(#1164),#13840,.T.);
#14593=ADVANCED_FACE('',(#1165),#13841,.T.);
#14594=ADVANCED_FACE('',(#1166),#13842,.T.);
#14595=ADVANCED_FACE('',(#1167),#13843,.T.);
#14596=ADVANCED_FACE('',(#1168),#13844,.T.);
#14597=ADVANCED_FACE('',(#1169),#13845,.T.);
#14598=ADVANCED_FACE('',(#1170),#13846,.T.);
#14599=ADVANCED_FACE('',(#1171),#13847,.T.);
#14600=ADVANCED_FACE('',(#1172),#13848,.T.);
#14601=ADVANCED_FACE('',(#1173),#13849,.T.);
#14602=ADVANCED_FACE('',(#1174),#13850,.T.);
#14603=ADVANCED_FACE('',(#1175),#13851,.T.);
#14604=ADVANCED_FACE('',(#1176),#13852,.T.);
#14605=ADVANCED_FACE('',(#1177),#13853,.T.);
#14606=ADVANCED_FACE('',(#1178),#13854,.T.);
#14607=ADVANCED_FACE('',(#1179),#13855,.T.);
#14608=ADVANCED_FACE('',(#1180),#13856,.T.);
#14609=ADVANCED_FACE('',(#1181),#13857,.T.);
#14610=ADVANCED_FACE('',(#1182),#13858,.T.);
#14611=ADVANCED_FACE('',(#1183),#13859,.T.);
#14612=ADVANCED_FACE('',(#1184),#13860,.T.);
#14613=ADVANCED_FACE('',(#1185),#13861,.T.);
#14614=ADVANCED_FACE('',(#1186),#13862,.T.);
#14615=ADVANCED_FACE('',(#1187),#13863,.T.);
#14616=ADVANCED_FACE('',(#1188),#13864,.T.);
#14617=ADVANCED_FACE('',(#1189),#13865,.T.);
#14618=ADVANCED_FACE('',(#1190),#13866,.T.);
#14619=ADVANCED_FACE('',(#1191),#13867,.T.);
#14620=ADVANCED_FACE('',(#1192),#13868,.T.);
#14621=ADVANCED_FACE('',(#1193),#13869,.T.);
#14622=ADVANCED_FACE('',(#1194),#13870,.T.);
#14623=ADVANCED_FACE('',(#1195),#13871,.T.);
#14624=ADVANCED_FACE('',(#1196),#13872,.T.);
#14625=ADVANCED_FACE('',(#1197),#13873,.T.);
#14626=ADVANCED_FACE('',(#1198),#13874,.T.);
#14627=ADVANCED_FACE('',(#1199),#13875,.T.);
#14628=ADVANCED_FACE('',(#1200),#13876,.T.);
#14629=ADVANCED_FACE('',(#1201),#13877,.T.);
#14630=ADVANCED_FACE('',(#1202),#211,.T.);
#14631=ADVANCED_FACE('',(#1203),#294,.F.);
#14632=ADVANCED_FACE('',(#1204),#13878,.T.);
#14633=ADVANCED_FACE('',(#1205),#295,.F.);
#14634=ADVANCED_FACE('',(#1206),#13879,.T.);
#14635=ADVANCED_FACE('',(#1207),#500,.F.);
#14636=ADVANCED_FACE('',(#1208),#501,.F.);
#14637=ADVANCED_FACE('',(#1209),#502,.F.);
#14638=ADVANCED_FACE('',(#1210),#503,.F.);
#14639=ADVANCED_FACE('',(#1211),#504,.F.);
#14640=ADVANCED_FACE('',(#1212),#505,.F.);
#14641=ADVANCED_FACE('',(#1213),#506,.F.);
#14642=ADVANCED_FACE('',(#1214,#359),#507,.T.);
#14643=ADVANCED_FACE('',(#1215),#13880,.T.);
#14644=ADVANCED_FACE('',(#1216,#360),#508,.F.);
#14645=ADVANCED_FACE('',(#1217),#509,.T.);
#14739=CLOSED_SHELL('',(#14552,#14553,#14554,#14555,#14556,#14557,#14558,
#14559,#14560,#14561,#14562,#14563,#14564,#14565,#14566,#14567,#14568,#14569,
#14570,#14571,#14572,#14573,#14574,#14575,#14576,#14577,#14578,#14579,#14580,
#14581,#14582,#14583,#14584,#14585,#14586,#14587,#14588,#14589,#14590,#14591,
#14592,#14593,#14594,#14595,#14596,#14597,#14598,#14599,#14600,#14601,#14602,
#14603,#14604,#14605,#14606,#14607,#14608,#14609,#14610,#14611,#14612,#14613,
#14614,#14615,#14616,#14617,#14618,#14619,#14620,#14621,#14622,#14623,#14624,
#14625,#14626,#14627,#14628,#14629,#14630,#14631,#14632,#14633,#14634,#14635,
#14636,#14637,#14638,#14639,#14640,#14641,#14642,#14643,#14644,#14645));
#15615=AXIS2_PLACEMENT_3D('',#59292,#18028,#18029);
#15616=AXIS2_PLACEMENT_3D('',#59293,#18030,#18031);
#15617=AXIS2_PLACEMENT_3D('',#59309,#18033,#18034);
#15618=AXIS2_PLACEMENT_3D('',#59317,#18035,#18036);
#15619=AXIS2_PLACEMENT_3D('',#59365,#18038,#18039);
#15620=AXIS2_PLACEMENT_3D('',#59413,#18041,#18042);
#15621=AXIS2_PLACEMENT_3D('',#59464,#18044,#18045);
#15622=AXIS2_PLACEMENT_3D('',#59515,#18047,#18048);
#15623=AXIS2_PLACEMENT_3D('',#59563,#18050,#18051);
#15624=AXIS2_PLACEMENT_3D('',#59611,#18053,#18054);
#15625=AXIS2_PLACEMENT_3D('',#59665,#18056,#18057);
#15626=AXIS2_PLACEMENT_3D('',#59713,#18059,#18060);
#15627=AXIS2_PLACEMENT_3D('',#59761,#18062,#18063);
#15628=AXIS2_PLACEMENT_3D('',#59812,#18065,#18066);
#15629=AXIS2_PLACEMENT_3D('',#59863,#18068,#18069);
#15630=AXIS2_PLACEMENT_3D('',#59911,#18071,#18072);
#15631=AXIS2_PLACEMENT_3D('',#59962,#18074,#18075);
#15632=AXIS2_PLACEMENT_3D('',#60013,#18077,#18078);
#15633=AXIS2_PLACEMENT_3D('',#60061,#18080,#18081);
#15634=AXIS2_PLACEMENT_3D('',#60112,#18083,#18084);
#15635=AXIS2_PLACEMENT_3D('',#60160,#18086,#18087);
#15636=AXIS2_PLACEMENT_3D('',#60211,#18089,#18090);
#15637=AXIS2_PLACEMENT_3D('',#60259,#18092,#18093);
#15638=AXIS2_PLACEMENT_3D('',#60310,#18095,#18096);
#15639=AXIS2_PLACEMENT_3D('',#60361,#18098,#18099);
#15640=AXIS2_PLACEMENT_3D('',#60409,#18101,#18102);
#15641=AXIS2_PLACEMENT_3D('',#60460,#18104,#18105);
#15642=AXIS2_PLACEMENT_3D('',#60508,#18107,#18108);
#15643=AXIS2_PLACEMENT_3D('',#60559,#18110,#18111);
#15644=AXIS2_PLACEMENT_3D('',#60610,#18113,#18114);
#15645=AXIS2_PLACEMENT_3D('',#60658,#18116,#18117);
#15646=AXIS2_PLACEMENT_3D('',#60709,#18119,#18120);
#15647=AXIS2_PLACEMENT_3D('',#60760,#18122,#18123);
#15648=AXIS2_PLACEMENT_3D('',#60808,#18125,#18126);
#15649=AXIS2_PLACEMENT_3D('',#60856,#18128,#18129);
#15650=AXIS2_PLACEMENT_3D('',#60907,#18131,#18132);
#15651=AXIS2_PLACEMENT_3D('',#60958,#18134,#18135);
#15652=AXIS2_PLACEMENT_3D('',#61006,#18137,#18138);
#15653=AXIS2_PLACEMENT_3D('',#61057,#18140,#18141);
#15654=AXIS2_PLACEMENT_3D('',#61108,#18143,#18144);
#15655=AXIS2_PLACEMENT_3D('',#61156,#18146,#18147);
#15656=AXIS2_PLACEMENT_3D('',#61204,#18149,#18150);
#15657=AXIS2_PLACEMENT_3D('',#61220,#18152,#18153);
#15658=AXIS2_PLACEMENT_3D('',#61229,#18154,#18155);
#15659=AXIS2_PLACEMENT_3D('',#61254,#18157,#18158);
#15660=AXIS2_PLACEMENT_3D('',#61278,#18160,#18161);
#15661=AXIS2_PLACEMENT_3D('',#61302,#18163,#18164);
#15662=AXIS2_PLACEMENT_3D('',#61328,#18166,#18167);
#15663=AXIS2_PLACEMENT_3D('',#61352,#18169,#18170);
#15664=AXIS2_PLACEMENT_3D('',#61376,#18172,#18173);
#15665=AXIS2_PLACEMENT_3D('',#61402,#18175,#18176);
#15666=AXIS2_PLACEMENT_3D('',#61426,#18178,#18179);
#15667=AXIS2_PLACEMENT_3D('',#61450,#18181,#18182);
#15668=AXIS2_PLACEMENT_3D('',#61474,#18184,#18185);
#15669=AXIS2_PLACEMENT_3D('',#61500,#18187,#18188);
#15670=AXIS2_PLACEMENT_3D('',#61524,#18190,#18191);
#15671=AXIS2_PLACEMENT_3D('',#61548,#18193,#18194);
#15672=AXIS2_PLACEMENT_3D('',#61574,#18196,#18197);
#15673=AXIS2_PLACEMENT_3D('',#61598,#18199,#18200);
#15674=AXIS2_PLACEMENT_3D('',#61622,#18202,#18203);
#15675=AXIS2_PLACEMENT_3D('',#61647,#18205,#18206);
#15676=AXIS2_PLACEMENT_3D('',#61672,#18208,#18209);
#15677=AXIS2_PLACEMENT_3D('',#61696,#18211,#18212);
#15678=AXIS2_PLACEMENT_3D('',#61721,#18214,#18215);
#15679=AXIS2_PLACEMENT_3D('',#61746,#18217,#18218);
#15680=AXIS2_PLACEMENT_3D('',#61770,#18220,#18221);
#15681=AXIS2_PLACEMENT_3D('',#61794,#18223,#18224);
#15682=AXIS2_PLACEMENT_3D('',#61819,#18226,#18227);
#15683=AXIS2_PLACEMENT_3D('',#61844,#18229,#18230);
#15684=AXIS2_PLACEMENT_3D('',#61868,#18232,#18233);
#15685=AXIS2_PLACEMENT_3D('',#61893,#18235,#18236);
#15686=AXIS2_PLACEMENT_3D('',#61918,#18238,#18239);
#15687=AXIS2_PLACEMENT_3D('',#61942,#18241,#18242);
#15688=AXIS2_PLACEMENT_3D('',#61967,#18244,#18245);
#15689=AXIS2_PLACEMENT_3D('',#61991,#18247,#18248);
#15690=AXIS2_PLACEMENT_3D('',#62016,#18250,#18251);
#15691=AXIS2_PLACEMENT_3D('',#62041,#18253,#18254);
#15692=AXIS2_PLACEMENT_3D('',#62065,#18256,#18257);
#15693=AXIS2_PLACEMENT_3D('',#62090,#18259,#18260);
#15694=AXIS2_PLACEMENT_3D('',#62114,#18262,#18263);
#15695=AXIS2_PLACEMENT_3D('',#62139,#18265,#18266);
#15696=AXIS2_PLACEMENT_3D('',#62163,#18268,#18269);
#15697=AXIS2_PLACEMENT_3D('',#62457,#18270,#18271);
#15698=AXIS2_PLACEMENT_3D('',#62491,#18273,#18274);
#15699=AXIS2_PLACEMENT_3D('',#63622,#18275,#18276);
#15700=AXIS2_PLACEMENT_3D('',#63633,#18277,#18278);
#15701=AXIS2_PLACEMENT_3D('',#64767,#18279,#18280);
#15702=AXIS2_PLACEMENT_3D('',#64768,#18281,#18282);
#15703=AXIS2_PLACEMENT_3D('',#64777,#18287,#18288);
#15704=AXIS2_PLACEMENT_3D('',#64783,#18292,#18293);
#15705=AXIS2_PLACEMENT_3D('',#64789,#18297,#18298);
#15706=AXIS2_PLACEMENT_3D('',#64795,#18302,#18303);
#15707=AXIS2_PLACEMENT_3D('',#64801,#18307,#18308);
#15708=AXIS2_PLACEMENT_3D('',#64804,#18311,#18312);
#15709=AXIS2_PLACEMENT_3D('',#64805,#18313,#18314);
#15710=AXIS2_PLACEMENT_3D('',#64807,#18315,#18316);
#15711=AXIS2_PLACEMENT_3D('',#64808,#18317,#18318);
#15712=AXIS2_PLACEMENT_3D('',#64811,#18320,#18321);
#15713=AXIS2_PLACEMENT_3D('',#64812,#18322,#18323);
#15714=AXIS2_PLACEMENT_3D('',#64813,#18324,#18325);
#18028=DIRECTION('axis',(0.,0.,1.));
#18029=DIRECTION('refdir',(1.,0.,0.));
#18030=DIRECTION('center_axis',(0.,0.,1.));
#18031=DIRECTION('ref_axis',(1.,0.,0.));
#18032=DIRECTION('',(0.,0.,-1.));
#18033=DIRECTION('center_axis',(0.,0.,-1.));
#18034=DIRECTION('ref_axis',(1.,0.,0.));
#18035=DIRECTION('center_axis',(0.,0.,1.));
#18036=DIRECTION('ref_axis',(1.,0.,0.));
#18037=DIRECTION('',(0.,0.,-1.));
#18038=DIRECTION('center_axis',(0.,0.,1.));
#18039=DIRECTION('ref_axis',(1.,0.,0.));
#18040=DIRECTION('',(0.,0.,-1.));
#18041=DIRECTION('center_axis',(0.,0.,1.));
#18042=DIRECTION('ref_axis',(1.,0.,0.));
#18043=DIRECTION('',(0.,0.,-1.));
#18044=DIRECTION('center_axis',(0.,0.,1.));
#18045=DIRECTION('ref_axis',(1.,0.,0.));
#18046=DIRECTION('',(0.,0.,-1.));
#18047=DIRECTION('center_axis',(0.,0.,1.));
#18048=DIRECTION('ref_axis',(1.,0.,0.));
#18049=DIRECTION('',(0.,0.,-1.));
#18050=DIRECTION('center_axis',(0.,0.,1.));
#18051=DIRECTION('ref_axis',(1.,0.,0.));
#18052=DIRECTION('',(0.,0.,-1.));
#18053=DIRECTION('center_axis',(0.,0.,1.));
#18054=DIRECTION('ref_axis',(1.,0.,0.));
#18055=DIRECTION('',(0.,0.,-1.));
#18056=DIRECTION('center_axis',(0.,0.,1.));
#18057=DIRECTION('ref_axis',(1.,0.,0.));
#18058=DIRECTION('',(0.,0.,-1.));
#18059=DIRECTION('center_axis',(0.,0.,1.));
#18060=DIRECTION('ref_axis',(1.,0.,0.));
#18061=DIRECTION('',(0.,0.,-1.));
#18062=DIRECTION('center_axis',(0.,0.,1.));
#18063=DIRECTION('ref_axis',(1.,0.,0.));
#18064=DIRECTION('',(0.,0.,-1.));
#18065=DIRECTION('center_axis',(0.,0.,1.));
#18066=DIRECTION('ref_axis',(1.,0.,0.));
#18067=DIRECTION('',(0.,0.,-1.));
#18068=DIRECTION('center_axis',(0.,0.,1.));
#18069=DIRECTION('ref_axis',(1.,0.,0.));
#18070=DIRECTION('',(0.,0.,-1.));
#18071=DIRECTION('center_axis',(0.,0.,1.));
#18072=DIRECTION('ref_axis',(1.,0.,0.));
#18073=DIRECTION('',(0.,0.,-1.));
#18074=DIRECTION('center_axis',(0.,0.,1.));
#18075=DIRECTION('ref_axis',(1.,0.,0.));
#18076=DIRECTION('',(0.,0.,-1.));
#18077=DIRECTION('center_axis',(0.,0.,1.));
#18078=DIRECTION('ref_axis',(1.,0.,0.));
#18079=DIRECTION('',(0.,0.,-1.));
#18080=DIRECTION('center_axis',(0.,0.,1.));
#18081=DIRECTION('ref_axis',(1.,0.,0.));
#18082=DIRECTION('',(0.,0.,-1.));
#18083=DIRECTION('center_axis',(0.,0.,1.));
#18084=DIRECTION('ref_axis',(1.,0.,0.));
#18085=DIRECTION('',(0.,0.,-1.));
#18086=DIRECTION('center_axis',(0.,0.,1.));
#18087=DIRECTION('ref_axis',(1.,0.,0.));
#18088=DIRECTION('',(0.,0.,-1.));
#18089=DIRECTION('center_axis',(0.,0.,1.));
#18090=DIRECTION('ref_axis',(1.,0.,0.));
#18091=DIRECTION('',(0.,0.,-1.));
#18092=DIRECTION('center_axis',(0.,0.,1.));
#18093=DIRECTION('ref_axis',(1.,0.,0.));
#18094=DIRECTION('',(0.,0.,-1.));
#18095=DIRECTION('center_axis',(0.,0.,1.));
#18096=DIRECTION('ref_axis',(1.,0.,0.));
#18097=DIRECTION('',(0.,0.,-1.));
#18098=DIRECTION('center_axis',(0.,0.,1.));
#18099=DIRECTION('ref_axis',(1.,0.,0.));
#18100=DIRECTION('',(0.,0.,-1.));
#18101=DIRECTION('center_axis',(0.,0.,1.));
#18102=DIRECTION('ref_axis',(1.,0.,0.));
#18103=DIRECTION('',(0.,0.,-1.));
#18104=DIRECTION('center_axis',(0.,0.,1.));
#18105=DIRECTION('ref_axis',(1.,0.,0.));
#18106=DIRECTION('',(0.,0.,-1.));
#18107=DIRECTION('center_axis',(0.,0.,1.));
#18108=DIRECTION('ref_axis',(1.,0.,0.));
#18109=DIRECTION('',(0.,0.,-1.));
#18110=DIRECTION('center_axis',(0.,0.,1.));
#18111=DIRECTION('ref_axis',(1.,0.,0.));
#18112=DIRECTION('',(0.,0.,-1.));
#18113=DIRECTION('center_axis',(0.,0.,1.));
#18114=DIRECTION('ref_axis',(1.,0.,0.));
#18115=DIRECTION('',(0.,0.,-1.));
#18116=DIRECTION('center_axis',(0.,0.,1.));
#18117=DIRECTION('ref_axis',(1.,0.,0.));
#18118=DIRECTION('',(0.,0.,-1.));
#18119=DIRECTION('center_axis',(0.,0.,1.));
#18120=DIRECTION('ref_axis',(1.,0.,0.));
#18121=DIRECTION('',(0.,0.,-1.));
#18122=DIRECTION('center_axis',(0.,0.,1.));
#18123=DIRECTION('ref_axis',(1.,0.,0.));
#18124=DIRECTION('',(0.,0.,-1.));
#18125=DIRECTION('center_axis',(0.,0.,1.));
#18126=DIRECTION('ref_axis',(1.,0.,0.));
#18127=DIRECTION('',(0.,0.,-1.));
#18128=DIRECTION('center_axis',(0.,0.,1.));
#18129=DIRECTION('ref_axis',(1.,0.,0.));
#18130=DIRECTION('',(0.,0.,-1.));
#18131=DIRECTION('center_axis',(0.,0.,1.));
#18132=DIRECTION('ref_axis',(1.,0.,0.));
#18133=DIRECTION('',(0.,0.,-1.));
#18134=DIRECTION('center_axis',(0.,0.,1.));
#18135=DIRECTION('ref_axis',(1.,0.,0.));
#18136=DIRECTION('',(0.,0.,-1.));
#18137=DIRECTION('center_axis',(0.,0.,1.));
#18138=DIRECTION('ref_axis',(1.,0.,0.));
#18139=DIRECTION('',(0.,0.,-1.));
#18140=DIRECTION('center_axis',(0.,0.,1.));
#18141=DIRECTION('ref_axis',(1.,0.,0.));
#18142=DIRECTION('',(0.,0.,-1.));
#18143=DIRECTION('center_axis',(0.,0.,1.));
#18144=DIRECTION('ref_axis',(1.,0.,0.));
#18145=DIRECTION('',(0.,0.,-1.));
#18146=DIRECTION('center_axis',(0.,0.,1.));
#18147=DIRECTION('ref_axis',(1.,0.,0.));
#18148=DIRECTION('',(0.,0.,-1.));
#18149=DIRECTION('center_axis',(0.,0.,1.));
#18150=DIRECTION('ref_axis',(0.997336311962016,-0.0729402552915997,0.));
#18151=DIRECTION('',(0.,0.,1.));
#18152=DIRECTION('center_axis',(0.,0.,-1.));
#18153=DIRECTION('ref_axis',(1.,-4.53607687595903E-13,0.));
#18154=DIRECTION('center_axis',(0.,0.,1.));
#18155=DIRECTION('ref_axis',(1.,-4.53607687595903E-13,0.));
#18156=DIRECTION('',(0.,0.,1.));
#18157=DIRECTION('center_axis',(0.,0.,1.));
#18158=DIRECTION('ref_axis',(1.,-4.53607687595903E-13,0.));
#18159=DIRECTION('',(0.,0.,1.));
#18160=DIRECTION('center_axis',(0.,0.,1.));
#18161=DIRECTION('ref_axis',(1.,-4.53607687595903E-13,0.));
#18162=DIRECTION('',(0.,0.,1.));
#18163=DIRECTION('center_axis',(0.,0.,1.));
#18164=DIRECTION('ref_axis',(1.,-4.53607687595903E-13,0.));
#18165=DIRECTION('',(0.,0.,1.));
#18166=DIRECTION('center_axis',(0.,0.,1.));
#18167=DIRECTION('ref_axis',(1.,-4.53607687595903E-13,0.));
#18168=DIRECTION('',(0.,0.,1.));
#18169=DIRECTION('center_axis',(0.,0.,1.));
#18170=DIRECTION('ref_axis',(1.,-4.53607687595903E-13,0.));
#18171=DIRECTION('',(0.,0.,1.));
#18172=DIRECTION('center_axis',(0.,0.,1.));
#18173=DIRECTION('ref_axis',(1.,-4.53607687595903E-13,0.));
#18174=DIRECTION('',(0.,0.,1.));
#18175=DIRECTION('center_axis',(0.,0.,1.));
#18176=DIRECTION('ref_axis',(1.,-4.53607687595903E-13,0.));
#18177=DIRECTION('',(0.,0.,1.));
#18178=DIRECTION('center_axis',(0.,0.,1.));
#18179=DIRECTION('ref_axis',(1.,-4.53607687595903E-13,0.));
#18180=DIRECTION('',(0.,0.,1.));
#18181=DIRECTION('center_axis',(0.,0.,1.));
#18182=DIRECTION('ref_axis',(1.,-4.53607687595903E-13,0.));
#18183=DIRECTION('',(0.,0.,1.));
#18184=DIRECTION('center_axis',(0.,0.,1.));
#18185=DIRECTION('ref_axis',(1.,-4.53607687595903E-13,0.));
#18186=DIRECTION('',(0.,0.,1.));
#18187=DIRECTION('center_axis',(0.,0.,1.));
#18188=DIRECTION('ref_axis',(1.,-4.53607687595903E-13,0.));
#18189=DIRECTION('',(0.,0.,1.));
#18190=DIRECTION('center_axis',(0.,0.,1.));
#18191=DIRECTION('ref_axis',(1.,-4.53607687595903E-13,0.));
#18192=DIRECTION('',(0.,0.,1.));
#18193=DIRECTION('center_axis',(0.,0.,1.));
#18194=DIRECTION('ref_axis',(1.,-4.53607687595903E-13,0.));
#18195=DIRECTION('',(0.,0.,1.));
#18196=DIRECTION('center_axis',(0.,0.,1.));
#18197=DIRECTION('ref_axis',(1.,-4.53607687595903E-13,0.));
#18198=DIRECTION('',(0.,0.,1.));
#18199=DIRECTION('center_axis',(0.,0.,1.));
#18200=DIRECTION('ref_axis',(1.,-4.53607687595903E-13,0.));
#18201=DIRECTION('',(0.,0.,1.));
#18202=DIRECTION('center_axis',(0.,0.,1.));
#18203=DIRECTION('ref_axis',(1.,-4.53607687595903E-13,0.));
#18204=DIRECTION('',(0.,0.,1.));
#18205=DIRECTION('center_axis',(0.,0.,1.));
#18206=DIRECTION('ref_axis',(1.,-4.53607687595903E-13,0.));
#18207=DIRECTION('',(0.,0.,1.));
#18208=DIRECTION('center_axis',(0.,0.,1.));
#18209=DIRECTION('ref_axis',(1.,-4.53607687595903E-13,0.));
#18210=DIRECTION('',(0.,0.,1.));
#18211=DIRECTION('center_axis',(0.,0.,1.));
#18212=DIRECTION('ref_axis',(1.,-4.53607687595903E-13,0.));
#18213=DIRECTION('',(0.,0.,1.));
#18214=DIRECTION('center_axis',(0.,0.,1.));
#18215=DIRECTION('ref_axis',(1.,-4.53607687595903E-13,0.));
#18216=DIRECTION('',(0.,0.,1.));
#18217=DIRECTION('center_axis',(0.,0.,1.));
#18218=DIRECTION('ref_axis',(1.,-4.53607687595903E-13,0.));
#18219=DIRECTION('',(0.,0.,1.));
#18220=DIRECTION('center_axis',(0.,0.,1.));
#18221=DIRECTION('ref_axis',(1.,-4.53607687595903E-13,0.));
#18222=DIRECTION('',(0.,0.,1.));
#18223=DIRECTION('center_axis',(0.,0.,1.));
#18224=DIRECTION('ref_axis',(1.,-4.53607687595903E-13,0.));
#18225=DIRECTION('',(0.,0.,1.));
#18226=DIRECTION('center_axis',(0.,0.,1.));
#18227=DIRECTION('ref_axis',(1.,-4.53607687595903E-13,0.));
#18228=DIRECTION('',(0.,0.,1.));
#18229=DIRECTION('center_axis',(0.,0.,1.));
#18230=DIRECTION('ref_axis',(1.,-4.53607687595903E-13,0.));
#18231=DIRECTION('',(0.,0.,1.));
#18232=DIRECTION('center_axis',(0.,0.,1.));
#18233=DIRECTION('ref_axis',(1.,-4.53607687595903E-13,0.));
#18234=DIRECTION('',(0.,0.,1.));
#18235=DIRECTION('center_axis',(0.,0.,1.));
#18236=DIRECTION('ref_axis',(1.,-4.53607687595903E-13,0.));
#18237=DIRECTION('',(0.,0.,1.));
#18238=DIRECTION('center_axis',(0.,0.,1.));
#18239=DIRECTION('ref_axis',(1.,-4.53607687595903E-13,0.));
#18240=DIRECTION('',(0.,0.,1.));
#18241=DIRECTION('center_axis',(0.,0.,1.));
#18242=DIRECTION('ref_axis',(1.,-4.53607687595903E-13,0.));
#18243=DIRECTION('',(0.,0.,1.));
#18244=DIRECTION('center_axis',(0.,0.,1.));
#18245=DIRECTION('ref_axis',(1.,-4.53607687595903E-13,0.));
#18246=DIRECTION('',(0.,0.,1.));
#18247=DIRECTION('center_axis',(0.,0.,1.));
#18248=DIRECTION('ref_axis',(1.,-4.53607687595903E-13,0.));
#18249=DIRECTION('',(0.,0.,1.));
#18250=DIRECTION('center_axis',(0.,0.,1.));
#18251=DIRECTION('ref_axis',(1.,-4.53607687595903E-13,0.));
#18252=DIRECTION('',(0.,0.,1.));
#18253=DIRECTION('center_axis',(0.,0.,1.));
#18254=DIRECTION('ref_axis',(1.,-4.53607687595903E-13,0.));
#18255=DIRECTION('',(0.,0.,1.));
#18256=DIRECTION('center_axis',(0.,0.,1.));
#18257=DIRECTION('ref_axis',(1.,-4.53607687595903E-13,0.));
#18258=DIRECTION('',(0.,0.,1.));
#18259=DIRECTION('center_axis',(0.,0.,1.));
#18260=DIRECTION('ref_axis',(1.,-4.53607687595903E-13,0.));
#18261=DIRECTION('',(0.,0.,1.));
#18262=DIRECTION('center_axis',(0.,0.,1.));
#18263=DIRECTION('ref_axis',(1.,-4.53607687595903E-13,0.));
#18264=DIRECTION('',(0.,0.,1.));
#18265=DIRECTION('center_axis',(0.,0.,1.));
#18266=DIRECTION('ref_axis',(1.,-4.53607687595903E-13,0.));
#18267=DIRECTION('',(0.,0.,1.));
#18268=DIRECTION('center_axis',(0.,0.,-1.));
#18269=DIRECTION('ref_axis',(1.,0.,0.));
#18270=DIRECTION('center_axis',(0.,0.,-1.));
#18271=DIRECTION('ref_axis',(1.,0.,0.));
#18272=DIRECTION('',(0.707106781186547,8.65956056235493E-17,0.707106781186548));
#18273=DIRECTION('center_axis',(0.,0.,1.));
#18274=DIRECTION('ref_axis',(1.,0.,0.));
#18275=DIRECTION('center_axis',(0.,0.,1.));
#18276=DIRECTION('ref_axis',(1.,-4.53607687595903E-13,0.));
#18277=DIRECTION('center_axis',(0.,0.,-1.));
#18278=DIRECTION('ref_axis',(1.,-4.53607687595903E-13,0.));
#18279=DIRECTION('center_axis',(0.,0.,1.));
#18280=DIRECTION('ref_axis',(1.,0.,0.));
#18281=DIRECTION('center_axis',(-1.92296268638356E-16,-1.,0.));
#18282=DIRECTION('ref_axis',(1.,-1.92296268638356E-16,0.));
#18283=DIRECTION('',(1.,-1.92296268638356E-16,0.));
#18284=DIRECTION('',(0.,0.,1.));
#18285=DIRECTION('',(1.,-1.92296268638356E-16,0.));
#18286=DIRECTION('',(0.,0.,1.));
#18287=DIRECTION('center_axis',(-0.866025403784439,-0.5,0.));
#18288=DIRECTION('ref_axis',(0.5,-0.866025403784439,0.));
#18289=DIRECTION('',(0.5,-0.866025403784439,0.));
#18290=DIRECTION('',(0.,0.,1.));
#18291=DIRECTION('',(0.5,-0.866025403784439,0.));
#18292=DIRECTION('center_axis',(-0.866025403784439,0.5,0.));
#18293=DIRECTION('ref_axis',(-0.5,-0.866025403784438,0.));
#18294=DIRECTION('',(-0.5,-0.866025403784438,0.));
#18295=DIRECTION('',(0.,0.,1.));
#18296=DIRECTION('',(-0.5,-0.866025403784439,0.));
#18297=DIRECTION('center_axis',(1.92296268638356E-16,1.,0.));
#18298=DIRECTION('ref_axis',(-1.,1.92296268638356E-16,0.));
#18299=DIRECTION('',(-1.,1.92296268638356E-16,0.));
#18300=DIRECTION('',(0.,0.,1.));
#18301=DIRECTION('',(-1.,1.92296268638356E-16,0.));
#18302=DIRECTION('center_axis',(0.866025403784439,0.5,0.));
#18303=DIRECTION('ref_axis',(-0.5,0.866025403784439,0.));
#18304=DIRECTION('',(-0.5,0.866025403784439,0.));
#18305=DIRECTION('',(0.,0.,1.));
#18306=DIRECTION('',(-0.5,0.866025403784439,0.));
#18307=DIRECTION('center_axis',(0.866025403784439,-0.5,0.));
#18308=DIRECTION('ref_axis',(0.5,0.866025403784439,0.));
#18309=DIRECTION('',(0.5,0.866025403784439,0.));
#18310=DIRECTION('',(0.5,0.866025403784439,0.));
#18311=DIRECTION('center_axis',(0.,0.,1.));
#18312=DIRECTION('ref_axis',(1.,0.,0.));
#18313=DIRECTION('center_axis',(0.,0.,1.));
#18314=DIRECTION('ref_axis',(1.,0.,0.));
#18315=DIRECTION('center_axis',(0.,0.,1.));
#18316=DIRECTION('ref_axis',(1.,0.,0.));
#18317=DIRECTION('center_axis',(0.,0.,1.));
#18318=DIRECTION('ref_axis',(1.,0.,0.));
#18319=DIRECTION('',(0.,0.,-1.));
#18320=DIRECTION('center_axis',(0.,0.,1.));
#18321=DIRECTION('ref_axis',(1.,0.,0.));
#18322=DIRECTION('center_axis',(0.,0.,1.));
#18323=DIRECTION('ref_axis',(1.,0.,0.));
#18324=DIRECTION('center_axis',(0.,0.,1.));
#18325=DIRECTION('ref_axis',(1.,0.,0.));
#59292=CARTESIAN_POINT('',(0.,0.,0.));
#59293=CARTESIAN_POINT('Origin',(0.,0.,0.));
#59294=CARTESIAN_POINT('',(-2.94578277890271,0.00179111083247481,0.322176117089595));
#59295=CARTESIAN_POINT('',(-2.94467343002877,0.00314729851841336,0.177823882910467));
#59296=CARTESIAN_POINT('',(-2.942,-3.60291088309151E-16,0.));
#59297=CARTESIAN_POINT('',(1.28892185405323,2.64462557919718,0.));
#59298=CARTESIAN_POINT('Ctrl Pts',(-2.94578277890271,0.00179111083247481,
0.322176117089595));
#59299=CARTESIAN_POINT('Ctrl Pts',(-2.94637589714326,0.0927166687183431,
0.317238878916034));
#59300=CARTESIAN_POINT('Ctrl Pts',(-2.94253410879075,0.183587894393493,
0.312301640742474));
#59301=CARTESIAN_POINT('Ctrl Pts',(-2.93409440150521,0.274025695936747,
0.307364402568913));
#59302=CARTESIAN_POINT('Ctrl Pts',(-2.84341104252089,1.24576598806222,0.254314536437722));
#59303=CARTESIAN_POINT('Ctrl Pts',(-2.22189000884716,2.16746671627164,0.20126467030653));
#59304=CARTESIAN_POINT('Ctrl Pts',(-1.35502173669404,2.61657805746752,0.148214804175339));
#59305=CARTESIAN_POINT('Ctrl Pts',(-0.547713942644492,3.03483201575685,
0.0988098694502261));
#59306=CARTESIAN_POINT('Ctrl Pts',(0.472384848283181,3.0432066234576,0.0494049347251131));
#59307=CARTESIAN_POINT('Ctrl Pts',(1.29201581877684,2.64862154577367,3.40875331157512E-17));
#59308=CARTESIAN_POINT('',(-1.28892185405299,2.64462557919729,0.));
#59309=CARTESIAN_POINT('Origin',(0.,0.,0.));
#59310=CARTESIAN_POINT('Ctrl Pts',(-1.28892185405299,2.64462557919729,-1.41553435639707E-14));
#59311=CARTESIAN_POINT('Ctrl Pts',(-2.1671763893535,2.21658711777033,0.0528538148029031));
#59312=CARTESIAN_POINT('Ctrl Pts',(-2.80795602549936,1.32047159410707,0.105707629605821));
#59313=CARTESIAN_POINT('Ctrl Pts',(-2.9249109785407,0.356582248145783,0.158561444408738));
#59314=CARTESIAN_POINT('Ctrl Pts',(-2.93911895702394,0.23948657385823,0.164982257242648));
#59315=CARTESIAN_POINT('Ctrl Pts',(-2.94559633372376,0.121390693875098,
0.171403070076557));
#59316=CARTESIAN_POINT('Ctrl Pts',(-2.94467343002877,0.00314729851841336,
0.177823882910467));
#59317=CARTESIAN_POINT('Origin',(0.,0.,0.));
#59318=CARTESIAN_POINT('',(-2.93831560050017,0.00184555222839333,1.32217611708959));
#59319=CARTESIAN_POINT('',(-2.93760127776231,0.0011368673086444,1.17782388291046));
#59320=CARTESIAN_POINT('',(-2.942,-3.60291088309151E-16,0.));
#59321=CARTESIAN_POINT('Ctrl Pts',(-2.93831560050017,0.00184555222839333,
1.32217611708959));
#59322=CARTESIAN_POINT('Ctrl Pts',(-2.94042418966808,0.372080548742382,
1.30220474236985));
#59323=CARTESIAN_POINT('Ctrl Pts',(-2.87561341710461,0.741603687830221,
1.2822333676501));
#59324=CARTESIAN_POINT('Ctrl Pts',(-2.74052219187739,1.08334315658386,1.26226199293036));
#59325=CARTESIAN_POINT('Ctrl Pts',(-2.38168002330511,1.99110405554696,1.20921212679917));
#59326=CARTESIAN_POINT('Ctrl Pts',(-1.52694572694536,2.70282604358144,1.15616226066798));
#59327=CARTESIAN_POINT('Ctrl Pts',(-0.569210306211631,2.89137544039496,
1.10311239453678));
#59328=CARTESIAN_POINT('Ctrl Pts',(0.388525114522094,3.07992483720848,1.05006252840559));
#59329=CARTESIAN_POINT('Ctrl Pts',(1.4492616596298,2.74530164280104,0.997012662274401));
#59330=CARTESIAN_POINT('Ctrl Pts',(2.12540309125483,2.04127771721126,0.94396279614321));
#59331=CARTESIAN_POINT('Ctrl Pts',(2.80154452287985,1.33725379162148,0.890912930012018));
#59332=CARTESIAN_POINT('Ctrl Pts',(3.0930908410222,0.263829134849373,0.837863063880828));
#59333=CARTESIAN_POINT('Ctrl Pts',(2.86604250647906,-0.685491427036063,
0.784813197749637));
#59334=CARTESIAN_POINT('Ctrl Pts',(2.63899417193593,-1.63481198892151,0.731763331618445));
#59335=CARTESIAN_POINT('Ctrl Pts',(1.8933511847073,-2.46002845592027,0.678713465487253));
#59336=CARTESIAN_POINT('Ctrl Pts',(0.97183346999997,-2.78197492031178,0.625663599356061));
#59337=CARTESIAN_POINT('Ctrl Pts',(0.0503157552926523,-3.10392138470329,
0.57261373322487));
#59338=CARTESIAN_POINT('Ctrl Pts',(-1.04707668689336,-2.92259784648754,
0.519563867093679));
#59339=CARTESIAN_POINT('Ctrl Pts',(-1.81585006583891,-2.3210461493589,0.466514000962488));
#59340=CARTESIAN_POINT('Ctrl Pts',(-2.51307534202467,-1.77547958883907,
0.418401373004857));
#59341=CARTESIAN_POINT('Ctrl Pts',(-2.94000293271358,-0.884264490420376,
0.370288745047226));
#59342=CARTESIAN_POINT('Ctrl Pts',(-2.94578277890271,0.00179111083247481,
0.322176117089595));
#59343=CARTESIAN_POINT('Ctrl Pts',(-2.94467343002877,0.00314729851841336,
0.177823882910467));
#59344=CARTESIAN_POINT('Ctrl Pts',(-2.93799932346391,-0.851946277862307,
0.224256884879474));
#59345=CARTESIAN_POINT('Ctrl Pts',(-2.54431566930391,-1.71475440760266,
0.270689886848481));
#59346=CARTESIAN_POINT('Ctrl Pts',(-1.88854677527079,-2.26279797837909,
0.317122888817489));
#59347=CARTESIAN_POINT('Ctrl Pts',(-1.14209734902272,-2.88662569068338,
0.369976703620406));
#59348=CARTESIAN_POINT('Ctrl Pts',(-0.0560682265897754,-3.10261794703268,
0.422830518423324));
#59349=CARTESIAN_POINT('Ctrl Pts',(0.872963891668672,-2.8142569045846,0.475684333226241));
#59350=CARTESIAN_POINT('Ctrl Pts',(1.80199600992712,-2.52589586213653,0.528538148029158));
#59351=CARTESIAN_POINT('Ctrl Pts',(2.57403112401107,-1.73318152089108,0.581391962832075));
#59352=CARTESIAN_POINT('Ctrl Pts',(2.83696576039216,-0.796977059524136,
0.634245777634992));
#59353=CARTESIAN_POINT('Ctrl Pts',(3.09990039677324,0.139227401842806,0.68709959243791));
#59354=CARTESIAN_POINT('Ctrl Pts',(2.85373455545147,1.21892198333124,0.739953407240827));
#59355=CARTESIAN_POINT('Ctrl Pts',(2.21066027791899,1.94860552630545,0.792807222043744));
#59356=CARTESIAN_POINT('Ctrl Pts',(1.56758600038652,2.67828906927967,0.845661036846661));
#59357=CARTESIAN_POINT('Ctrl Pts',(0.527603286643354,3.05796157373966,0.898514851649578));
#59358=CARTESIAN_POINT('Ctrl Pts',(-0.434365791604633,2.91456720332865,
0.951368666452495));
#59359=CARTESIAN_POINT('Ctrl Pts',(-1.39633486985262,2.77117283291763,1.00422248125541));
#59360=CARTESIAN_POINT('Ctrl Pts',(-2.28029031260542,2.10471158763561,1.05707629605833));
#59361=CARTESIAN_POINT('Ctrl Pts',(-2.68270470090093,1.21931408472001,1.10993011086125));
#59362=CARTESIAN_POINT('Ctrl Pts',(-2.85501286099708,0.840199373321872,
1.13256136821099));
#59363=CARTESIAN_POINT('Ctrl Pts',(-2.9390337672121,0.420944198753331,1.15519262556072));
#59364=CARTESIAN_POINT('Ctrl Pts',(-2.93760127776231,0.0011368673086444,
1.17782388291046));
#59365=CARTESIAN_POINT('Origin',(0.,0.,0.));
#59366=CARTESIAN_POINT('',(-2.93907445095043,-0.00223594544481509,2.3221761170896));
#59367=CARTESIAN_POINT('',(-2.94106450717812,-0.00264273247052857,2.17782388291046));
#59368=CARTESIAN_POINT('',(-2.942,-3.60291088309151E-16,0.));
#59369=CARTESIAN_POINT('Ctrl Pts',(-2.93907445095043,-0.00223594544481509,
2.3221761170896));
#59370=CARTESIAN_POINT('Ctrl Pts',(-2.93451423355693,0.646284517263058,
2.28717060582367));
#59371=CARTESIAN_POINT('Ctrl Pts',(-2.72312957542652,1.29750586897281,2.25216509455774));
#59372=CARTESIAN_POINT('Ctrl Pts',(-2.32830278838925,1.80640429077704,2.2171595832918));
#59373=CARTESIAN_POINT('Ctrl Pts',(-1.72995391588694,2.57762551208695,2.16410971716061));
#59374=CARTESIAN_POINT('Ctrl Pts',(-0.710301786504807,3.02198008474211,
2.11105985102942));
#59375=CARTESIAN_POINT('Ctrl Pts',(0.261950767826724,2.93521227313122,2.05800998489823));
#59376=CARTESIAN_POINT('Ctrl Pts',(1.23420332215825,2.84844446152033,2.00496011876704));
#59377=CARTESIAN_POINT('Ctrl Pts',(2.15905630143918,2.23055426564339,1.95191025263585));
#59378=CARTESIAN_POINT('Ctrl Pts',(2.611382890642,1.36556600713954,1.89886038650466));
#59379=CARTESIAN_POINT('Ctrl Pts',(3.06370947984483,0.500577748635682,1.84581052037347));
#59380=CARTESIAN_POINT('Ctrl Pts',(3.04350967896956,-0.611508572495087,
1.79276065424227));
#59381=CARTESIAN_POINT('Ctrl Pts',(2.56006903828727,-1.45949911536289,1.73971078811108));
#59382=CARTESIAN_POINT('Ctrl Pts',(2.07662839760498,-2.3074896582307,1.68666092197989));
#59383=CARTESIAN_POINT('Ctrl Pts',(1.12994691711567,-2.89138442283555,1.6336110558487));
#59384=CARTESIAN_POINT('Ctrl Pts',(0.155184530430073,-2.94278816759169,
1.58056118971751));
#59385=CARTESIAN_POINT('Ctrl Pts',(-0.819577856255521,-2.99419191234782,
1.52751132358632));
#59386=CARTESIAN_POINT('Ctrl Pts',(-1.82242114913739,-2.51310463725525,
1.47446145745513));
#59387=CARTESIAN_POINT('Ctrl Pts',(-2.39236777518593,-1.7206610947631,1.42141159132393));
#59388=CARTESIAN_POINT('Ctrl Pts',(-2.74774990806646,-1.22654416618201,
1.38833309991249));
#59389=CARTESIAN_POINT('Ctrl Pts',(-2.93482315445378,-0.611372882869942,
1.35525460850104));
#59390=CARTESIAN_POINT('Ctrl Pts',(-2.93831560050017,0.00184555222839333,
1.32217611708959));
#59391=CARTESIAN_POINT('Ctrl Pts',(-2.93760127776231,0.0011368673086444,
1.17782388291046));
#59392=CARTESIAN_POINT('Ctrl Pts',(-2.93568828220805,-0.559488245020752,
1.20804644036364));
#59393=CARTESIAN_POINT('Ctrl Pts',(-2.78137900093947,-1.12109806552238,
1.23826899781682));
#59394=CARTESIAN_POINT('Ctrl Pts',(-2.48142253148132,-1.58940935219029,
1.26849155527));
#59395=CARTESIAN_POINT('Ctrl Pts',(-1.956852639928,-2.40840152563582,1.32134537007292));
#59396=CARTESIAN_POINT('Ctrl Pts',(-0.986839522983141,-2.94205211197772,
1.37419918487583));
#59397=CARTESIAN_POINT('Ctrl Pts',(-0.0142707720111539,-2.94675725529095,
1.42705299967875));
#59398=CARTESIAN_POINT('Ctrl Pts',(0.958297978960832,-2.95146239860418,
1.47990681448167));
#59399=CARTESIAN_POINT('Ctrl Pts',(1.93342236395995,-2.42722209888874,1.53276062928459));
#59400=CARTESIAN_POINT('Ctrl Pts',(2.46590395666548,-1.61336359456041,1.5856144440875));
#59401=CARTESIAN_POINT('Ctrl Pts',(2.99838554937101,-0.799505090232077,
1.63846825889042));
#59402=CARTESIAN_POINT('Ctrl Pts',(3.08822434978297,0.303971618709142,1.69132207369334));
#59403=CARTESIAN_POINT('Ctrl Pts',(2.69439912910768,1.19324786258786,1.74417588849625));
#59404=CARTESIAN_POINT('Ctrl Pts',(2.3005739084324,2.08252410646659,1.79702970329917));
#59405=CARTESIAN_POINT('Ctrl Pts',(1.42308466666986,2.75759988528281,1.84988351810209));
#59406=CARTESIAN_POINT('Ctrl Pts',(0.462563168363892,2.91026618027041,1.90273733290501));
#59407=CARTESIAN_POINT('Ctrl Pts',(-0.497958329942082,3.06293247525801,
1.95559114770792));
#59408=CARTESIAN_POINT('Ctrl Pts',(-1.54151208479149,2.69318928641698,2.00844496251084));
#59409=CARTESIAN_POINT('Ctrl Pts',(-2.19165060625059,1.96984474512453,2.06129877731376));
#59410=CARTESIAN_POINT('Ctrl Pts',(-2.66943043569144,1.43826659653236,2.10014047917933));
#59411=CARTESIAN_POINT('Ctrl Pts',(-2.93474154792488,0.715721704963004,
2.13898218104489));
#59412=CARTESIAN_POINT('Ctrl Pts',(-2.94106450717812,-0.00264273247052857,
2.17782388291046));
#59413=CARTESIAN_POINT('Origin',(0.,0.,0.));
#59414=CARTESIAN_POINT('',(-2.94645640454328,-0.00101572304112452,3.32217611708959));
#59415=CARTESIAN_POINT('',(-2.94656901584595,0.000739931193793274,3.17782388291046));
#59416=CARTESIAN_POINT('',(-2.942,-3.60291088309151E-16,0.));
#59417=CARTESIAN_POINT('Ctrl Pts',(-2.94645640454328,-0.00101572304112452,
3.32217611708959));
#59418=CARTESIAN_POINT('Ctrl Pts',(-2.94234855388754,0.920065526773415,
3.27213646927748));
#59419=CARTESIAN_POINT('Ctrl Pts',(-2.47563861836594,1.8447343524899,3.22209682146536));
#59420=CARTESIAN_POINT('Ctrl Pts',(-1.73034924050614,2.38536824088973,3.17205717365325));
#59421=CARTESIAN_POINT('Ctrl Pts',(-0.94022573937933,2.95852486088202,3.11900730752206));
#59422=CARTESIAN_POINT('Ctrl Pts',(0.163002154399846,3.10005226661288,3.06595744139087));
#59423=CARTESIAN_POINT('Ctrl Pts',(1.07221429851196,2.74489464521787,3.01290757525968));
#59424=CARTESIAN_POINT('Ctrl Pts',(1.98142644262409,2.38973702382286,2.95985770912849));
#59425=CARTESIAN_POINT('Ctrl Pts',(2.69662283706915,1.53789437530197,2.90680784299729));
#59426=CARTESIAN_POINT('Ctrl Pts',(2.88904955483864,0.580932710785723,2.8537579768661));
#59427=CARTESIAN_POINT('Ctrl Pts',(3.08147627260814,-0.376028953730528,
2.80070811073491));
#59428=CARTESIAN_POINT('Ctrl Pts',(2.75113331370206,-1.43810963424215,2.74765824460372));
#59429=CARTESIAN_POINT('Ctrl Pts',(2.0498692464734,-2.11710326668621,2.69460837847253));
#59430=CARTESIAN_POINT('Ctrl Pts',(1.34860517924474,-2.79609689913027,2.64155851234134));
#59431=CARTESIAN_POINT('Ctrl Pts',(0.2764200036935,-3.09200348350679,2.58850864621014));
#59432=CARTESIAN_POINT('Ctrl Pts',(-0.673835537461917,-2.86880387612486,
2.53545878007895));
#59433=CARTESIAN_POINT('Ctrl Pts',(-1.62409107861733,-2.64560426874294,
2.48240891394776));
#59434=CARTESIAN_POINT('Ctrl Pts',(-2.45241698537691,-1.90329846960257,
2.42935904781657));
#59435=CARTESIAN_POINT('Ctrl Pts',(-2.77805713094547,-0.98310163505006,
2.37630918168538));
#59436=CARTESIAN_POINT('Ctrl Pts',(-2.8888202067746,-0.670106345156332,
2.35826482682012));
#59437=CARTESIAN_POINT('Ctrl Pts',(-2.94142511454412,-0.336529973536149,
2.34022047195486));
#59438=CARTESIAN_POINT('Ctrl Pts',(-2.93907445095043,-0.00223594544481509,
2.3221761170896));
#59439=CARTESIAN_POINT('Ctrl Pts',(-2.94106450717812,-0.00264273247052857,
2.17782388291046));
#59440=CARTESIAN_POINT('Ctrl Pts',(-2.94334550968056,-0.261792129742843,
2.19183599584781));
#59441=CARTESIAN_POINT('Ctrl Pts',(-2.91192179745946,-0.520397482770503,
2.20584810878516));
#59442=CARTESIAN_POINT('Ctrl Pts',(-2.84460938087215,-0.769297041196698,
2.21986022172251));
#59443=CARTESIAN_POINT('Ctrl Pts',(-2.59070634596583,-1.70814839248162,
2.27271403652542));
#59444=CARTESIAN_POINT('Ctrl Pts',(-1.82617698808441,-2.50890520130758,
2.32556785132834));
#59445=CARTESIAN_POINT('Ctrl Pts',(-0.900077862744179,-2.80597194921199,
2.37842166613126));
#59446=CARTESIAN_POINT('Ctrl Pts',(0.0260212625960488,-3.1030386971164,
2.43127548093418));
#59447=CARTESIAN_POINT('Ctrl Pts',(1.11369015539508,-2.89641538409926,2.48412929573709));
#59448=CARTESIAN_POINT('Ctrl Pts',(1.86633899573991,-2.28043823425261,2.53698311054001));
#59449=CARTESIAN_POINT('Ctrl Pts',(2.61898783608474,-1.66446108440595,2.58983692534293));
#59450=CARTESIAN_POINT('Ctrl Pts',(3.03661662397538,-0.63913009772978,2.64269074014585));
#59451=CARTESIAN_POINT('Ctrl Pts',(2.92855118796608,0.327425723295819,2.69554455494876));
#59452=CARTESIAN_POINT('Ctrl Pts',(2.82048575195678,1.29398154432143,2.74839836975168));
#59453=CARTESIAN_POINT('Ctrl Pts',(2.18672609204752,2.20176219969646,2.8012521845546));
#59454=CARTESIAN_POINT('Ctrl Pts',(1.31662381963688,2.63630824527895,2.85410599935752));
#59455=CARTESIAN_POINT('Ctrl Pts',(0.446521547226236,3.07085429086145,2.90695981416043));
#59456=CARTESIAN_POINT('Ctrl Pts',(-0.659923337685789,3.03216572665139,
2.95981362896335));
#59457=CARTESIAN_POINT('Ctrl Pts',(-1.49754844237796,2.53790627629345,3.01266744376627));
#59458=CARTESIAN_POINT('Ctrl Pts',(-2.33517354707012,2.04364682593551,3.06552125856918));
#59459=CARTESIAN_POINT('Ctrl Pts',(-2.90397887154242,1.09381648942966,3.1183750733721));
#59460=CARTESIAN_POINT('Ctrl Pts',(-2.94426861939999,0.12207322109005,3.17122888817502));
#59461=CARTESIAN_POINT('Ctrl Pts',(-2.94594437781657,0.0816558184686259,
3.1734272197535));
#59462=CARTESIAN_POINT('Ctrl Pts',(-2.94670583035639,0.0412005075560573,
3.17562555133198));
#59463=CARTESIAN_POINT('Ctrl Pts',(-2.94656901584595,0.000739931193793274,
3.17782388291046));
#59464=CARTESIAN_POINT('Origin',(0.,0.,0.));
#59465=CARTESIAN_POINT('',(-2.94218751408198,0.00271333560157655,4.32217611708959));
#59466=CARTESIAN_POINT('',(-2.93894157525109,0.00211448818579894,4.17782388291047));
#59467=CARTESIAN_POINT('',(-2.942,-3.60291088309151E-16,0.));
#59468=CARTESIAN_POINT('Ctrl Pts',(-2.94218751408198,0.00271333560157655,
4.32217611708959));
#59469=CARTESIAN_POINT('Ctrl Pts',(-2.94425072300269,0.224874109476442,
4.31015219886249));
#59470=CARTESIAN_POINT('Ctrl Pts',(-2.92122841359833,0.446611437489588,
4.29812828063538));
#59471=CARTESIAN_POINT('Ctrl Pts',(-2.87151357587431,0.662193261821331,
4.28610436240827));
#59472=CARTESIAN_POINT('Ctrl Pts',(-2.65217031054445,1.61334634728837,4.23305449627708));
#59473=CARTESIAN_POINT('Ctrl Pts',(-1.91323048328662,2.4446764429101,4.18000463014589));
#59474=CARTESIAN_POINT('Ctrl Pts',(-0.994362148038726,2.77404651207381,
4.1269547640147));
#59475=CARTESIAN_POINT('Ctrl Pts',(-0.0754938127908314,3.10341658123751,
4.0739048978835));
#59476=CARTESIAN_POINT('Ctrl Pts',(1.02330303044713,2.9308266239432,4.02085503175231));
#59477=CARTESIAN_POINT('Ctrl Pts',(1.79694505607989,2.33561096879262,3.96780516562112));
#59478=CARTESIAN_POINT('Ctrl Pts',(2.57058708171265,1.74039531364205,3.91475529948993));
#59479=CARTESIAN_POINT('Ctrl Pts',(3.01907428974022,0.722553960635232,3.86170543335874));
#59480=CARTESIAN_POINT('Ctrl Pts',(2.93625081795067,-0.250042529555778,
3.80865556722755));
#59481=CARTESIAN_POINT('Ctrl Pts',(2.85342734616113,-1.22263901974679,3.75560570109635));
#59482=CARTESIAN_POINT('Ctrl Pts',(2.23929319455449,-2.14999064712199,3.70255583496516));
#59483=CARTESIAN_POINT('Ctrl Pts',(1.37614706260187,-2.60582221104315,3.64950596883397));
#59484=CARTESIAN_POINT('Ctrl Pts',(0.513000930649261,-3.06165377496431,
3.59645610270278));
#59485=CARTESIAN_POINT('Ctrl Pts',(-0.599157181649314,-3.04596527543143,
3.54340623657159));
#59486=CARTESIAN_POINT('Ctrl Pts',(-1.44910218190426,-2.5659682376169,3.4903563704404));
#59487=CARTESIAN_POINT('Ctrl Pts',(-2.29904718215921,-2.08597119980237,
3.43730650430921));
#59488=CARTESIAN_POINT('Ctrl Pts',(-2.88677907037054,-1.14166562370618,
3.38425663817802));
#59489=CARTESIAN_POINT('Ctrl Pts',(-2.94213546023897,-0.16711991853123,
3.33120677204682));
#59490=CARTESIAN_POINT('Ctrl Pts',(-2.94527655805905,-0.111821092192249,
3.32819655372775));
#59491=CARTESIAN_POINT('Ctrl Pts',(-2.94670351913813,-0.0564248990201435,
3.32518633540867));
#59492=CARTESIAN_POINT('Ctrl Pts',(-2.94645640454328,-0.00101572304112452,
3.32217611708959));
#59493=CARTESIAN_POINT('Ctrl Pts',(-2.94656901584595,0.000739931193793274,
3.17782388291046));
#59494=CARTESIAN_POINT('Ctrl Pts',(-2.94341644086314,-0.931580773849932,
3.2284793661349));
#59495=CARTESIAN_POINT('Ctrl Pts',(-2.46331480529716,-1.86669725247251,
3.27913484935933));
#59496=CARTESIAN_POINT('Ctrl Pts',(-1.70249726223018,-2.40522818466485,
3.32979033258377));
#59497=CARTESIAN_POINT('Ctrl Pts',(-0.908661985959945,-2.96713012190678,
3.38264414738669));
#59498=CARTESIAN_POINT('Ctrl Pts',(0.190782737823382,-3.09727779621724,
3.4354979621896));
#59499=CARTESIAN_POINT('Ctrl Pts',(1.0938705148769,-2.73625051267428,3.48835177699252));
#59500=CARTESIAN_POINT('Ctrl Pts',(1.99695829193042,-2.37522322913131,3.54120559179544));
#59501=CARTESIAN_POINT('Ctrl Pts',(2.70368912225412,-1.5230209877349,3.59405940659836));
#59502=CARTESIAN_POINT('Ctrl Pts',(2.89139545991222,-0.568728282942871,
3.64691322140127));
#59503=CARTESIAN_POINT('Ctrl Pts',(3.07910179757031,0.385564421849148,3.69976703620419));
#59504=CARTESIAN_POINT('Ctrl Pts',(2.74778364256282,1.44194759003679,3.75262085100711));
#59505=CARTESIAN_POINT('Ctrl Pts',(2.0487087923059,2.11811516372279,3.80547466581002));
#59506=CARTESIAN_POINT('Ctrl Pts',(1.34963394204897,2.79428273740879,3.85832848061294));
#59507=CARTESIAN_POINT('Ctrl Pts',(0.282802396542619,3.09023471659314,3.91118229541586));
#59508=CARTESIAN_POINT('Ctrl Pts',(-0.664709435881276,2.87085021059064,
3.96403611021878));
#59509=CARTESIAN_POINT('Ctrl Pts',(-1.61222126830517,2.65146570458813,4.0168899250217));
#59510=CARTESIAN_POINT('Ctrl Pts',(-2.4404133876466,1.91674471339877,4.06974373982461));
#59511=CARTESIAN_POINT('Ctrl Pts',(-2.77116345090882,1.00213406940284,4.12259755462753));
#59512=CARTESIAN_POINT('Ctrl Pts',(-2.88636239880838,0.683578774547044,
4.14100633072184));
#59513=CARTESIAN_POINT('Ctrl Pts',(-2.94121657433896,0.343201038228005,
4.15941510681615));
#59514=CARTESIAN_POINT('Ctrl Pts',(-2.93894157525109,0.00211448818579894,
4.17782388291047));
#59515=CARTESIAN_POINT('Origin',(0.,0.,0.));
#59516=CARTESIAN_POINT('',(-2.93713130355353,-0.000163959391183133,5.32217611708959));
#59517=CARTESIAN_POINT('',(-2.93901369524072,-0.00214676294064878,5.17782388291046));
#59518=CARTESIAN_POINT('',(-2.942,-3.60291088309151E-16,0.));
#59519=CARTESIAN_POINT('Ctrl Pts',(-2.93713130355353,-0.000163959391183133,
5.32217611708959));
#59520=CARTESIAN_POINT('Ctrl Pts',(-2.93688283938904,0.501950620212298,
5.2951180623163));
#59521=CARTESIAN_POINT('Ctrl Pts',(-2.81488686979709,1.00417843559043,5.26806000754301));
#59522=CARTESIAN_POINT('Ctrl Pts',(-2.57182512474634,1.43868191764525,5.24100195276971));
#59523=CARTESIAN_POINT('Ctrl Pts',(-2.09527966925843,2.29056693856319,5.18795208663852));
#59524=CARTESIAN_POINT('Ctrl Pts',(-1.15336587844195,2.88212438019234,5.13490222050733));
#59525=CARTESIAN_POINT('Ctrl Pts',(-0.179052733645313,2.94143336674734,
5.08185235437614));
#59526=CARTESIAN_POINT('Ctrl Pts',(0.795260411151313,3.00074235330235,5.02880248824495));
#59527=CARTESIAN_POINT('Ctrl Pts',(1.80197290992809,2.52780288478322,4.97575262211376));
#59528=CARTESIAN_POINT('Ctrl Pts',(2.3783297957712,1.74001078013272,4.92270275598257));
#59529=CARTESIAN_POINT('Ctrl Pts',(2.95468668161432,0.952218675482221,4.86965288985138));
#59530=CARTESIAN_POINT('Ctrl Pts',(3.10068795452377,-0.150426065299655,
4.81660302372019));
#59531=CARTESIAN_POINT('Ctrl Pts',(2.74922129166827,-1.06107135569284,4.763553157589));
#59532=CARTESIAN_POINT('Ctrl Pts',(2.39775462881276,-1.97171664608602,4.7105032914578));
#59533=CARTESIAN_POINT('Ctrl Pts',(1.54882003019229,-2.69036248609052,4.65745342532661));
#59534=CARTESIAN_POINT('Ctrl Pts',(0.592646784285425,-2.88666934745533,
4.60440355919542));
#59535=CARTESIAN_POINT('Ctrl Pts',(-0.363526461621441,-3.08297620882014,
4.55135369306423));
#59536=CARTESIAN_POINT('Ctrl Pts',(-1.4269383548147,-2.75694409154526,4.49830382693304));
#59537=CARTESIAN_POINT('Ctrl Pts',(-2.10877094971039,-2.05843999525165,
4.44525396080185));
#59538=CARTESIAN_POINT('Ctrl Pts',(-2.63606405254913,-1.51825403899565,
4.40422801289776));
#59539=CARTESIAN_POINT('Ctrl Pts',(-2.93514778708967,-0.755305486812967,
4.36320206499368));
#59540=CARTESIAN_POINT('Ctrl Pts',(-2.94218751408198,0.00271333560157655,
4.32217611708959));
#59541=CARTESIAN_POINT('Ctrl Pts',(-2.93894157525109,0.00211448818579894,
4.17782388291047));
#59542=CARTESIAN_POINT('Ctrl Pts',(-2.93468477777351,-0.636099554887777,
4.21226892161907));
#59543=CARTESIAN_POINT('Ctrl Pts',(-2.73041348393046,-1.27679522001876,
4.24671396032768));
#59544=CARTESIAN_POINT('Ctrl Pts',(-2.34719296232994,-1.78165786895326,
4.28115899903628));
#59545=CARTESIAN_POINT('Ctrl Pts',(-1.7591644033058,-2.55633886651094,4.3340128138392));
#59546=CARTESIAN_POINT('Ctrl Pts',(-0.749799278074486,-3.01120056482378,
4.38686662864211));
#59547=CARTESIAN_POINT('Ctrl Pts',(0.220063078064465,-2.93856968720406,
4.43972044344503));
#59548=CARTESIAN_POINT('Ctrl Pts',(1.18992543420341,-2.86593880958434,4.49257425824795));
#59549=CARTESIAN_POINT('Ctrl Pts',(2.12028502125,-2.26581535603204,4.54542807305087));
#59550=CARTESIAN_POINT('Ctrl Pts',(2.58637355360725,-1.41219382731194,4.59828188785378));
#59551=CARTESIAN_POINT('Ctrl Pts',(3.05246208596449,-0.558572298591845,
4.6511357026567));
#59552=CARTESIAN_POINT('Ctrl Pts',(3.0542795636324,0.548547305296054,4.70398951745962));
#59553=CARTESIAN_POINT('Ctrl Pts',(2.59099619255503,1.4036945162104,4.75684333226253));
#59554=CARTESIAN_POINT('Ctrl Pts',(2.12771282147767,2.25884172712474,4.80969714706545));
#59555=CARTESIAN_POINT('Ctrl Pts',(1.19932860165501,2.86201654506552,4.86255096186837));
#59556=CARTESIAN_POINT('Ctrl Pts',(0.229709937944512,2.93783132755223,4.91540477667129));
#59557=CARTESIAN_POINT('Ctrl Pts',(-0.739908725765991,3.01364611003894,
4.9682585914742));
#59558=CARTESIAN_POINT('Ctrl Pts',(-1.75076183336435,2.56210085707158,5.02111240627712));
#59559=CARTESIAN_POINT('Ctrl Pts',(-2.34133069094863,1.78935467706368,5.07396622108004));
#59560=CARTESIAN_POINT('Ctrl Pts',(-2.72815297884642,1.28320633978488,5.10858544169018));
#59561=CARTESIAN_POINT('Ctrl Pts',(-2.93466310894815,0.639254998375354,
5.14320466230032));
#59562=CARTESIAN_POINT('Ctrl Pts',(-2.93901369524072,-0.00214676294064878,
5.17782388291046));
#59563=CARTESIAN_POINT('Origin',(0.,0.,0.));
#59564=CARTESIAN_POINT('',(-2.94279128603782,-0.00266058177182005,6.32217611708959));
#59565=CARTESIAN_POINT('',(-2.94660273288284,-0.000682925830890656,6.17782388291046));
#59566=CARTESIAN_POINT('',(-2.942,-3.60291088309151E-16,0.));
#59567=CARTESIAN_POINT('Ctrl Pts',(-2.94279128603782,-0.00266058177182005,
6.32217611708959));
#59568=CARTESIAN_POINT('Ctrl Pts',(-2.93556455204489,0.77464982053833,6.28008392577012));
#59569=CARTESIAN_POINT('Ctrl Pts',(-2.61900297877672,1.55716311141226,6.23799173445064));
#59570=CARTESIAN_POINT('Ctrl Pts',(-2.06697687324552,2.10040394636479,6.19589954313117));
#59571=CARTESIAN_POINT('Ctrl Pts',(-1.37124424252826,2.78506427569988,6.14284967699998));
#59572=CARTESIAN_POINT('Ctrl Pts',(-0.301494896051831,3.08965930485894,
6.08979981086878));
#59573=CARTESIAN_POINT('Ctrl Pts',(0.65054008701558,2.87417600846268,6.03674994473758));
#59574=CARTESIAN_POINT('Ctrl Pts',(1.60257507008298,2.65869271206642,5.98370007860639));
#59575=CARTESIAN_POINT('Ctrl Pts',(2.43689568974137,1.92313109011485,5.9306502124752));
#59576=CARTESIAN_POINT('Ctrl Pts',(2.76999025698787,1.00560633879706,5.87760034634401));
#59577=CARTESIAN_POINT('Ctrl Pts',(3.10308482423439,0.088081587479254,5.82455048021282));
#59578=CARTESIAN_POINT('Ctrl Pts',(2.93495333906901,-1.01140629320476,5.77150061408163));
#59579=CARTESIAN_POINT('Ctrl Pts',(2.34288070651628,-1.78745632882884,5.71845074795044));
#59580=CARTESIAN_POINT('Ctrl Pts',(1.75080807396356,-2.56350636445291,5.66540088181925));
#59581=CARTESIAN_POINT('Ctrl Pts',(0.734794294023496,-3.01611855501705,
5.61235101568806));
#59582=CARTESIAN_POINT('Ctrl Pts',(-0.238130151719265,-2.93724090998327,
5.55930114955686));
#59583=CARTESIAN_POINT('Ctrl Pts',(-1.21105459746203,-2.8583632649495,5.50625128342567));
#59584=CARTESIAN_POINT('Ctrl Pts',(-2.14088970900749,-2.24799578431781,
5.45320141729448));
#59585=CARTESIAN_POINT('Ctrl Pts',(-2.60021870470055,-1.38670574389861,
5.40015155116329));
#59586=CARTESIAN_POINT('Ctrl Pts',(-2.82526720110472,-0.96471621051031,
5.37415973980539));
#59587=CARTESIAN_POINT('Ctrl Pts',(-2.93736997679693,-0.482492328612542,
5.34816792844749));
#59588=CARTESIAN_POINT('Ctrl Pts',(-2.93713130355353,-0.000163959391183133,
5.32217611708959));
#59589=CARTESIAN_POINT('Ctrl Pts',(-2.93901369524072,-0.00214676294064878,
5.17782388291046));
#59590=CARTESIAN_POINT('Ctrl Pts',(-2.94130523081396,-0.339985126312179,
5.19605847710324));
#59591=CARTESIAN_POINT('Ctrl Pts',(-2.88751110036054,-0.677116152820267,
5.21429307129601));
#59592=CARTESIAN_POINT('Ctrl Pts',(-2.77443876694001,-0.993030257951712,
5.23252766548879));
#59593=CARTESIAN_POINT('Ctrl Pts',(-2.44669337777689,-1.90872190591076,
5.28538148029171));
#59594=CARTESIAN_POINT('Ctrl Pts',(-1.62091799188044,-2.64615809478042,
5.33823529509463));
#59595=CARTESIAN_POINT('Ctrl Pts',(-0.674131559565751,-2.86865233256197,
5.39108910989754));
#59596=CARTESIAN_POINT('Ctrl Pts',(0.272654872748948,-3.09114657034351,
5.44394292470046));
#59597=CARTESIAN_POINT('Ctrl Pts',(1.34045235148189,-2.79869885703692,5.49679673950337));
#59598=CARTESIAN_POINT('Ctrl Pts',(2.04174345790288,-2.1248301618769,5.54965055430629));
#59599=CARTESIAN_POINT('Ctrl Pts',(2.74303456432387,-1.45096146671689,5.60250436910921));
#59600=CARTESIAN_POINT('Ctrl Pts',(3.07781929843291,-0.395671789703455,
5.65535818391213));
#59601=CARTESIAN_POINT('Ctrl Pts',(2.8932471500414,0.559232056921528,5.70821199871505));
#59602=CARTESIAN_POINT('Ctrl Pts',(2.70867500164989,1.5141359035465,5.76106581351796));
#59603=CARTESIAN_POINT('Ctrl Pts',(2.00474597075782,2.36865391978304,5.81391962832088));
#59604=CARTESIAN_POINT('Ctrl Pts',(1.10284840201293,2.73264431766924,5.86677344312379));
#59605=CARTESIAN_POINT('Ctrl Pts',(0.200950833268036,3.09663471555545,5.91962725792671));
#59606=CARTESIAN_POINT('Ctrl Pts',(-0.898915273329681,2.97009749509133,
5.97248107272963));
#59607=CARTESIAN_POINT('Ctrl Pts',(-1.69459113213402,2.4108049401817,6.02533488753255));
#59608=CARTESIAN_POINT('Ctrl Pts',(-2.45979488521509,1.87293168771145,6.07616455265852));
#59609=CARTESIAN_POINT('Ctrl Pts',(-2.94366147355347,0.934814970161849,
6.12699421778449));
#59610=CARTESIAN_POINT('Ctrl Pts',(-2.94660273288284,-0.000682925830890656,
6.17782388291046));
#59611=CARTESIAN_POINT('Origin',(0.,0.,0.));
#59612=CARTESIAN_POINT('',(-2.94613349194407,0.00134377452219305,7.3221761170896));
#59613=CARTESIAN_POINT('',(-2.94097104012875,0.00263417315905663,7.17782388291047));
#59614=CARTESIAN_POINT('',(-2.942,-3.60291088309151E-16,0.));
#59615=CARTESIAN_POINT('Ctrl Pts',(-2.94613349194407,0.00134377452219305,
7.3221761170896));
#59616=CARTESIAN_POINT('Ctrl Pts',(-2.94655901031452,0.076401152092742,
7.31809965535512));
#59617=CARTESIAN_POINT('Ctrl Pts',(-2.94394049027812,0.151428352789515,
7.31402319362065));
#59618=CARTESIAN_POINT('Ctrl Pts',(-2.93818267368556,0.226213855655731,
7.30994673188618));
#59619=CARTESIAN_POINT('Ctrl Pts',(-2.86325215321475,1.19945024888809,7.25689686575499));
#59620=CARTESIAN_POINT('Ctrl Pts',(-2.25666138625707,2.13175354584505,7.2038469996238));
#59621=CARTESIAN_POINT('Ctrl Pts',(-1.39724160877638,2.5945724154744,7.15079713349261));
#59622=CARTESIAN_POINT('Ctrl Pts',(-0.537821831295674,3.05739128510375,
7.09774726736142));
#59623=CARTESIAN_POINT('Ctrl Pts',(0.574426956708044,3.05072572740549,7.04469740123023));
#59624=CARTESIAN_POINT('Ctrl Pts',(1.42823798173304,2.57763969552996,6.99164753509903));
#59625=CARTESIAN_POINT('Ctrl Pts',(2.28204900675803,2.10455366365443,6.93859766896784));
#59626=CARTESIAN_POINT('Ctrl Pts',(2.8774222688043,1.16504715760165,6.88554780283665));
#59627=CARTESIAN_POINT('Ctrl Pts',(2.94068287606827,0.190982603489069,6.83249793670546));
#59628=CARTESIAN_POINT('Ctrl Pts',(3.00394348333225,-0.783081950623512,
6.77944807057427));
#59629=CARTESIAN_POINT('Ctrl Pts',(2.53509143581391,-1.7917045527959,6.72639820444308));
#59630=CARTESIAN_POINT('Ctrl Pts',(1.74964368994405,-2.37125221996219,6.67334833831189));
#59631=CARTESIAN_POINT('Ctrl Pts',(0.964195944074186,-2.95079988712848,
6.62029847218069));
#59632=CARTESIAN_POINT('Ctrl Pts',(-0.137847500147206,-3.10127261928869,
6.5672486060495));
#59633=CARTESIAN_POINT('Ctrl Pts',(-1.04991095384295,-2.75350270045941,
6.51419873991831));
#59634=CARTESIAN_POINT('Ctrl Pts',(-1.96197440753872,-2.40573278163011,
6.46114887378712));
#59635=CARTESIAN_POINT('Ctrl Pts',(-2.68405787070882,-1.55972021181128,
6.40809900765593));
#59636=CARTESIAN_POINT('Ctrl Pts',(-2.88424164481483,-0.604351112146305,
6.35504914152473));
#59637=CARTESIAN_POINT('Ctrl Pts',(-2.92559045225217,-0.407015573289341,
6.34409146671302));
#59638=CARTESIAN_POINT('Ctrl Pts',(-2.94467258987502,-0.205014375890775,
6.33313379190131));
#59639=CARTESIAN_POINT('Ctrl Pts',(-2.94279128603782,-0.00266058177182005,
6.32217611708959));
#59640=CARTESIAN_POINT('Ctrl Pts',(-2.94660273288284,-0.000682925830890656,
6.17782388291046));
#59641=CARTESIAN_POINT('Ctrl Pts',(-2.94671986033404,-0.03793652093653,
6.1798480325874));
#59642=CARTESIAN_POINT('Ctrl Pts',(-2.94607433229542,-0.0751859630926007,
6.18187218226435));
#59643=CARTESIAN_POINT('Ctrl Pts',(-2.94465354469403,-0.11240581138343,
6.1838963319413));
#59644=CARTESIAN_POINT('Ctrl Pts',(-2.90755448743874,-1.08427611868375,
6.23675014674421));
#59645=CARTESIAN_POINT('Ctrl Pts',(-2.3418707619172,-2.03596884392924,6.28960396154713));
#59646=CARTESIAN_POINT('Ctrl Pts',(-1.50587294394191,-2.53297576802774,
6.34245777635005));
#59647=CARTESIAN_POINT('Ctrl Pts',(-0.66987512596661,-3.02998269212625,
6.39531159115297));
#59648=CARTESIAN_POINT('Ctrl Pts',(0.436436784462447,-3.07230381507775,
6.44816540595589));
#59649=CARTESIAN_POINT('Ctrl Pts',(1.30796108255195,-2.64061685430534,6.5010192207588));
#59650=CARTESIAN_POINT('Ctrl Pts',(2.17948538064144,-2.20892989353293,6.55387303556172));
#59651=CARTESIAN_POINT('Ctrl Pts',(2.81622206639138,-1.30323484903661,6.60672685036463));
#59652=CARTESIAN_POINT('Ctrl Pts',(2.9274603714869,-0.337039075013164,6.65958066516755));
#59653=CARTESIAN_POINT('Ctrl Pts',(3.03869867658241,0.629156699010298,6.71243447997047));
#59654=CARTESIAN_POINT('Ctrl Pts',(2.62443860102348,1.65585320256089,6.76528829477339));
#59655=CARTESIAN_POINT('Ctrl Pts',(1.87381619985943,2.27429822447636,6.81814210957631));
#59656=CARTESIAN_POINT('Ctrl Pts',(1.12319379869538,2.89274324639182,6.87099592437922));
#59657=CARTESIAN_POINT('Ctrl Pts',(0.0362090719262038,3.10293678667218,
6.92384973918214));
#59658=CARTESIAN_POINT('Ctrl Pts',(-0.890860363440002,2.80891213418353,
6.97670355398506));
#59659=CARTESIAN_POINT('Ctrl Pts',(-1.81792979880623,2.51488748169487,7.02955736878797));
#59660=CARTESIAN_POINT('Ctrl Pts',(-2.58508394276949,1.7166446364372,7.08241118359089));
#59661=CARTESIAN_POINT('Ctrl Pts',(-2.84206816794824,0.778632193944778,
7.13526499839381));
#59662=CARTESIAN_POINT('Ctrl Pts',(-2.91104434310083,0.526863780986117,
7.1494512932327));
#59663=CARTESIAN_POINT('Ctrl Pts',(-2.943266897151,0.265026097713286,7.16363758807158));
#59664=CARTESIAN_POINT('Ctrl Pts',(-2.94097104012875,0.00263417315905663,
7.17782388291047));
#59665=CARTESIAN_POINT('Origin',(0.,0.,0.));
#59666=CARTESIAN_POINT('',(-2.93863545697552,0.00202987236895366,8.3221761170896));
#59667=CARTESIAN_POINT('',(-2.93764652921007,-0.00116347631119334,8.17782388291046));
#59668=CARTESIAN_POINT('',(-2.942,-3.60291088309151E-16,0.));
#59669=CARTESIAN_POINT('Ctrl Pts',(-2.93863545697552,0.00202987236895366,
8.3221761170896));
#59670=CARTESIAN_POINT('Ctrl Pts',(-2.9408741470766,0.356210246758157,8.30306551880894));
#59671=CARTESIAN_POINT('Ctrl Pts',(-2.88168510873734,0.709667537581135,
8.28395492052829));
#59672=CARTESIAN_POINT('Ctrl Pts',(-2.75773880406503,1.0387332771172,8.26484432224763));
#59673=CARTESIAN_POINT('Ctrl Pts',(-2.41367135134812,1.9521998873394,8.21179445611644));
#59674=CARTESIAN_POINT('Ctrl Pts',(-1.57059473032904,2.67770909277114,8.15874458998524));
#59675=CARTESIAN_POINT('Ctrl Pts',(-0.616045496221141,2.88176648585937,
8.10569472385405));
#59676=CARTESIAN_POINT('Ctrl Pts',(0.338503737886761,3.08582387894761,8.05264485772286));
#59677=CARTESIAN_POINT('Ctrl Pts',(1.40452558508349,2.76842945969235,7.99959499159167));
#59678=CARTESIAN_POINT('Ctrl Pts',(2.09200238369389,2.07547974190444,7.94654512546048));
#59679=CARTESIAN_POINT('Ctrl Pts',(2.77947918230429,1.38253002411653,7.89349525932929));
#59680=CARTESIAN_POINT('Ctrl Pts',(3.08841093232836,0.314025007795969,7.8404453931981));
#59681=CARTESIAN_POINT('Ctrl Pts',(2.87679115035106,-0.638876208430471,
7.78739552706691));
#59682=CARTESIAN_POINT('Ctrl Pts',(2.66517136837375,-1.59177742465692,7.73434566093571));
#59683=CARTESIAN_POINT('Ctrl Pts',(1.93300005439505,-2.42907484078926,7.68129579480452));
#59684=CARTESIAN_POINT('Ctrl Pts',(1.01683398364893,-2.76588842546718,7.62824592867333));
#59685=CARTESIAN_POINT('Ctrl Pts',(0.100667912902824,-3.10270201014509,
7.57519606254214));
#59686=CARTESIAN_POINT('Ctrl Pts',(-0.999492914610703,-2.93903176336861,
7.52214619641095));
#59687=CARTESIAN_POINT('Ctrl Pts',(-1.7779381913755,-2.35011189522649,7.46909633027976));
#59688=CARTESIAN_POINT('Ctrl Pts',(-2.49656611864381,-1.80644585112258,
7.42012292588304));
#59689=CARTESIAN_POINT('Ctrl Pts',(-2.94102144022082,-0.900373338050325,
7.37114952148632));
#59690=CARTESIAN_POINT('Ctrl Pts',(-2.94613349194407,0.00134377452219305,
7.3221761170896));
#59691=CARTESIAN_POINT('Ctrl Pts',(-2.94097104012875,0.00263417315905663,
7.17782388291047));
#59692=CARTESIAN_POINT('Ctrl Pts',(-2.93471323298103,-0.712566314094985,
7.2164914028745));
#59693=CARTESIAN_POINT('Ctrl Pts',(-2.67200379227269,-1.43188449036145,
7.25515892283853));
#59694=CARTESIAN_POINT('Ctrl Pts',(-2.19810644885855,-1.9626379197902,7.29382644280256));
#59695=CARTESIAN_POINT('Ctrl Pts',(-1.55034619819585,-2.68811355130562,
7.34668025760548));
#59696=CARTESIAN_POINT('Ctrl Pts',(-0.50801139047619,-3.0612827746093,7.39953407240839));
#59697=CARTESIAN_POINT('Ctrl Pts',(0.453005883307361,-2.91177012045952,
7.45238788721131));
#59698=CARTESIAN_POINT('Ctrl Pts',(1.41402315709093,-2.76225746630973,7.50524170201423));
#59699=CARTESIAN_POINT('Ctrl Pts',(2.2937228969384,-2.09006293470645,7.55809551681715));
#59700=CARTESIAN_POINT('Ctrl Pts',(2.69046625749842,-1.20208605431325,7.61094933162007));
#59701=CARTESIAN_POINT('Ctrl Pts',(3.08720961805843,-0.31410917392004,7.66380314642299));
#59702=CARTESIAN_POINT('Ctrl Pts',(3.000996599331,0.789650055263082,7.7166569612259));
#59703=CARTESIAN_POINT('Ctrl Pts',(2.47118892410342,1.60525538968118,7.76951077602881));
#59704=CARTESIAN_POINT('Ctrl Pts',(1.94138124887585,2.42086072409927,7.82236459083173));
#59705=CARTESIAN_POINT('Ctrl Pts',(0.967978917148135,2.94831216375233,7.87521840563465));
#59706=CARTESIAN_POINT('Ctrl Pts',(-0.00459803675616453,2.94679460138808,
7.92807222043756));
#59707=CARTESIAN_POINT('Ctrl Pts',(-0.977174990660472,2.94527703902382,
7.98092603524048));
#59708=CARTESIAN_POINT('Ctrl Pts',(-1.94892656674138,2.41479047464224,8.0337798500434));
#59709=CARTESIAN_POINT('Ctrl Pts',(-2.47618640555083,1.59753574284808,8.08663366484632));
#59710=CARTESIAN_POINT('Ctrl Pts',(-2.77941863111983,1.12752465355612,8.11703040420104));
#59711=CARTESIAN_POINT('Ctrl Pts',(-2.935634717328,0.562664672081437,8.14742714355575));
#59712=CARTESIAN_POINT('Ctrl Pts',(-2.93764652921007,-0.00116347631119334,
8.17782388291046));
#59713=CARTESIAN_POINT('Origin',(0.,0.,0.));
#59714=CARTESIAN_POINT('',(-2.93871642317227,-0.00207197768594736,9.3221761170896));
#59715=CARTESIAN_POINT('',(-2.94520105889964,-0.0018935710546995,9.17782388291047));
#59716=CARTESIAN_POINT('',(-2.942,-3.60291088309151E-16,0.));
#59717=CARTESIAN_POINT('Ctrl Pts',(-2.93871642317227,-0.00207197768594736,
9.3221761170896));
#59718=CARTESIAN_POINT('Ctrl Pts',(-2.93462655422571,0.63069516315242,9.28803138226276));
#59719=CARTESIAN_POINT('Ctrl Pts',(-2.73431821504367,1.26582298942305,9.25388664743592));
#59720=CARTESIAN_POINT('Ctrl Pts',(-2.35730441600429,1.76839080033892,9.21974191260908));
#59721=CARTESIAN_POINT('Ctrl Pts',(-1.77154700215763,2.54921850997377,9.16669204647789));
#59722=CARTESIAN_POINT('Ctrl Pts',(-0.759238489877945,3.01005825656821,
9.11364218034669));
#59723=CARTESIAN_POINT('Ctrl Pts',(0.214293837547277,2.93907609354129,9.0605923142155));
#59724=CARTESIAN_POINT('Ctrl Pts',(1.18782616497251,2.86809393051436,9.0075424480843));
#59725=CARTESIAN_POINT('Ctrl Pts',(2.12258230754328,2.26528985786606,8.95449258195312));
#59726=CARTESIAN_POINT('Ctrl Pts',(2.58888343604653,1.40775448392131,8.90144271582193));
#59727=CARTESIAN_POINT('Ctrl Pts',(3.05518456454977,0.550219109976561,8.84839284969073));
#59728=CARTESIAN_POINT('Ctrl Pts',(3.05303067898551,-0.562047565264635,
8.79534298355954));
#59729=CARTESIAN_POINT('Ctrl Pts',(2.58341185471709,-1.41777054608419,8.74229311742835));
#59730=CARTESIAN_POINT('Ctrl Pts',(2.11379303044867,-2.27349352690374,8.68924325129716));
#59731=CARTESIAN_POINT('Ctrl Pts',(1.17670926747611,-2.87267281330165,8.63619338516597));
#59732=CARTESIAN_POINT('Ctrl Pts',(0.202909330970668,-2.93988400040574,
8.58314351903477));
#59733=CARTESIAN_POINT('Ctrl Pts',(-0.770890605534777,-3.00709518750983,
8.53009365290358));
#59734=CARTESIAN_POINT('Ctrl Pts',(-1.7814067155731,-2.54233827532011,8.47704378677239));
#59735=CARTESIAN_POINT('Ctrl Pts',(-2.3641356283849,-1.75924781171891,8.4239939206412));
#59736=CARTESIAN_POINT('Ctrl Pts',(-2.73694321676338,-1.25825659470745,
8.39005465279067));
#59737=CARTESIAN_POINT('Ctrl Pts',(-2.93465967862159,-0.626973072346038,
8.35611538494013));
#59738=CARTESIAN_POINT('Ctrl Pts',(-2.93863545697552,0.00202987236895366,
8.3221761170896));
#59739=CARTESIAN_POINT('Ctrl Pts',(-2.93764652921007,-0.00116347631119334,
8.17782388291046));
#59740=CARTESIAN_POINT('Ctrl Pts',(-2.93913285347321,-0.417719052240401,
8.20028095835866));
#59741=CARTESIAN_POINT('Ctrl Pts',(-2.85645082861081,-0.833711429208547,
8.22273803380687));
#59742=CARTESIAN_POINT('Ctrl Pts',(-2.68670181103504,-1.21047632909238,
8.24519510925507));
#59743=CARTESIAN_POINT('Ctrl Pts',(-2.28718927617178,-2.09721077003196,
8.29804892405799));
#59744=CARTESIAN_POINT('Ctrl Pts',(-1.40539610490722,-2.7666567527044,8.35090273886091));
#59745=CARTESIAN_POINT('Ctrl Pts',(-0.443916927094085,-2.91316963573206,
8.40375655366382));
#59746=CARTESIAN_POINT('Ctrl Pts',(0.517562250719054,-3.05968251875972,
8.45661036846674));
#59747=CARTESIAN_POINT('Ctrl Pts',(1.55872743508076,-2.68326230214263,8.50946418326965));
#59748=CARTESIAN_POINT('Ctrl Pts',(2.20422054240271,-1.95576874020468,8.56231799807257));
#59749=CARTESIAN_POINT('Ctrl Pts',(2.84971364972467,-1.22827517826673,8.61517181287549));
#59750=CARTESIAN_POINT('Ctrl Pts',(3.09953468000683,-0.149708271007917,
8.66802562767841));
#59751=CARTESIAN_POINT('Ctrl Pts',(2.8396244541884,0.787497634210531,8.72087944248132));
#59752=CARTESIAN_POINT('Ctrl Pts',(2.57971422836996,1.72470353942896,8.77373325728424));
#59753=CARTESIAN_POINT('Ctrl Pts',(1.81007274645093,2.52054844260704,8.82658707208716));
#59754=CARTESIAN_POINT('Ctrl Pts',(0.882090263685985,2.8116785611841,8.87944088689007));
#59755=CARTESIAN_POINT('Ctrl Pts',(-0.0458922190789657,3.10280867976116,
8.93229470169299));
#59756=CARTESIAN_POINT('Ctrl Pts',(-1.13221570268984,2.88922401373721,8.98514851649591));
#59757=CARTESIAN_POINT('Ctrl Pts',(-1.88090446966924,2.26843953868958,9.03800233129883));
#59758=CARTESIAN_POINT('Ctrl Pts',(-2.54110799810967,1.72102368459441,9.08460951516938));
#59759=CARTESIAN_POINT('Ctrl Pts',(-2.93876870791001,0.856971595110357,
9.13121669903992));
#59760=CARTESIAN_POINT('Ctrl Pts',(-2.94520105889964,-0.0018935710546995,
9.17782388291047));
#59761=CARTESIAN_POINT('Origin',(0.,0.,0.));
#59762=CARTESIAN_POINT('',(-2.94620168531707,-0.00128244101107317,10.3221761170896));
#59763=CARTESIAN_POINT('',(-2.94330664216,0.0025268841526987,10.1778238829105));
#59764=CARTESIAN_POINT('',(-2.942,-3.60291088309151E-16,0.));
#59765=CARTESIAN_POINT('Ctrl Pts',(-2.94620168531707,-0.00128244101107317,
10.3221761170896));
#59766=CARTESIAN_POINT('Ctrl Pts',(-2.94126630412904,0.904162302447864,
10.2729972457166));
#59767=CARTESIAN_POINT('Ctrl Pts',(-2.49257491833407,1.81383213622128,10.2238183743435));
#59768=CARTESIAN_POINT('Ctrl Pts',(-1.76882298743563,2.35698013813353,10.1746395029705));
#59769=CARTESIAN_POINT('Ctrl Pts',(-0.988102690804116,2.9428807085698,10.1215896368393));
#59770=CARTESIAN_POINT('Ctrl Pts',(0.112683772548088,3.10228885822241,10.0685397707081));
#59771=CARTESIAN_POINT('Ctrl Pts',(1.02753850943148,2.76192953278536,10.0154899045769));
#59772=CARTESIAN_POINT('Ctrl Pts',(1.94239324631488,2.42157020734831,9.96244003844575));
#59773=CARTESIAN_POINT('Ctrl Pts',(2.67131625672946,1.58144340682159,9.90939017231457));
#59774=CARTESIAN_POINT('Ctrl Pts',(2.87924391130981,0.627729744095369,9.85634030618337));
#59775=CARTESIAN_POINT('Ctrl Pts',(3.08717156589015,-0.325983918630861,
9.80329044005218));
#59776=CARTESIAN_POINT('Ctrl Pts',(2.77410386463627,-1.39328444355657,9.75024057392098));
#59777=CARTESIAN_POINT('Ctrl Pts',(2.08394846133389,-2.08356639993563,9.69719070778979));
#59778=CARTESIAN_POINT('Ctrl Pts',(1.39379305803153,-2.77384835631469,9.6441408416586));
#59779=CARTESIAN_POINT('Ctrl Pts',(0.326549952680647,-3.08711174414709,
9.59109097552742));
#59780=CARTESIAN_POINT('Ctrl Pts',(-0.627201817996116,-2.87935895850778,
9.53804110939623));
#59781=CARTESIAN_POINT('Ctrl Pts',(-1.58095358867288,-2.67160617286848,
9.48499124326504));
#59782=CARTESIAN_POINT('Ctrl Pts',(-2.42121402467556,-1.94283721375749,
9.43194137713383));
#59783=CARTESIAN_POINT('Ctrl Pts',(-2.76174108497008,-1.02804489786436,
9.37889151100264));
#59784=CARTESIAN_POINT('Ctrl Pts',(-2.88309311197862,-0.702044662436785,
9.35998637969829));
#59785=CARTESIAN_POINT('Ctrl Pts',(-2.94098088678121,-0.35242016294182,
9.34108124839394));
#59786=CARTESIAN_POINT('Ctrl Pts',(-2.93871642317227,-0.00207197768594736,
9.3221761170896));
#59787=CARTESIAN_POINT('Ctrl Pts',(-2.94520105889964,-0.0018935710546995,
9.17782388291047));
#59788=CARTESIAN_POINT('Ctrl Pts',(-2.94606316897201,-0.117004875110373,
9.18407051384284));
#59789=CARTESIAN_POINT('Ctrl Pts',(-2.93989752914462,-0.232023004939246,
9.19031714477521));
#59790=CARTESIAN_POINT('Ctrl Pts',(-2.92639431994892,-0.346173148702556,
9.19656377570758));
#59791=CARTESIAN_POINT('Ctrl Pts',(-2.81214135290127,-1.3120170769757,9.2494175905105));
#59792=CARTESIAN_POINT('Ctrl Pts',(-2.17258136845806,-2.21572064945068,
9.30227140531341));
#59793=CARTESIAN_POINT('Ctrl Pts',(-1.29971415023778,-2.64468574548728,
9.35512522011633));
#59794=CARTESIAN_POINT('Ctrl Pts',(-0.426846932017496,-3.07365084152388,
9.40797903491925));
#59795=CARTESIAN_POINT('Ctrl Pts',(0.679327519979847,-3.02787746112211,
9.46083284972217));
#59796=CARTESIAN_POINT('Ctrl Pts',(1.51377025947196,-2.528264061812,9.51368666452509));
#59797=CARTESIAN_POINT('Ctrl Pts',(2.34821299896408,-2.02865066250189,9.566540479328));
#59798=CARTESIAN_POINT('Ctrl Pts',(2.91092402595096,-1.07519724428343,9.61939429413091));
#59799=CARTESIAN_POINT('Ctrl Pts',(2.9449899904472,-0.103215894501322,9.67224810893383));
#59800=CARTESIAN_POINT('Ctrl Pts',(2.97905595494345,0.868765455280781,9.72510192373675));
#59801=CARTESIAN_POINT('Ctrl Pts',(2.48447685694907,1.85927473662654,9.77795573853967));
#59802=CARTESIAN_POINT('Ctrl Pts',(1.68705949036834,2.41608150538637,9.83080955334259));
#59803=CARTESIAN_POINT('Ctrl Pts',(0.889642123787608,2.97288827414619,9.8836633681455));
#59804=CARTESIAN_POINT('Ctrl Pts',(-0.210613511379468,3.09599253032006,
9.93651718294842));
#59805=CARTESIAN_POINT('Ctrl Pts',(-1.11137078493627,2.72918935640275,9.98937099775133));
#59806=CARTESIAN_POINT('Ctrl Pts',(-2.01212805849309,2.36238618248543,10.0422248125543));
#59807=CARTESIAN_POINT('Ctrl Pts',(-2.71338697043961,1.50567557847691,10.0950786273572));
#59808=CARTESIAN_POINT('Ctrl Pts',(-2.89497825514053,0.550200388018259,
10.1479324421601));
#59809=CARTESIAN_POINT('Ctrl Pts',(-2.9292111996477,0.370077596184809,10.1578962557436));
#59810=CARTESIAN_POINT('Ctrl Pts',(-2.94497596099191,0.186444863810624,
10.167860069327));
#59811=CARTESIAN_POINT('Ctrl Pts',(-2.94330664216,0.0025268841526987,10.1778238829105));
#59812=CARTESIAN_POINT('Origin',(0.,0.,0.));
#59813=CARTESIAN_POINT('',(-2.94267506677377,0.0026741096853234,11.3221761170896));
#59814=CARTESIAN_POINT('',(-2.93720511247626,7.6518416280307E-5,11.1778238829105));
#59815=CARTESIAN_POINT('',(-2.942,-3.60291088309151E-16,0.));
#59816=CARTESIAN_POINT('Ctrl Pts',(-2.94267506677377,0.0026741096853234,
11.3221761170896));
#59817=CARTESIAN_POINT('Ctrl Pts',(-2.94459362275203,0.208843135527949,
11.3110129753016));
#59818=CARTESIAN_POINT('Ctrl Pts',(-2.92478181403725,0.414645989663669,
11.2998498335136));
#59819=CARTESIAN_POINT('Ctrl Pts',(-2.88187939068302,0.615517107798873,
11.2886866917255));
#59820=CARTESIAN_POINT('Ctrl Pts',(-2.67799701967457,1.57010374022251,11.2356368255943));
#59821=CARTESIAN_POINT('Ctrl Pts',(-1.95264240634497,2.41331337073947,11.1825869594632));
#59822=CARTESIAN_POINT('Ctrl Pts',(-1.0392388969828,2.75754830373552,11.129537093332));
#59823=CARTESIAN_POINT('Ctrl Pts',(-0.125835387620612,3.10178323673157,
11.0764872272008));
#59824=CARTESIAN_POINT('Ctrl Pts',(0.97561701777415,2.94704347220669,11.0234373610696));
#59825=CARTESIAN_POINT('Ctrl Pts',(1.75881431280863,2.3644581505064,10.9703874949384));
#59826=CARTESIAN_POINT('Ctrl Pts',(2.5420116078431,1.78187282880611,10.9173376288072));
#59827=CARTESIAN_POINT('Ctrl Pts',(3.0069537925173,0.771441949930418,10.864287762676));
#59828=CARTESIAN_POINT('Ctrl Pts',(2.93992115485034,-0.202370293521759,
10.8112378965448));
#59829=CARTESIAN_POINT('Ctrl Pts',(2.87288851718338,-1.17618253697395,10.7581880304136));
#59830=CARTESIAN_POINT('Ctrl Pts',(2.27388105717527,-2.11337614500262,10.7051381642824));
#59831=CARTESIAN_POINT('Ctrl Pts',(1.41824419635842,-2.58315186002146,10.6520882981512));
#59832=CARTESIAN_POINT('Ctrl Pts',(0.562607335541579,-3.05292757504029,
10.59903843202));
#59833=CARTESIAN_POINT('Ctrl Pts',(-0.549658926083981,-3.05528539704932,
10.5459885658889));
#59834=CARTESIAN_POINT('Ctrl Pts',(-1.40727978292664,-2.58914150733454,
10.4929386997577));
#59835=CARTESIAN_POINT('Ctrl Pts',(-2.26490063976931,-2.12299761761977,
10.4398888336265));
#59836=CARTESIAN_POINT('Ctrl Pts',(-2.86787609182906,-1.18835201618118,
10.3868389674953));
#59837=CARTESIAN_POINT('Ctrl Pts',(-2.93903675290352,-0.214832719851918,
10.3337891013641));
#59838=CARTESIAN_POINT('Ctrl Pts',(-2.9442292739426,-0.143796007266396,
10.3299181066059));
#59839=CARTESIAN_POINT('Ctrl Pts',(-2.94659016179437,-0.0725523127645525,
10.3260471118478));
#59840=CARTESIAN_POINT('Ctrl Pts',(-2.94620168531707,-0.00128244101107317,
10.3221761170896));
#59841=CARTESIAN_POINT('Ctrl Pts',(-2.94330664216,0.0025268841526987,10.1778238829105));
#59842=CARTESIAN_POINT('Ctrl Pts',(-2.93612093097255,-0.789162192096626,
10.2207138841299));
#59843=CARTESIAN_POINT('Ctrl Pts',(-2.60589249191516,-1.58613672417313,
10.2636038853494));
#59844=CARTESIAN_POINT('Ctrl Pts',(-2.0351025661624,-2.13119147659499,10.3064938865688));
#59845=CARTESIAN_POINT('Ctrl Pts',(-1.33171193502808,-2.80286837384081,
10.3593477013718));
#59846=CARTESIAN_POINT('Ctrl Pts',(-0.263007015304154,-3.09198239142367,
10.4122015161747));
#59847=CARTESIAN_POINT('Ctrl Pts',(0.68308046979022,-2.86653460410006,10.4650553309776));
#59848=CARTESIAN_POINT('Ctrl Pts',(1.62916795488458,-2.64108681677646,10.5179091457805));
#59849=CARTESIAN_POINT('Ctrl Pts',(2.4526380053494,-1.90107722454637,10.5707629605834));
#59850=CARTESIAN_POINT('Ctrl Pts',(2.77752420302081,-0.984367241605259,
10.6236167753863));
#59851=CARTESIAN_POINT('Ctrl Pts',(3.10241040069222,-0.0676572586641361,
10.6764705901893));
#59852=CARTESIAN_POINT('Ctrl Pts',(2.92871274557025,1.02575311498802,10.7293244049922));
#59853=CARTESIAN_POINT('Ctrl Pts',(2.33573525751911,1.79665254612406,10.7821782197951));
#59854=CARTESIAN_POINT('Ctrl Pts',(1.74275776946797,2.5675519772601,10.835032034598));
#59855=CARTESIAN_POINT('Ctrl Pts',(0.730500448487692,3.01594046588001,10.8878858494009));
#59856=CARTESIAN_POINT('Ctrl Pts',(-0.23887689886381,2.93710016715487,10.9407396642038));
#59857=CARTESIAN_POINT('Ctrl Pts',(-1.20825424621531,2.85825986842973,10.9935934790068));
#59858=CARTESIAN_POINT('Ctrl Pts',(-2.13475161993805,2.2521907823595,11.0464472938097));
#59859=CARTESIAN_POINT('Ctrl Pts',(-2.5953640803379,1.3956019687589,11.0993011086126));
#59860=CARTESIAN_POINT('Ctrl Pts',(-2.82346851267095,0.971402187234134,
11.1254753667119));
#59861=CARTESIAN_POINT('Ctrl Pts',(-2.93731807226522,0.48576427202227,11.1516496248112));
#59862=CARTESIAN_POINT('Ctrl Pts',(-2.93720511247626,7.6518416280307E-5,
11.1778238829105));
#59863=CARTESIAN_POINT('Origin',(0.,0.,0.));
#59864=CARTESIAN_POINT('',(-2.93712622074894,0.000100805557199934,12.3221761170896));
#59865=CARTESIAN_POINT('',(-2.9430272628276,-0.00257481030056199,12.1778238829105));
#59866=CARTESIAN_POINT('',(-2.942,-3.60291088309151E-16,0.));
#59867=CARTESIAN_POINT('Ctrl Pts',(-2.93712622074894,0.000100805557199934,
12.3221761170896));
#59868=CARTESIAN_POINT('Ctrl Pts',(-2.93727410781314,0.486244108806712,
12.2959788387554));
#59869=CARTESIAN_POINT('Ctrl Pts',(-2.82330164211032,0.972322158399294,
12.2697815604212));
#59870=CARTESIAN_POINT('Ctrl Pts',(-2.59482855910859,1.3967658648718,12.243584282087));
#59871=CARTESIAN_POINT('Ctrl Pts',(-2.13216727371862,2.2562704867391,12.1905344159558));
#59872=CARTESIAN_POINT('Ctrl Pts',(-1.19997521215115,2.8630321833101,12.1374845498246));
#59873=CARTESIAN_POINT('Ctrl Pts',(-0.226752573949602,2.93814114750192,
12.0844346836934));
#59874=CARTESIAN_POINT('Ctrl Pts',(0.74647006425197,3.01325011169373,12.0313848175622));
#59875=CARTESIAN_POINT('Ctrl Pts',(1.76072327908759,2.55670634350636,11.978334951431));
#59876=CARTESIAN_POINT('Ctrl Pts',(2.349785866942,1.77836905954762,11.9252850852998));
#59877=CARTESIAN_POINT('Ctrl Pts',(2.93884845479638,1.00003177558891,11.8722352191686));
#59878=CARTESIAN_POINT('Ctrl Pts',(3.10272041566954,-0.100099024141179,
11.8191853530375));
#59879=CARTESIAN_POINT('Ctrl Pts',(2.76607481766758,-1.01632683498072,11.7661354869063));
#59880=CARTESIAN_POINT('Ctrl Pts',(2.4294292196656,-1.93255464582029,11.7130856207751));
#59881=CARTESIAN_POINT('Ctrl Pts',(1.59226606278853,-2.66487946776933,11.6600357546439));
#59882=CARTESIAN_POINT('Ctrl Pts',(0.639403663520396,-2.87667396267171,
11.6069858885127));
#59883=CARTESIAN_POINT('Ctrl Pts',(-0.313458735747721,-3.08846845757408,
11.5539360223815));
#59884=CARTESIAN_POINT('Ctrl Pts',(-1.38202037740687,-2.77973262542978,
11.5008861562503));
#59885=CARTESIAN_POINT('Ctrl Pts',(-2.07509613389281,-2.09238289219248,
11.4478362901191));
#59886=CARTESIAN_POINT('Ctrl Pts',(-2.62232980813185,-1.54967032940742,
11.4059495657759));
#59887=CARTESIAN_POINT('Ctrl Pts',(-2.93547619508296,-0.770920396015258,
11.3640628414328));
#59888=CARTESIAN_POINT('Ctrl Pts',(-2.94267506677377,0.0026741096853234,
11.3221761170896));
#59889=CARTESIAN_POINT('Ctrl Pts',(-2.93720511247626,7.6518416280307E-5,
11.1778238829105));
#59890=CARTESIAN_POINT('Ctrl Pts',(-2.93708997197894,-0.494987521734636,
11.2045034396141));
#59891=CARTESIAN_POINT('Ctrl Pts',(-2.81856970692698,-0.990103343131662,
11.2311829963177));
#59892=CARTESIAN_POINT('Ctrl Pts',(-2.58195393144776,-1.42025823729116,
11.2578625530213));
#59893=CARTESIAN_POINT('Ctrl Pts',(-2.11320377508074,-2.27242108860962,
11.3107163678243));
#59894=CARTESIAN_POINT('Ctrl Pts',(-1.18097591526968,-2.86963825011554,
11.3635701826272));
#59895=CARTESIAN_POINT('Ctrl Pts',(-0.210891622840258,-2.93924212819014,
11.4164239974301));
#59896=CARTESIAN_POINT('Ctrl Pts',(0.75919266958915,-3.00884600626475,11.469277812233));
#59897=CARTESIAN_POINT('Ctrl Pts',(1.76713339463694,-2.55083660090805,11.5221316270359));
#59898=CARTESIAN_POINT('Ctrl Pts',(2.35274154615311,-1.77432431694913,11.5749854418389));
#59899=CARTESIAN_POINT('Ctrl Pts',(2.93834969766929,-0.997812032990198,
11.6278392566418));
#59900=CARTESIAN_POINT('Ctrl Pts',(3.10162527565385,0.0972031295709437,
11.6806930714447));
#59901=CARTESIAN_POINT('Ctrl Pts',(2.76802260088771,1.01077714936912,11.7335468862476));
#59902=CARTESIAN_POINT('Ctrl Pts',(2.43441992612157,1.92435116916729,11.7864007010505));
#59903=CARTESIAN_POINT('Ctrl Pts',(1.60393899860469,2.65648404620246,11.8392545158534));
#59904=CARTESIAN_POINT('Ctrl Pts',(0.655747147489709,2.87291058741323,11.8921083306564));
#59905=CARTESIAN_POINT('Ctrl Pts',(-0.292444703625262,3.08933712862399,
11.9449621454593));
#59906=CARTESIAN_POINT('Ctrl Pts',(-1.35834747833835,2.79005733401037,11.9978159602622));
#59907=CARTESIAN_POINT('Ctrl Pts',(-2.05530881073343,2.11171145217178,12.0506697750651));
#59908=CARTESIAN_POINT('Ctrl Pts',(-2.61421830322617,1.56773012217451,12.0930544776802));
#59909=CARTESIAN_POINT('Ctrl Pts',(-2.93586860501076,0.779978635821696,
12.1354391802953));
#59910=CARTESIAN_POINT('Ctrl Pts',(-2.9430272628276,-0.00257481030056199,
12.1778238829105));
#59911=CARTESIAN_POINT('Origin',(0.,0.,0.));
#59912=CARTESIAN_POINT('',(-2.94230384945163,-0.00270653131051041,13.3221761170896));
#59913=CARTESIAN_POINT('',(-2.94542263194624,0.00177224128177641,13.1778238829105));
#59914=CARTESIAN_POINT('',(-2.942,-3.60291088309151E-16,0.));
#59915=CARTESIAN_POINT('Ctrl Pts',(-2.94230384945163,-0.00270653131051041,
13.3221761170896));
#59916=CARTESIAN_POINT('Ctrl Pts',(-2.9352201389254,0.75903152900975,13.2809447022092));
#59917=CARTESIAN_POINT('Ctrl Pts',(-2.63281541581416,1.52575687849258,13.2397132873288));
#59918=CARTESIAN_POINT('Ctrl Pts',(-2.10078289570291,2.06659172493232,13.1984818724484));
#59919=CARTESIAN_POINT('Ctrl Pts',(-1.41625014194664,2.7624498778951,13.1454320063172));
#59920=CARTESIAN_POINT('Ctrl Pts',(-0.351583517635692,3.08436100717369,
13.0923821401861));
#59921=CARTESIAN_POINT('Ctrl Pts',(0.603822270094866,2.88435240540648,13.0393322740549));
#59922=CARTESIAN_POINT('Ctrl Pts',(1.55922805782544,2.68434380363926,12.9862824079237));
#59923=CARTESIAN_POINT('Ctrl Pts',(2.40537300897562,1.96241547082624,12.9332325417925));
#59924=CARTESIAN_POINT('Ctrl Pts',(2.75331015075007,1.05041579682204,12.8801826756613));
#59925=CARTESIAN_POINT('Ctrl Pts',(3.10124729252453,0.138416122817822,12.8271328095301));
#59926=CARTESIAN_POINT('Ctrl Pts',(2.95097662492324,-0.963654892377583,
12.7740829433989));
#59927=CARTESIAN_POINT('Ctrl Pts',(2.37157298102772,-1.7492088863529,12.7210330772677));
#59928=CARTESIAN_POINT('Ctrl Pts',(1.7921693371322,-2.53476288032821,12.6679832111365));
#59929=CARTESIAN_POINT('Ctrl Pts',(0.783632716942436,-3.00379985308343,
12.6149333450053));
#59930=CARTESIAN_POINT('Ctrl Pts',(-0.190443419765153,-2.94071784370837,
12.5618834788741));
#59931=CARTESIAN_POINT('Ctrl Pts',(-1.16451955647273,-2.87763583433331,
12.5088336127429));
#59932=CARTESIAN_POINT('Ctrl Pts',(-2.10413520969813,-2.28243484282798,
12.4557837466118));
#59933=CARTESIAN_POINT('Ctrl Pts',(-2.57737778170459,-1.42871057349352,
12.4027338804806));
#59934=CARTESIAN_POINT('Ctrl Pts',(-2.8169219811687,-0.996575535866305,
12.3758812926836));
#59935=CARTESIAN_POINT('Ctrl Pts',(-2.93697463437708,-0.498203085629071,
12.3490287048866));
#59936=CARTESIAN_POINT('Ctrl Pts',(-2.93712622074894,0.000100805557199934,
12.3221761170896));
#59937=CARTESIAN_POINT('Ctrl Pts',(-2.9430272628276,-0.00257481030056199,
12.1778238829105));
#59938=CARTESIAN_POINT('Ctrl Pts',(-2.94479546661752,-0.195867185023464,
12.1882929950983));
#59939=CARTESIAN_POINT('Ctrl Pts',(-2.92737651745624,-0.388842427018477,
12.1987621072861));
#59940=CARTESIAN_POINT('Ctrl Pts',(-2.88960655205276,-0.577748681561196,
12.2092312194739));
#59941=CARTESIAN_POINT('Ctrl Pts',(-2.69892307089993,-1.53145096439204,
12.2620850342768));
#59942=CARTESIAN_POINT('Ctrl Pts',(-1.98953621851721,-2.38144356099016,
12.3149388490797));
#59943=CARTESIAN_POINT('Ctrl Pts',(-1.08532618196459,-2.73965082509689,
12.3677926638826));
#59944=CARTESIAN_POINT('Ctrl Pts',(-0.181116145411983,-3.09785808920362,
12.4206464786855));
#59945=CARTESIAN_POINT('Ctrl Pts',(0.917917075310514,-2.96428002081899,
12.4735002934884));
#59946=CARTESIAN_POINT('Ctrl Pts',(1.70999495989744,-2.39990349844265,12.5263541082914));
#59947=CARTESIAN_POINT('Ctrl Pts',(2.50207284448437,-1.83552697606631,12.5792079230943));
#59948=CARTESIAN_POINT('Ctrl Pts',(2.98719539293572,-0.840351999698262,
12.6320617378972));
#59949=CARTESIAN_POINT('Ctrl Pts',(2.94387332727614,0.131260800180532,12.6849155527001));
#59950=CARTESIAN_POINT('Ctrl Pts',(2.90055126161656,1.10287360005931,12.737769367503));
#59951=CARTESIAN_POINT('Ctrl Pts',(2.32878458184608,2.05092422344884,12.7906231823059));
#59952=CARTESIAN_POINT('Ctrl Pts',(1.48962111902714,2.54256730224792,12.8434769971089));
#59953=CARTESIAN_POINT('Ctrl Pts',(0.650457656208199,3.034210381047,12.8963308119118));
#59954=CARTESIAN_POINT('Ctrl Pts',(-0.456102589659198,3.06944591525562,
12.9491846267147));
#59955=CARTESIAN_POINT('Ctrl Pts',(-1.32484453286982,2.63218664392115,13.0020384415176));
#59956=CARTESIAN_POINT('Ctrl Pts',(-2.19358647608043,2.19492737258668,13.0548922563205));
#59957=CARTESIAN_POINT('Ctrl Pts',(-2.82451011663427,1.28517329570913,13.1077460711235));
#59958=CARTESIAN_POINT('Ctrl Pts',(-2.92955871082826,0.318284973761263,
13.1605998859264));
#59959=CARTESIAN_POINT('Ctrl Pts',(-2.94096978668171,0.213255143821896,
13.1663412182544));
#59960=CARTESIAN_POINT('Ctrl Pts',(-2.94617567004577,0.107551144246887,
13.1720825505824));
#59961=CARTESIAN_POINT('Ctrl Pts',(-2.94542263194624,0.00177224128177641,
13.1778238829105));
#59962=CARTESIAN_POINT('Origin',(0.,0.,0.));
#59963=CARTESIAN_POINT('',(-2.94640032942472,0.00108073188550471,14.3221761170896));
#59964=CARTESIAN_POINT('',(-2.93776462225576,0.00129977310561086,14.1778238829105));
#59965=CARTESIAN_POINT('',(-2.942,-3.60291088309151E-16,0.));
#59966=CARTESIAN_POINT('Ctrl Pts',(-2.94640032942472,0.00108073188550471,
14.3221761170896));
#59967=CARTESIAN_POINT('Ctrl Pts',(-2.94667898956338,0.0602749409108862,
14.3189604317942));
#59968=CARTESIAN_POINT('Ctrl Pts',(-2.94505040817207,0.119453520431582,
14.3157447464988));
#59969=CARTESIAN_POINT('Ctrl Pts',(-2.94146614700694,0.178513412517928,
14.3125290612034));
#59970=CARTESIAN_POINT('Ctrl Pts',(-2.88233580385349,1.15283741536734,14.2594791950723));
#59971=CARTESIAN_POINT('Ctrl Pts',(-2.29095107408328,2.09485965367689,14.2064293289411));
#59972=CARTESIAN_POINT('Ctrl Pts',(-1.43915344311655,2.57156129610056,14.1533794628099));
#59973=CARTESIAN_POINT('Ctrl Pts',(-0.587355812149814,3.04826293852424,
14.1003295966787));
#59974=CARTESIAN_POINT('Ctrl Pts',(0.524854720013437,3.05964398506203,14.0472797305475));
#59975=CARTESIAN_POINT('Ctrl Pts',(1.3862289649121,2.60047291646642,13.9942298644163));
#59976=CARTESIAN_POINT('Ctrl Pts',(2.24760320981075,2.14130184787082,13.9411799982851));
#59977=CARTESIAN_POINT('Ctrl Pts',(2.85814116744481,1.21157866414187,13.8881301321539));
#59978=CARTESIAN_POINT('Ctrl Pts',(2.93719719893692,0.238668697138423,13.8350802660227));
#59979=CARTESIAN_POINT('Ctrl Pts',(3.01625323042904,-0.734241269865052,
13.7820303998915));
#59980=CARTESIAN_POINT('Ctrl Pts',(2.56382733577916,-1.75033802014301,13.7289805337603));
#59981=CARTESIAN_POINT('Ctrl Pts',(1.78788587098706,-2.3425529331824,13.6759306676291));
#59982=CARTESIAN_POINT('Ctrl Pts',(1.01194440619497,-2.93476784622179,13.622880801498));
#59983=CARTESIAN_POINT('Ctrl Pts',(-0.0875126287393881,-3.10310092202263,
13.5698309353668));
#59984=CARTESIAN_POINT('Ctrl Pts',(-1.00509843823799,-2.77017459050656,
13.5167810692356));
#59985=CARTESIAN_POINT('Ctrl Pts',(-1.92268424773658,-2.43724825899049,
13.4637312031044));
#59986=CARTESIAN_POINT('Ctrl Pts',(-2.65839883179945,-1.60306252015755,
13.4106813369732));
#59987=CARTESIAN_POINT('Ctrl Pts',(-2.87405668223012,-0.65106706241757,
13.357631470842));
#59988=CARTESIAN_POINT('Ctrl Pts',(-2.92210094658066,-0.438981477122014,
13.3458130195912));
#59989=CARTESIAN_POINT('Ctrl Pts',(-2.94433430336091,-0.221048884050304,
13.3339945683404));
#59990=CARTESIAN_POINT('Ctrl Pts',(-2.94230384945163,-0.00270653131051041,
13.3221761170896));
#59991=CARTESIAN_POINT('Ctrl Pts',(-2.94542263194624,0.00177224128177641,
13.1778238829105));
#59992=CARTESIAN_POINT('Ctrl Pts',(-2.93924331811451,-0.866233027778004,
13.2249363653854));
#59993=CARTESIAN_POINT('Ctrl Pts',(-2.53181472316137,-1.73928198328602,
13.2720488478602));
#59994=CARTESIAN_POINT('Ctrl Pts',(-1.85921337766286,-2.28625133811473,
13.3191613303351));
#59995=CARTESIAN_POINT('Ctrl Pts',(-1.10464590246936,-2.89987676102466,
13.372015145138));
#59996=CARTESIAN_POINT('Ctrl Pts',(-0.0163374042482181,-3.10310503982634,
13.4248689599409));
#59997=CARTESIAN_POINT('Ctrl Pts',(0.908830114185135,-2.80314954796603,
13.4777227747439));
#59998=CARTESIAN_POINT('Ctrl Pts',(1.83399763261852,-2.50319405610571,13.5305765895468));
#59999=CARTESIAN_POINT('Ctrl Pts',(2.59602417126411,-1.70005479358336,13.5834304043497));
#60000=CARTESIAN_POINT('Ctrl Pts',(2.84699618048077,-0.760415881633083,
13.6362842191526));
#60001=CARTESIAN_POINT('Ctrl Pts',(3.09796818969742,0.179223030317163,13.6891380339556));
#60002=CARTESIAN_POINT('Ctrl Pts',(2.8378856694852,1.2553615916953,13.7419918487585));
#60003=CARTESIAN_POINT('Ctrl Pts',(2.18549282128288,1.97667414938146,13.7948456635614));
#60004=CARTESIAN_POINT('Ctrl Pts',(1.53309997308057,2.69798670706761,13.8476994783643));
#60005=CARTESIAN_POINT('Ctrl Pts',(0.488396796888163,3.06447326106177,13.9005532931672));
#60006=CARTESIAN_POINT('Ctrl Pts',(-0.47164330555891,2.90880940541545,13.9534071079701));
#60007=CARTESIAN_POINT('Ctrl Pts',(-1.43168340800602,2.75314554976913,14.006260922773));
#60008=CARTESIAN_POINT('Ctrl Pts',(-2.30706043670781,2.07533128448227,14.059114737576));
#60009=CARTESIAN_POINT('Ctrl Pts',(-2.69810913870436,1.18483190383781,14.1119685523789));
#60010=CARTESIAN_POINT('Ctrl Pts',(-2.86052341047112,0.814980763359175,
14.1339203292228));
#60011=CARTESIAN_POINT('Ctrl Pts',(-2.93939151111869,0.408441644783018,
14.1558721060666));
#60012=CARTESIAN_POINT('Ctrl Pts',(-2.93776462225576,0.00129977310561086,
14.1778238829105));
#60013=CARTESIAN_POINT('Origin',(0.,0.,0.));
#60014=CARTESIAN_POINT('',(-2.93898631063874,0.00219869534614975,15.3221761170896));
#60015=CARTESIAN_POINT('',(-2.94070302830747,-0.00260312230465348,15.1778238829105));
#60016=CARTESIAN_POINT('',(-2.942,-3.60291088309151E-16,0.));
#60017=CARTESIAN_POINT('Ctrl Pts',(-2.93898631063874,0.00219869534614975,
15.3221761170896));
#60018=CARTESIAN_POINT('Ctrl Pts',(-2.9413195721644,0.340324726473414,15.303926295248));
#60019=CARTESIAN_POINT('Ctrl Pts',(-2.88747827444888,0.677730458314348,
15.2856764734065));
#60020=CARTESIAN_POINT('Ctrl Pts',(-2.7742287838461,0.993853503951382,15.2674266515649));
#60021=CARTESIAN_POINT('Ctrl Pts',(-2.44502719667123,1.91278221446787,15.2143767854337));
#60022=CARTESIAN_POINT('Ctrl Pts',(-1.61383260128749,2.65187445545,15.1613269193025));
#60023=CARTESIAN_POINT('Ctrl Pts',(-0.662719748881298,2.87139211304889,
15.1082770531713));
#60024=CARTESIAN_POINT('Ctrl Pts',(0.288393103524908,3.09090977064778,15.0552271870401));
#60025=CARTESIAN_POINT('Ctrl Pts',(1.35942421295354,2.79085284486343,15.0021773209089));
#60026=CARTESIAN_POINT('Ctrl Pts',(2.05805331298264,2.10914833365457,14.9491274547778));
#60027=CARTESIAN_POINT('Ctrl Pts',(2.75668241301172,1.42744382244573,14.8960775886466));
#60028=CARTESIAN_POINT('Ctrl Pts',(3.08290950364125,0.364091725812366,14.8430277225154));
#60029=CARTESIAN_POINT('Ctrl Pts',(2.88677796198798,-0.592117497307048,
14.7899778563842));
#60030=CARTESIAN_POINT('Ctrl Pts',(2.69064642033471,-1.54832672042648,14.736927990253));
#60031=CARTESIAN_POINT('Ctrl Pts',(1.97215624639864,-2.39739307003199,14.6838781241218));
#60032=CARTESIAN_POINT('Ctrl Pts',(1.06157541348122,-2.74902669574685,14.6308282579906));
#60033=CARTESIAN_POINT('Ctrl Pts',(0.150994580563778,-3.10066032146171,
14.5777783918594));
#60034=CARTESIAN_POINT('Ctrl Pts',(-0.951676911334983,-2.95486122328588,
14.5247285257282));
#60035=CARTESIAN_POINT('Ctrl Pts',(-1.73957467901604,-2.37864879050332,
14.471678659597));
#60036=CARTESIAN_POINT('Ctrl Pts',(-2.47971301862363,-1.83736420923569,
14.4218444787612));
#60037=CARTESIAN_POINT('Ctrl Pts',(-2.94208187209259,-0.916264917963124,
14.3720102979254));
#60038=CARTESIAN_POINT('Ctrl Pts',(-2.94640032942472,0.00108073188550471,
14.3221761170896));
#60039=CARTESIAN_POINT('Ctrl Pts',(-2.93776462225576,0.00129977310561086,
14.1778238829105));
#60040=CARTESIAN_POINT('Ctrl Pts',(-2.93547441213952,-0.571843515603255,
14.2087259208695));
#60041=CARTESIAN_POINT('Ctrl Pts',(-2.77366839213467,-1.14618127181492,
14.2396279588286));
#60042=CARTESIAN_POINT('Ctrl Pts',(-2.46085834215274,-1.62104774284077,
14.2705299967876));
#60043=CARTESIAN_POINT('Ctrl Pts',(-1.92583846831326,-2.4332435128729,14.3233838115905));
#60044=CARTESIAN_POINT('Ctrl Pts',(-0.949078345342955,-2.95445055693513,
14.3762376263935));
#60045=CARTESIAN_POINT('Ctrl Pts',(0.0234689473096315,-2.94670473125899,
14.4290914411964));
#60046=CARTESIAN_POINT('Ctrl Pts',(0.996016239962246,-2.93895890558285,
14.4819452559993));
#60047=CARTESIAN_POINT('Ctrl Pts',(1.96435070229714,-2.40226021016833,14.5347990708022));
#60048=CARTESIAN_POINT('Ctrl Pts',(2.48636610448465,-1.58164571228254,14.5876528856051));
#60049=CARTESIAN_POINT('Ctrl Pts',(3.00838150667215,-0.761031214396772,
14.6405067004081));
#60050=CARTESIAN_POINT('Ctrl Pts',(3.08407784871226,0.343499085960264,14.693360515211));
#60051=CARTESIAN_POINT('Ctrl Pts',(2.67889493917015,1.22765690223306,14.7462143300139));
#60052=CARTESIAN_POINT('Ctrl Pts',(2.27371202962803,2.11181471850586,14.7990681448168));
#60053=CARTESIAN_POINT('Ctrl Pts',(1.3876498685037,2.77560005069443,14.8519219596197));
#60054=CARTESIAN_POINT('Ctrl Pts',(0.425252150859725,2.91595270416053,14.9047757744226));
#60055=CARTESIAN_POINT('Ctrl Pts',(-0.53714556678425,3.05630535762663,14.9576295892256));
#60056=CARTESIAN_POINT('Ctrl Pts',(-1.57587884094787,2.67322533237025,15.0104834040285));
#60057=CARTESIAN_POINT('Ctrl Pts',(-2.21669990962147,1.94161300865957,15.0633372188314));
#60058=CARTESIAN_POINT('Ctrl Pts',(-2.6793941459007,1.41336445080168,15.1014994401911));
#60059=CARTESIAN_POINT('Ctrl Pts',(-2.93464390538761,0.703414755606144,
15.1396616615508));
#60060=CARTESIAN_POINT('Ctrl Pts',(-2.94070302830747,-0.00260312230465348,
15.1778238829105));
#60061=CARTESIAN_POINT('Origin',(0.,0.,0.));
#60062=CARTESIAN_POINT('',(-2.9383894490365,-0.00188841566858416,16.3221761170896));
#60063=CARTESIAN_POINT('',(-2.94668624203375,0.000515437224130946,16.1778238829105));
#60064=CARTESIAN_POINT('',(-2.942,-3.60291088309151E-16,0.));
#60065=CARTESIAN_POINT('Ctrl Pts',(-2.9383894490365,-0.00188841566858416,
16.3221761170896));
#60066=CARTESIAN_POINT('Ctrl Pts',(-2.93478084744062,0.615099093327396,
16.2888921587018));
#60067=CARTESIAN_POINT('Ctrl Pts',(-2.74519813105489,1.23411540322869,16.2556082003141));
#60068=CARTESIAN_POINT('Ctrl Pts',(-2.38568546251023,1.72991184931602,16.2223242419263));
#60069=CARTESIAN_POINT('Ctrl Pts',(-1.81267372164173,2.52014042690405,16.1692743757951));
#60070=CARTESIAN_POINT('Ctrl Pts',(-0.807975369726903,2.99734375645525,
16.116224509664));
#60071=CARTESIAN_POINT('Ctrl Pts',(0.166580468072483,2.94216605243372,16.0631746435328));
#60072=CARTESIAN_POINT('Ctrl Pts',(1.14113630587187,2.88698834841218,16.0101247774016));
#60073=CARTESIAN_POINT('Ctrl Pts',(2.08554962955581,2.29942961081791,15.9570749112704));
#60074=CARTESIAN_POINT('Ctrl Pts',(2.5657024989119,1.44957263340403,15.9040250451392));
#60075=CARTESIAN_POINT('Ctrl Pts',(3.04585536826799,0.599715655990127,15.850975179008));
#60076=CARTESIAN_POINT('Ctrl Pts',(3.06174778329622,-0.512439561243392,
15.7979253128768));
#60077=CARTESIAN_POINT('Ctrl Pts',(2.60607448653775,-1.375669256418,15.7448754467456));
#60078=CARTESIAN_POINT('Ctrl Pts',(2.15040118977928,-2.23889895159261,15.6918255806144));
#60079=CARTESIAN_POINT('Ctrl Pts',(1.22316218123412,-2.8532031247083,15.6387757144832));
#60080=CARTESIAN_POINT('Ctrl Pts',(0.250580893354547,-2.93620492273994,
15.585725848352));
#60081=CARTESIAN_POINT('Ctrl Pts',(-0.722000394525,-3.01920672077158,15.5326759822209));
#60082=CARTESIAN_POINT('Ctrl Pts',(-1.73992396173896,-2.57090614371921,
15.4796261160897));
#60083=CARTESIAN_POINT('Ctrl Pts',(-2.33528145586295,-1.79737326516761,
15.4265762499585));
#60084=CARTESIAN_POINT('Ctrl Pts',(-2.72582847651777,-1.28994543553831,
15.3917762056688));
#60085=CARTESIAN_POINT('Ctrl Pts',(-2.93453708340038,-0.642563810329421,
15.3569761613792));
#60086=CARTESIAN_POINT('Ctrl Pts',(-2.93898631063874,0.00219869534614975,
15.3221761170896));
#60087=CARTESIAN_POINT('Ctrl Pts',(-2.94070302830747,-0.00260312230465348,
15.1778238829105));
#60088=CARTESIAN_POINT('Ctrl Pts',(-2.94303565380434,-0.274404061986468,
15.1925154763537));
#60089=CARTESIAN_POINT('Ctrl Pts',(-2.90843633003559,-0.54562227641632,
15.2072070697969));
#60090=CARTESIAN_POINT('Ctrl Pts',(-2.8345231637324,-0.805666183339214,
15.2218986632402));
#60091=CARTESIAN_POINT('Ctrl Pts',(-2.56861648598613,-1.74118842946232,
15.2747524780431));
#60092=CARTESIAN_POINT('Ctrl Pts',(-1.79389426731002,-2.53208829954357,
15.327606292846));
#60093=CARTESIAN_POINT('Ctrl Pts',(-0.864066442222231,-2.81726973293956,
15.3804601076489));
#60094=CARTESIAN_POINT('Ctrl Pts',(0.0657613828655833,-3.10245116633556,
15.4333139224518));
#60095=CARTESIAN_POINT('Ctrl Pts',(1.15069481436507,-2.88191416304626,15.4861677372547));
#60096=CARTESIAN_POINT('Ctrl Pts',(1.89539278194,-2.25634788250431,15.5390215520576));
#60097=CARTESIAN_POINT('Ctrl Pts',(2.64009074951493,-1.63078160196237,15.5918753668606));
#60098=CARTESIAN_POINT('Ctrl Pts',(3.0445532531653,-0.600186044167799,15.6447291816635));
#60099=CARTESIAN_POINT('Ctrl Pts',(2.92411745215616,0.364906413629165,15.6975829964664));
#60100=CARTESIAN_POINT('Ctrl Pts',(2.80368165114701,1.32999887142613,15.7504368112693));
#60101=CARTESIAN_POINT('Ctrl Pts',(2.15834754547832,2.22958822922551,15.8032906260722));
#60102=CARTESIAN_POINT('Ctrl Pts',(1.28275117211377,2.6529547668878,15.8561444408751));
#60103=CARTESIAN_POINT('Ctrl Pts',(0.407154798749216,3.07632130455008,15.9089982556781));
#60104=CARTESIAN_POINT('Ctrl Pts',(-0.698703842311192,3.0234650220753,15.961852070481));
#60105=CARTESIAN_POINT('Ctrl Pts',(-1.52992999255096,2.51851817198227,16.0147058852839));
#60106=CARTESIAN_POINT('Ctrl Pts',(-2.36115614279074,2.01357132188925,16.0675597000868));
#60107=CARTESIAN_POINT('Ctrl Pts',(-2.91774980220986,1.05653390417798,16.1204135148897));
#60108=CARTESIAN_POINT('Ctrl Pts',(-2.94559058794027,0.0843543297622131,
16.1732673296926));
#60109=CARTESIAN_POINT('Ctrl Pts',(-2.94639064385726,0.0564169709381923,
16.1747861807653));
#60110=CARTESIAN_POINT('Ctrl Pts',(-2.94675405280721,0.0284671076397201,
16.1763050318379));
#60111=CARTESIAN_POINT('Ctrl Pts',(-2.94668624203375,0.000515437224130946,
16.1778238829105));
#60112=CARTESIAN_POINT('Origin',(0.,0.,0.));
#60113=CARTESIAN_POINT('',(-2.9458984904506,-0.00153267693865478,17.3221761170896));
#60114=CARTESIAN_POINT('',(-2.93922953893335,0.0022355800204151,17.1778238829105));
#60115=CARTESIAN_POINT('',(-2.942,-3.60291088309151E-16,0.));
#60116=CARTESIAN_POINT('Ctrl Pts',(-2.9458984904506,-0.00153267693865478,
17.3221761170896));
#60117=CARTESIAN_POINT('Ctrl Pts',(-2.94027455109819,0.888306186912937,
17.2738580221557));
#60118=CARTESIAN_POINT('Ctrl Pts',(-2.50916352361795,1.78286348468974,17.2255399272217));
#60119=CARTESIAN_POINT('Ctrl Pts',(-1.80683108598698,2.32797155462599,17.1772218322878));
#60120=CARTESIAN_POINT('Ctrl Pts',(-1.03571952111964,2.92646183402729,17.1241719661566));
#60121=CARTESIAN_POINT('Ctrl Pts',(0.0623357253435999,3.10370875724391,
17.0711221000254));
#60122=CARTESIAN_POINT('Ctrl Pts',(0.982592217141216,2.77823733097987,17.0180722338942));
#60123=CARTESIAN_POINT('Ctrl Pts',(1.90284870893879,2.45276590471584,16.965022367763));
#60124=CARTESIAN_POINT('Ctrl Pts',(2.64530644607076,1.6245761289712,16.9119725016318));
#60125=CARTESIAN_POINT('Ctrl Pts',(2.86868029896989,0.674361531182407,16.8589226355006));
#60126=CARTESIAN_POINT('Ctrl Pts',(3.09205415186903,-0.275853066606427,
16.8058727693694));
#60127=CARTESIAN_POINT('Ctrl Pts',(2.79634412053529,-1.34809248643939,16.7528229032383));
#60128=CARTESIAN_POINT('Ctrl Pts',(2.1174790684053,-2.04948103853197,16.6997730371071));
#60129=CARTESIAN_POINT('Ctrl Pts',(1.43861401627531,-2.75086959062454,16.6467231709759));
#60130=CARTESIAN_POINT('Ctrl Pts',(0.376593943349051,-3.08140727497672,
16.5936733048447));
#60131=CARTESIAN_POINT('Ctrl Pts',(-0.580402982021727,-2.88915602051826,
16.5406234387135));
#60132=CARTESIAN_POINT('Ctrl Pts',(-1.53739990739248,-2.69690476605982,
16.4875735725823));
#60133=CARTESIAN_POINT('Ctrl Pts',(-2.3893736852078,-1.98186457279075,16.4345237064511));
#60134=CARTESIAN_POINT('Ctrl Pts',(-2.74469800920436,-1.07271756334381,
16.3814738403199));
#60135=CARTESIAN_POINT('Ctrl Pts',(-2.8770886883768,-0.733977483029354,
16.3617079325765));
#60136=CARTESIAN_POINT('Ctrl Pts',(-2.94053244192803,-0.368290693895058,
16.341942024833));
#60137=CARTESIAN_POINT('Ctrl Pts',(-2.9383894490365,-0.00188841566858416,
16.3221761170896));
#60138=CARTESIAN_POINT('Ctrl Pts',(-2.94668624203375,0.000515437224130946,
16.1778238829105));
#60139=CARTESIAN_POINT('Ctrl Pts',(-2.94439433622497,-0.944210489409022,
16.2291588466408));
#60140=CARTESIAN_POINT('Ctrl Pts',(-2.44950204050612,-1.8910007617774,16.2804938103711));
#60141=CARTESIAN_POINT('Ctrl Pts',(-1.67155253041584,-2.426835738729,16.3318287741014));
#60142=CARTESIAN_POINT('Ctrl Pts',(-0.8705857751193,-2.97852450168421,16.3846825889043));
#60143=CARTESIAN_POINT('Ctrl Pts',(0.230435647515488,-3.09458029647436,
16.4375364037072));
#60144=CARTESIAN_POINT('Ctrl Pts',(1.12882547663905,-2.72201627621926,16.4903902185102));
#60145=CARTESIAN_POINT('Ctrl Pts',(2.0272153057626,-2.34945225596416,16.5432440333131));
#60146=CARTESIAN_POINT('Ctrl Pts',(2.72297354137494,-1.48826842066384,16.596097848116));
#60147=CARTESIAN_POINT('Ctrl Pts',(2.89844232621279,-0.531649928364628,
16.6489516629189));
#60148=CARTESIAN_POINT('Ctrl Pts',(3.07391111105065,0.424968563934609,16.7018054777218));
#60149=CARTESIAN_POINT('Ctrl Pts',(2.72909044511397,1.4770217132327,16.7546592925247));
#60150=CARTESIAN_POINT('Ctrl Pts',(2.02141287935942,2.14418038790392,16.8075131073277));
#60151=CARTESIAN_POINT('Ctrl Pts',(1.31373531360488,2.81133906257512,16.8603669221306));
#60152=CARTESIAN_POINT('Ctrl Pts',(0.243200848032404,3.09360326261943,16.9132207369335));
#60153=CARTESIAN_POINT('Ctrl Pts',(-0.701423490172106,2.86210143987712,
16.9660745517364));
#60154=CARTESIAN_POINT('Ctrl Pts',(-1.6460478283766,2.63059961713482,17.0189283665393));
#60155=CARTESIAN_POINT('Ctrl Pts',(-2.46476203921317,1.88533177160598,17.0717821813422));
#60156=CARTESIAN_POINT('Ctrl Pts',(-2.78377104759162,0.966560044333808,
17.1246359961452));
#60157=CARTESIAN_POINT('Ctrl Pts',(-2.89077950149426,0.658367048391136,
17.1423652917336));
#60158=CARTESIAN_POINT('Ctrl Pts',(-2.94156105341168,0.330651370465482,
17.160094587322));
#60159=CARTESIAN_POINT('Ctrl Pts',(-2.93922953893335,0.0022355800204151,
17.1778238829105));
#60160=CARTESIAN_POINT('Origin',(0.,0.,0.));
#60161=CARTESIAN_POINT('',(-2.94316033587002,0.00260673739485059,18.3221761170896));
#60162=CARTESIAN_POINT('',(-2.93873926947604,-0.00201622880601424,18.1778238829105));
#60163=CARTESIAN_POINT('',(-2.942,-3.60291088309151E-16,0.));
#60164=CARTESIAN_POINT('Ctrl Pts',(-2.94316033587002,0.00260673739485059,
18.3221761170896));
#60165=CARTESIAN_POINT('Ctrl Pts',(-2.94491668517285,0.192797687418137,
18.3118737517407));
#60166=CARTESIAN_POINT('Ctrl Pts',(-2.92806785825349,0.382678731558034,
18.3015713863917));
#60167=CARTESIAN_POINT('Ctrl Pts',(-2.89148654186959,0.56867891698542,18.2912690210428));
#60168=CARTESIAN_POINT('Ctrl Pts',(-2.70311873784196,1.52644779850943,18.2382191549116));
#60169=CARTESIAN_POINT('Ctrl Pts',(-1.99154029026522,2.38131498645116,18.1851692887804));
#60170=CARTESIAN_POINT('Ctrl Pts',(-1.08384206308078,2.74032416234529,18.1321194226492));
#60171=CARTESIAN_POINT('Ctrl Pts',(-0.176143835896361,3.09933333823942,
18.0790695565181));
#60172=CARTESIAN_POINT('Ctrl Pts',(0.927674170895802,2.96248450208593,18.0260196903868));
#60173=CARTESIAN_POINT('Ctrl Pts',(1.72022055624172,2.39268288126949,17.9729698242556));
#60174=CARTESIAN_POINT('Ctrl Pts',(2.51276694158766,1.82288126045303,17.9199199581245));
#60175=CARTESIAN_POINT('Ctrl Pts',(2.99404170548737,0.820126854973603,17.8668700919933));
#60176=CARTESIAN_POINT('Ctrl Pts',(2.9428175484727,-0.154644782769381,17.8138202258621));
#60177=CARTESIAN_POINT('Ctrl Pts',(2.89159339145802,-1.12941642051234,17.7607703597309));
#60178=CARTESIAN_POINT('Ctrl Pts',(2.30787031352896,-2.07620529051882,17.7077204935997));
#60179=CARTESIAN_POINT('Ctrl Pts',(1.45996797292217,-2.55980148653722,17.6546706274685));
#60180=CARTESIAN_POINT('Ctrl Pts',(0.612065632315374,-3.04339768255563,
17.6016207613373));
#60181=CARTESIAN_POINT('Ctrl Pts',(-0.500015970969152,-3.06380120458596,
17.5485708952061));
#60182=CARTESIAN_POINT('Ctrl Pts',(-1.36508691313533,-2.61163317715626,
17.4955210290749));
#60183=CARTESIAN_POINT('Ctrl Pts',(-2.23015785530151,-2.15946514972656,
17.4424711629438));
#60184=CARTESIAN_POINT('Ctrl Pts',(-2.84821813634935,-1.23472557283683,
17.3894212968126));
#60185=CARTESIAN_POINT('Ctrl Pts',(-2.93516433523754,-0.262488966599004,
17.3363714306814));
#60186=CARTESIAN_POINT('Ctrl Pts',(-2.94291948241534,-0.175770535322769,
17.3316396594841));
#60187=CARTESIAN_POINT('Ctrl Pts',(-2.94644924052216,-0.0886742315037942,
17.3269078882868));
#60188=CARTESIAN_POINT('Ctrl Pts',(-2.9458984904506,-0.00153267693865478,
17.3221761170896));
#60189=CARTESIAN_POINT('Ctrl Pts',(-2.93922953893335,0.0022355800204151,
17.1778238829105));
#60190=CARTESIAN_POINT('Ctrl Pts',(-2.9346104425522,-0.648407683513794,
17.212948402125));
#60191=CARTESIAN_POINT('Ctrl Pts',(-2.72152344667222,-1.30179887700645,
17.2480729213394));
#60192=CARTESIAN_POINT('Ctrl Pts',(-2.32418176308124,-1.81157354166827,
17.2831974405539));
#60193=CARTESIAN_POINT('Ctrl Pts',(-1.72627966427209,-2.5786597913827,17.3360512553568));
#60194=CARTESIAN_POINT('Ctrl Pts',(-0.711171660733521,-3.02055668179605,
17.3889050701597));
#60195=CARTESIAN_POINT('Ctrl Pts',(0.257680923198029,-2.9355101952696,17.4417588849627));
#60196=CARTESIAN_POINT('Ctrl Pts',(1.22653350712957,-2.85046370874314,17.4946126997656));
#60197=CARTESIAN_POINT('Ctrl Pts',(2.14913067145408,-2.23847384527686,17.5474665145685));
#60198=CARTESIAN_POINT('Ctrl Pts',(2.60424816996682,-1.37895287589402,17.6003203293714));
#60199=CARTESIAN_POINT('Ctrl Pts',(3.05936566847955,-0.519431906511194,
17.6531741441743));
#60200=CARTESIAN_POINT('Ctrl Pts',(3.04700350118055,0.587620168788174,17.7060279589772));
#60201=CARTESIAN_POINT('Ctrl Pts',(2.57280578318673,1.43676371290232,17.7588817737802));
#60202=CARTESIAN_POINT('Ctrl Pts',(2.09860806519289,2.28590725701647,17.8117355885831));
#60203=CARTESIAN_POINT('Ctrl Pts',(1.16257479650419,2.87714226994538,17.864589403386));
#60204=CARTESIAN_POINT('Ctrl Pts',(0.192064658972456,2.94053238912373,17.9174432181889));
#60205=CARTESIAN_POINT('Ctrl Pts',(-0.778445478559264,3.00392250830208,
17.9702970329918));
#60206=CARTESIAN_POINT('Ctrl Pts',(-1.78343248493401,2.5394677337299,18.0231508477947));
#60207=CARTESIAN_POINT('Ctrl Pts',(-2.36405591431578,1.75922119095369,18.0760046625977));
#60208=CARTESIAN_POINT('Ctrl Pts',(-2.73689954660888,1.25819084947647,18.1099444027019));
#60209=CARTESIAN_POINT('Ctrl Pts',(-2.93475752332708,0.626944267538864,
18.1438841428062));
#60210=CARTESIAN_POINT('Ctrl Pts',(-2.93873926947604,-0.00201622880601424,
18.1778238829105));
#60211=CARTESIAN_POINT('Origin',(0.,0.,0.));
#60212=CARTESIAN_POINT('',(-2.93716369210466,0.00036464873958586,19.3221761170896));
#60213=CARTESIAN_POINT('',(-2.94645753962907,-0.000902846911536883,19.1778238829105));
#60214=CARTESIAN_POINT('',(-2.942,-3.60291088309151E-16,0.));
#60215=CARTESIAN_POINT('Ctrl Pts',(-2.93716369210466,0.00036464873958586,
19.3221761170896));
#60216=CARTESIAN_POINT('Ctrl Pts',(-2.93768143739811,0.470519560834665,
19.2968396151945));
#60217=CARTESIAN_POINT('Ctrl Pts',(-2.83142571131797,0.940453511257854,
19.2715031132994));
#60218=CARTESIAN_POINT('Ctrl Pts',(-2.61714889686116,1.35448210918234,19.2461666114043));
#60219=CARTESIAN_POINT('Ctrl Pts',(-2.16849357857734,2.22138006476051,19.1931167452731));
#60220=CARTESIAN_POINT('Ctrl Pts',(-1.24626864868979,2.84318628438932,19.1400668791419));
#60221=CARTESIAN_POINT('Ctrl Pts',(-0.274392720940246,2.93407545355119,
19.0870170130107));
#60222=CARTESIAN_POINT('Ctrl Pts',(0.697483206809295,3.02496462271307,19.0339671468795));
#60223=CARTESIAN_POINT('Ctrl Pts',(1.71901013242084,2.58493674140802,18.9809172807483));
#60224=CARTESIAN_POINT('Ctrl Pts',(2.32062334974625,1.81625917782929,18.9278674146171));
#60225=CARTESIAN_POINT('Ctrl Pts',(2.92223656707166,1.04758161425057,18.8748175484859));
#60226=CARTESIAN_POINT('Ctrl Pts',(3.10393607611096,-0.0497456316017877,
18.8217676823547));
#60227=CARTESIAN_POINT('Ctrl Pts',(2.78220016595262,-0.971314763096829,
18.7687178162235));
#60228=CARTESIAN_POINT('Ctrl Pts',(2.46046425579428,-1.89288389459188,18.7156679500923));
#60229=CARTESIAN_POINT('Ctrl Pts',(1.63529292643825,-2.63869491172959,18.6626180839611));
#60230=CARTESIAN_POINT('Ctrl Pts',(0.685992217770817,-2.86592128461242,
18.6095682178299));
#60231=CARTESIAN_POINT('Ctrl Pts',(-0.263308490896586,-3.09314765749525,
18.5565183516988));
#60232=CARTESIAN_POINT('Ctrl Pts',(-1.3367385788754,-2.80178938612322,18.5034684855676));
#60233=CARTESIAN_POINT('Ctrl Pts',(-2.04087504262555,-2.12577496288408,
18.4504186194364));
#60234=CARTESIAN_POINT('Ctrl Pts',(-2.60826712539801,-1.58104357723327,
18.4076711186541));
#60235=CARTESIAN_POINT('Ctrl Pts',(-2.93587273339684,-0.786550656032357,
18.3649236178719));
#60236=CARTESIAN_POINT('Ctrl Pts',(-2.94316033587002,0.00260673739485059,
18.3221761170896));
#60237=CARTESIAN_POINT('Ctrl Pts',(-2.93873926947604,-0.00201622880601424,
18.1778238829105));
#60238=CARTESIAN_POINT('Ctrl Pts',(-2.9409582329643,-0.352525860695343,
18.1967379576091));
#60239=CARTESIAN_POINT('Ctrl Pts',(-2.8829659327141,-0.702325513325489,
18.2156520323078));
#60240=CARTESIAN_POINT('Ctrl Pts',(-2.76149291692009,-1.02848258833687,
18.2345661070064));
#60241=CARTESIAN_POINT('Ctrl Pts',(-2.42204663775388,-1.93990151387084,
18.2874199218093));
#60242=CARTESIAN_POINT('Ctrl Pts',(-1.58689422703273,-2.6667010539585,18.3402737366122));
#60243=CARTESIAN_POINT('Ctrl Pts',(-0.637335842913562,-2.87705102284432,
18.3931275514152));
#60244=CARTESIAN_POINT('Ctrl Pts',(0.312222541205624,-3.08740099173015,
18.4459813662181));
#60245=CARTESIAN_POINT('Ctrl Pts',(1.37618689872286,-2.7813013894141,18.498835181021));
#60246=CARTESIAN_POINT('Ctrl Pts',(2.06878987437855,-2.0985061401818,18.5516889958239));
#60247=CARTESIAN_POINT('Ctrl Pts',(2.76139285003424,-1.4157108909495,18.6045428106268));
#60248=CARTESIAN_POINT('Ctrl Pts',(3.08263444382841,-0.356219994800951,
18.6573966254298));
#60249=CARTESIAN_POINT('Ctrl Pts',(2.88584744993387,0.596241612454314,18.7102504402327));
#60250=CARTESIAN_POINT('Ctrl Pts',(2.68906045603933,1.54870321970957,18.7631042550356));
#60251=CARTESIAN_POINT('Ctrl Pts',(1.97424487445611,2.39413553807152,18.8159580698385));
#60252=CARTESIAN_POINT('Ctrl Pts',(1.06775945217669,2.74654497814968,18.8688118846414));
#60253=CARTESIAN_POINT('Ctrl Pts',(0.161274029897288,3.09895441822785,18.9216656994444));
#60254=CARTESIAN_POINT('Ctrl Pts',(-0.936881233078337,2.95834098002222,
18.9745195142473));
#60255=CARTESIAN_POINT('Ctrl Pts',(-1.72532865995951,2.38890363552703,19.0273733290502));
#60256=CARTESIAN_POINT('Ctrl Pts',(-2.47344465061743,1.84859470867852,19.0775235136703));
#60257=CARTESIAN_POINT('Ctrl Pts',(-2.94272737324388,0.922211045366831,
19.1276736982904));
#60258=CARTESIAN_POINT('Ctrl Pts',(-2.94645753962907,-0.000902846911536883,
19.1778238829105));
#60259=CARTESIAN_POINT('Origin',(0.,0.,0.));
#60260=CARTESIAN_POINT('',(-2.94181767770235,-0.00272435142412375,20.3221761170896));
#60261=CARTESIAN_POINT('',(-2.94133845650885,0.002661508174006,20.1778238829105));
#60262=CARTESIAN_POINT('',(-2.942,-3.60291088309151E-16,0.));
#60263=CARTESIAN_POINT('Ctrl Pts',(-2.94181767770235,-0.00272435142412375,
20.3221761170896));
#60264=CARTESIAN_POINT('Ctrl Pts',(-2.93494169159882,0.743426259253046,
20.2818054786483));
#60265=CARTESIAN_POINT('Ctrl Pts',(-2.64630113395455,1.49430940028337,20.241434840207));
#60266=CARTESIAN_POINT('Ctrl Pts',(-2.13403588059313,2.03223546686346,20.2010642017657));
#60267=CARTESIAN_POINT('Ctrl Pts',(-1.46088320915349,2.73910825665216,20.1480143356345));
#60268=CARTESIAN_POINT('Ctrl Pts',(-0.401579583775771,3.07825074195412,
20.0949644695033));
#60269=CARTESIAN_POINT('Ctrl Pts',(0.556945495101902,2.89376948769634,20.0419146033721));
#60270=CARTESIAN_POINT('Ctrl Pts',(1.5154705739796,2.70928823343856,19.9888647372409));
#60271=CARTESIAN_POINT('Ctrl Pts',(2.37321710635726,2.00118323962099,19.9358148711097));
#60272=CARTESIAN_POINT('Ctrl Pts',(2.73590522713548,1.0949487296533,19.8827650049785));
#60273=CARTESIAN_POINT('Ctrl Pts',(3.09859334791368,0.188714219685681,19.8297151388474));
#60274=CARTESIAN_POINT('Ctrl Pts',(2.96622305709255,-0.915649806432031,
19.7766652727162));
#60275=CARTESIAN_POINT('Ctrl Pts',(2.39964093164797,-1.71050095925033,19.723615406585));
#60276=CARTESIAN_POINT('Ctrl Pts',(1.83305880620336,-2.50535211206866,19.6705655404538));
#60277=CARTESIAN_POINT('Ctrl Pts',(0.832264846135248,-2.99069039158755,
19.6175156743226));
#60278=CARTESIAN_POINT('Ctrl Pts',(-0.142706552994196,-2.9434206244044,
19.5644658081914));
#60279=CARTESIAN_POINT('Ctrl Pts',(-1.11767795212364,-2.89615085722124,
19.5114159420602));
#60280=CARTESIAN_POINT('Ctrl Pts',(-2.06682679031441,-2.31627304333605,
19.458366075929));
#60281=CARTESIAN_POINT('Ctrl Pts',(-2.55385835606975,-1.47033929062967,
19.4053162097978));
#60282=CARTESIAN_POINT('Ctrl Pts',(-2.80828469416576,-1.02842167767351,
19.3776028455618));
#60283=CARTESIAN_POINT('Ctrl Pts',(-2.93659737620366,-0.513896332520092,
19.3498894813257));
#60284=CARTESIAN_POINT('Ctrl Pts',(-2.93716369210466,0.00036464873958586,
19.3221761170896));
#60285=CARTESIAN_POINT('Ctrl Pts',(-2.94645753962907,-0.000902846911536883,
19.1778238829105));
#60286=CARTESIAN_POINT('Ctrl Pts',(-2.94665863540772,-0.0506685377110252,
19.1805275130933));
#60287=CARTESIAN_POINT('Ctrl Pts',(-2.94550666757136,-0.100424725376753,
19.1832311432761));
#60288=CARTESIAN_POINT('Ctrl Pts',(-2.94297238022198,-0.150110405910103,
19.1859347734589));
#60289=CARTESIAN_POINT('Ctrl Pts',(-2.89342908281652,-1.12142585206726,
19.2387885882619));
#60290=CARTESIAN_POINT('Ctrl Pts',(-2.31560289721883,-2.06579549359683,
19.2916424030648));
#60291=CARTESIAN_POINT('Ctrl Pts',(-1.47330820404643,-2.55205456458153,
19.3444962178677));
#60292=CARTESIAN_POINT('Ctrl Pts',(-0.63101351087402,-3.03831363556623,
19.3973500326706));
#60293=CARTESIAN_POINT('Ctrl Pts',(0.47574968987309,-3.06646213600607,19.4502038474735));
#60294=CARTESIAN_POINT('Ctrl Pts',(1.34167365068723,-2.62364848631891,19.5030576622764));
#60295=CARTESIAN_POINT('Ctrl Pts',(2.20759761150139,-2.18083483663175,19.5559114770793));
#60296=CARTESIAN_POINT('Ctrl Pts',(2.83268233238255,-1.26705903681756,19.6087652918823));
#60297=CARTESIAN_POINT('Ctrl Pts',(2.93153690758253,-0.299517819492232,
19.6616191066852));
#60298=CARTESIAN_POINT('Ctrl Pts',(3.03039148278251,0.668023397833066,19.7144729214881));
#60299=CARTESIAN_POINT('Ctrl Pts',(2.60301591230135,1.68933003266952,19.767326736291));
#60300=CARTESIAN_POINT('Ctrl Pts',(1.84453430824712,2.29811069150536,19.8201805510939));
#60301=CARTESIAN_POINT('Ctrl Pts',(1.08605270419287,2.90689135034122,19.8730343658968));
#60302=CARTESIAN_POINT('Ctrl Pts',(-0.00353493343442576,3.10314603317647,
19.9258881806998));
#60303=CARTESIAN_POINT('Ctrl Pts',(-0.92676259337782,2.79727200326095,19.9787419955027));
#60304=CARTESIAN_POINT('Ctrl Pts',(-1.8499902533212,2.49139797334544,20.0315958103056));
#60305=CARTESIAN_POINT('Ctrl Pts',(-2.60685793558067,1.68339523067915,20.0844496251085));
#60306=CARTESIAN_POINT('Ctrl Pts',(-2.85180743635457,0.742168384306878,
20.1373034399114));
#60307=CARTESIAN_POINT('Ctrl Pts',(-2.91440438305093,0.501637472647963,
20.1508102542444));
#60308=CARTESIAN_POINT('Ctrl Pts',(-2.94356999338208,0.25240622569323,20.1643170685774));
#60309=CARTESIAN_POINT('Ctrl Pts',(-2.94133845650885,0.002661508174006,
20.1778238829105));
#60310=CARTESIAN_POINT('Origin',(0.,0.,0.));
#60311=CARTESIAN_POINT('',(-2.94661408633091,0.000803455063355558,21.3221761170896));
#60312=CARTESIAN_POINT('',(-2.93750898741464,-0.00097440350457154,21.1778238829105));
#60313=CARTESIAN_POINT('',(-2.942,-3.60291088309151E-16,0.));
#60314=CARTESIAN_POINT('Ctrl Pts',(-2.94661408633091,0.000803455063355558,
21.3221761170896));
#60315=CARTESIAN_POINT('Ctrl Pts',(-2.94677107215841,0.0441441474901623,
21.3198212082333));
#60316=CARTESIAN_POINT('Ctrl Pts',(-2.94589802603797,0.0874783744189961,
21.317466299377));
#60317=CARTESIAN_POINT('Ctrl Pts',(-2.943975270306,0.130765975174579,21.3151113905207));
#60318=CARTESIAN_POINT('Ctrl Pts',(-2.90066067071482,1.10592109384657,21.2620615243895));
#60319=CARTESIAN_POINT('Ctrl Pts',(-2.32463766198353,2.05741428325321,21.2090116582583));
#60320=CARTESIAN_POINT('Ctrl Pts',(-1.48068641588049,2.54787320529567,21.1559617921271));
#60321=CARTESIAN_POINT('Ctrl Pts',(-0.636735169777449,3.03833212733813,
21.1029119259959));
#60322=CARTESIAN_POINT('Ctrl Pts',(0.475144313697323,3.06775678201641,21.0498620598648));
#60323=CARTESIAN_POINT('Ctrl Pts',(1.34385501904681,2.62262155489871,20.9968121937336));
#60324=CARTESIAN_POINT('Ctrl Pts',(2.2125657243963,2.17748632778101,20.9437623276024));
#60325=CARTESIAN_POINT('Ctrl Pts',(2.83810765162053,1.25779121886726,20.8907124614712));
#60326=CARTESIAN_POINT('Ctrl Pts',(2.93293829559698,0.286291960518122,20.83766259534));
#60327=CARTESIAN_POINT('Ctrl Pts',(3.02776893957345,-0.685207297831074,
20.7846127292088));
#60328=CARTESIAN_POINT('Ctrl Pts',(2.59188830030215,-1.70851070561573,20.7315628630776));
#60329=CARTESIAN_POINT('Ctrl Pts',(1.82565738556811,-2.31323696212845,20.6785129969464));
#60330=CARTESIAN_POINT('Ctrl Pts',(1.05942647083414,-2.91796321864112,20.6254631308152));
#60331=CARTESIAN_POINT('Ctrl Pts',(-0.0371547193624712,-3.10411232388192,
20.572413264684));
#60332=CARTESIAN_POINT('Ctrl Pts',(-0.96002132737357,-2.78611722356123,
20.5193633985529));
#60333=CARTESIAN_POINT('Ctrl Pts',(-1.88288793538472,-2.46812212324052,
20.4663135324217));
#60334=CARTESIAN_POINT('Ctrl Pts',(-2.63203996121031,-1.64598281735826,
20.4132636662905));
#60335=CARTESIAN_POINT('Ctrl Pts',(-2.86311511537232,-0.697611617279415,
20.3602138001593));
#60336=CARTESIAN_POINT('Ctrl Pts',(-2.91834342614413,-0.47094536423746,
20.3475345724694));
#60337=CARTESIAN_POINT('Ctrl Pts',(-2.94397722228141,-0.237068266928035,
20.3348553447795));
#60338=CARTESIAN_POINT('Ctrl Pts',(-2.94181767770235,-0.00272435142412375,
20.3221761170896));
#60339=CARTESIAN_POINT('Ctrl Pts',(-2.94133845650885,0.002661508174006,
20.1778238829105));
#60340=CARTESIAN_POINT('Ctrl Pts',(-2.93483771693884,-0.72487536879094,
20.2171708833804));
#60341=CARTESIAN_POINT('Ctrl Pts',(-2.66189196800706,-1.45676970117924,
20.2565178838503));
#60342=CARTESIAN_POINT('Ctrl Pts',(-2.17278956561389,-1.99062931463176,
20.2958648843202));
#60343=CARTESIAN_POINT('Ctrl Pts',(-1.51579087481095,-2.70774921711983,
20.3487186991231));
#60344=CARTESIAN_POINT('Ctrl Pts',(-0.468762173916675,-3.06753807201771,
20.401572513926));
#60345=CARTESIAN_POINT('Ctrl Pts',(0.490261385495665,-2.90572939872311,
20.4544263287289));
#60346=CARTESIAN_POINT('Ctrl Pts',(1.44928494490802,-2.74392072542852,20.5072801435319));
#60347=CARTESIAN_POINT('Ctrl Pts',(2.32030336283847,-2.06051452394146,20.5601339583348));
#60348=CARTESIAN_POINT('Ctrl Pts',(2.70564136917951,-1.16752916284621,20.6129877731377));
#60349=CARTESIAN_POINT('Ctrl Pts',(3.09097937552055,-0.274543801750937,
20.6658415879406));
#60350=CARTESIAN_POINT('Ctrl Pts',(2.99063697027215,0.828020718952537,20.7186954027435));
#60351=CARTESIAN_POINT('Ctrl Pts',(2.4504268392386,1.6367736160664,20.7715492175465));
#60352=CARTESIAN_POINT('Ctrl Pts',(1.91021670820505,2.44552651318024,20.8244030323494));
#60353=CARTESIAN_POINT('Ctrl Pts',(0.930138851386389,2.96046778670446,20.8772568471523));
#60354=CARTESIAN_POINT('Ctrl Pts',(-0.0423388953904588,2.94649401537642,
20.9301106619552));
#60355=CARTESIAN_POINT('Ctrl Pts',(-1.01481664216731,2.93252024404837,20.9829644767581));
#60356=CARTESIAN_POINT('Ctrl Pts',(-1.97969427890232,2.38963142786804,21.035818291561));
#60357=CARTESIAN_POINT('Ctrl Pts',(-2.49644383636957,1.56569081767899,21.088672106364));
#60358=CARTESIAN_POINT('Ctrl Pts',(-2.78698824487709,1.10242706878285,21.1183893652128));
#60359=CARTESIAN_POINT('Ctrl Pts',(-2.93586621539549,0.550314599197934,
21.1481066240616));
#60360=CARTESIAN_POINT('Ctrl Pts',(-2.93750898741464,-0.00097440350457154,
21.1778238829105));
#60361=CARTESIAN_POINT('Origin',(0.,0.,0.));
#60362=CARTESIAN_POINT('',(-2.93936618898165,0.00234662407228609,22.3221761170896));
#60363=CARTESIAN_POINT('',(-2.94488602564283,-0.00204434552984655,22.1778238829105));
#60364=CARTESIAN_POINT('',(-2.942,-3.60291088309151E-16,0.));
#60365=CARTESIAN_POINT('Ctrl Pts',(-2.93936618898165,0.00234662407228609,
22.3221761170896));
#60366=CARTESIAN_POINT('Ctrl Pts',(-2.94175919559491,0.324419742206598,
22.3047870716871));
#60367=CARTESIAN_POINT('Ctrl Pts',(-2.89299512987164,0.645788293098763,
22.2873980262846));
#60368=CARTESIAN_POINT('Ctrl Pts',(-2.78998843935577,0.948712095789747,
22.2700089808822));
#60369=CARTESIAN_POINT('Ctrl Pts',(-2.47573938105466,1.87286099578738,22.216959114751));
#60370=CARTESIAN_POINT('Ctrl Pts',(-1.65664562584339,2.62534170401123,22.1639092486198));
#60371=CARTESIAN_POINT('Ctrl Pts',(-0.709219538526518,2.86026183742134,
22.1108593824886));
#60372=CARTESIAN_POINT('Ctrl Pts',(0.238206548790326,3.09518197083143,22.0578095163574));
#60373=CARTESIAN_POINT('Ctrl Pts',(1.31396496821276,2.81254152942782,22.0047596502262));
#60374=CARTESIAN_POINT('Ctrl Pts',(2.02356245339832,2.14226168561014,21.951709784095));
#60375=CARTESIAN_POINT('Ctrl Pts',(2.7331599385839,1.47198184179245,21.8986599179638));
#60376=CARTESIAN_POINT('Ctrl Pts',(3.07659648953258,0.414062595560654,21.8456100518326));
#60377=CARTESIAN_POINT('Ctrl Pts',(2.89600482043572,-0.54520290942886,21.7925601857014));
#60378=CARTESIAN_POINT('Ctrl Pts',(2.71541315133886,-1.5044684144184,21.7395103195703));
#60379=CARTESIAN_POINT('Ctrl Pts',(2.01079326219644,-2.36508017816566,21.6864604534391));
#60380=CARTESIAN_POINT('Ctrl Pts',(1.10603738031632,-2.73144127628248,21.6334105873079));
#60381=CARTESIAN_POINT('Ctrl Pts',(0.201281498436279,-3.09780237439927,
21.5803607211767));
#60382=CARTESIAN_POINT('Ctrl Pts',(-0.903610376181412,-2.96991280688572,
21.5273108550455));
#60383=CARTESIAN_POINT('Ctrl Pts',(-1.70075321826476,-2.40655949916031,
21.4742609889143));
#60384=CARTESIAN_POINT('Ctrl Pts',(-2.4625105094419,-1.86821371342004,21.4235660316394));
#60385=CARTESIAN_POINT('Ctrl Pts',(-2.94323459680346,-0.932206986069505,
21.3728710743645));
#60386=CARTESIAN_POINT('Ctrl Pts',(-2.94661408633091,0.000803455063355558,
21.3221761170896));
#60387=CARTESIAN_POINT('Ctrl Pts',(-2.93750898741464,-0.00097440350457154,
21.1778238829105));
#60388=CARTESIAN_POINT('Ctrl Pts',(-2.93878797774595,-0.430183871402343,
21.2009604388645));
#60389=CARTESIAN_POINT('Ctrl Pts',(-2.85082038965928,-0.858894195057127,
21.2240969948186));
#60390=CARTESIAN_POINT('Ctrl Pts',(-2.67097820455793,-1.244787128584,21.2472335507727));
#60391=CARTESIAN_POINT('Ctrl Pts',(-2.26014153707957,-2.12633206046017,
21.3000873655756));
#60392=CARTESIAN_POINT('Ctrl Pts',(-1.36984672392337,-2.78442952001476,
21.3529411803785));
#60393=CARTESIAN_POINT('Ctrl Pts',(-0.406569934833748,-2.91861618799067,
21.4057949951814));
#60394=CARTESIAN_POINT('Ctrl Pts',(0.556706854255877,-3.05280285596659,
21.4586488099844));
#60395=CARTESIAN_POINT('Ctrl Pts',(1.59296561927893,-2.66307873236383,21.5115026247873));
#60396=CARTESIAN_POINT('Ctrl Pts',(2.22908836892936,-1.92737765064757,21.5643564395902));
#60397=CARTESIAN_POINT('Ctrl Pts',(2.86521111857982,-1.1916765689313,21.6172102543931));
#60398=CARTESIAN_POINT('Ctrl Pts',(3.10119785285763,-0.109998529101508,
21.670064069196));
#60399=CARTESIAN_POINT('Ctrl Pts',(2.82930562814205,0.823801691716928,21.722917883999));
#60400=CARTESIAN_POINT('Ctrl Pts',(2.55741340342647,1.75760191253534,21.7757716988019));
#60401=CARTESIAN_POINT('Ctrl Pts',(1.77764221971752,2.5435243143424,21.8286255136048));
#60402=CARTESIAN_POINT('Ctrl Pts',(0.846007184985371,2.82274536713198,21.8814793284077));
#60403=CARTESIAN_POINT('Ctrl Pts',(-0.0856278497467812,3.10196641992156,
21.9343331432106));
#60404=CARTESIAN_POINT('Ctrl Pts',(-1.16912673550214,2.87448612369365,21.9871869580135));
#60405=CARTESIAN_POINT('Ctrl Pts',(-1.90980336325705,2.2441636924262,22.0400407728165));
#60406=CARTESIAN_POINT('Ctrl Pts',(-2.55341965804143,1.69644047215729,22.0859684761811));
#60407=CARTESIAN_POINT('Ctrl Pts',(-2.93817544933017,0.844536541703994,
22.1318961795458));
#60408=CARTESIAN_POINT('Ctrl Pts',(-2.94488602564283,-0.00204434552984655,
22.1778238829105));
#60409=CARTESIAN_POINT('Origin',(0.,0.,0.));
#60410=CARTESIAN_POINT('',(-2.93809596128261,-0.00168714029618489,23.3221761170896));
#60411=CARTESIAN_POINT('',(-2.94367738520799,0.0024475330369777,23.1778238829105));
#60412=CARTESIAN_POINT('',(-2.942,-3.60291088309151E-16,0.));
#60413=CARTESIAN_POINT('Ctrl Pts',(-2.93809596128261,-0.00168714029618489,
23.3221761170896));
#60414=CARTESIAN_POINT('Ctrl Pts',(-2.93497421326337,0.599494484093746,
23.2897529351409));
#60415=CARTESIAN_POINT('Ctrl Pts',(-2.75577143026152,1.20238463007766,23.2573297531923));
#60416=CARTESIAN_POINT('Ctrl Pts',(-2.41343846997067,1.69097749367112,23.2249065712436));
#60417=CARTESIAN_POINT('Ctrl Pts',(-1.85332324918586,2.49039890910546,23.1718567051124));
#60418=CARTESIAN_POINT('Ctrl Pts',(-0.856499547571336,2.98384019636719,
23.1188068389812));
#60419=CARTESIAN_POINT('Ctrl Pts',(0.118823245776437,2.94448147705157,23.06575697285));
#60420=CARTESIAN_POINT('Ctrl Pts',(1.09414603912426,2.90512275773594,23.0127071067188));
#60421=CARTESIAN_POINT('Ctrl Pts',(2.04796792420534,2.3329640318429,22.9596572405877));
#60422=CARTESIAN_POINT('Ctrl Pts',(2.54184613269262,1.49100917842654,22.9066073744565));
#60423=CARTESIAN_POINT('Ctrl Pts',(3.0357243411799,0.649054325010205,22.8535575083253));
#60424=CARTESIAN_POINT('Ctrl Pts',(3.06965887307341,-0.462696655929437,
22.8005076421941));
#60425=CARTESIAN_POINT('Ctrl Pts',(2.62805106122367,-1.33320581758324,22.7474577760629));
#60426=CARTESIAN_POINT('Ctrl Pts',(2.18644324937392,-2.20371497923707,22.6944079099317));
#60427=CARTESIAN_POINT('Ctrl Pts',(1.26929309378089,-2.83298232160505,22.6413580438005));
#60428=CARTESIAN_POINT('Ctrl Pts',(0.298186489546595,-2.93175288008531,
22.5883081776693));
#60429=CARTESIAN_POINT('Ctrl Pts',(-0.672920114687705,-3.03052343856557,
22.5352583115381));
#60430=CARTESIAN_POINT('Ctrl Pts',(-1.69798316756328,-2.59879721315811,
22.4822084454069));
#60431=CARTESIAN_POINT('Ctrl Pts',(-2.30581251330558,-1.83502555456867,
22.4291585792757));
#60432=CARTESIAN_POINT('Ctrl Pts',(-2.71440342809815,-1.32160815729808,
22.393497758547));
#60433=CARTESIAN_POINT('Ctrl Pts',(-2.93445869821015,-0.658149191626092,
22.3578369378183));
#60434=CARTESIAN_POINT('Ctrl Pts',(-2.93936618898165,0.00234662407228609,
22.3221761170896));
#60435=CARTESIAN_POINT('Ctrl Pts',(-2.94488602564283,-0.00204434552984655,
22.1778238829105));
#60436=CARTESIAN_POINT('Ctrl Pts',(-2.94589801178521,-0.129712683742034,
22.1847499943487));
#60437=CARTESIAN_POINT('Ctrl Pts',(-2.93831247708221,-0.257259965072063,
22.191676105787));
#60438=CARTESIAN_POINT('Ctrl Pts',(-2.92172066492491,-0.383624713571277,
22.1986022172252));
#60439=CARTESIAN_POINT('Ctrl Pts',(-2.7951069690834,-1.34792612199431,22.2514560320281));
#60440=CARTESIAN_POINT('Ctrl Pts',(-2.14402520764591,-2.24336437253339,
22.304309846831));
#60441=CARTESIAN_POINT('Ctrl Pts',(-1.26573558775814,-2.66111498935963,
22.3571636616339));
#60442=CARTESIAN_POINT('Ctrl Pts',(-0.387445967870374,-3.07886560618586,
22.4100174764369));
#60443=CARTESIAN_POINT('Ctrl Pts',(0.718051510467669,-3.01892858929924,
22.4628712912398));
#60444=CARTESIAN_POINT('Ctrl Pts',(1.5460269824779,-2.50866899653226,22.5157251060427));
#60445=CARTESIAN_POINT('Ctrl Pts',(2.37400245448816,-1.99840940376527,22.5685789208456));
#60446=CARTESIAN_POINT('Ctrl Pts',(2.9244559201706,-1.03782723511788,22.6214327356485));
#60447=CARTESIAN_POINT('Ctrl Pts',(2.9460703853714,-0.0654893056121799,
22.6742865504515));
#60448=CARTESIAN_POINT('Ctrl Pts',(2.96768485057219,0.906848623893493,22.7271403652544));
#60449=CARTESIAN_POINT('Ctrl Pts',(2.46046031529139,1.89094231425748,22.7799941800573));
#60450=CARTESIAN_POINT('Ctrl Pts',(1.65597701930418,2.4374904463912,22.8328479948602));
#60451=CARTESIAN_POINT('Ctrl Pts',(0.851493723316973,2.98403857852492,22.8857018096631));
#60452=CARTESIAN_POINT('Ctrl Pts',(-0.250248333376632,3.09304115242837,
22.9385556244661));
#60453=CARTESIAN_POINT('Ctrl Pts',(-1.14623387467553,2.71473156486203,22.991409439269));
#60454=CARTESIAN_POINT('Ctrl Pts',(-2.04221941597443,2.33642197729568,23.0442632540719));
#60455=CARTESIAN_POINT('Ctrl Pts',(-2.73244844187862,1.47080022825954,23.0971170688748));
#60456=CARTESIAN_POINT('Ctrl Pts',(-2.90178753079562,0.513077665496164,
23.1499708836777));
#60457=CARTESIAN_POINT('Ctrl Pts',(-2.93153373758168,0.344843540830449,
23.1592552167553));
#60458=CARTESIAN_POINT('Ctrl Pts',(-2.94520702688292,0.173767493765761,
23.1685395498329));
#60459=CARTESIAN_POINT('Ctrl Pts',(-2.94367738520799,0.0024475330369777,
23.1778238829105));
#60460=CARTESIAN_POINT('Origin',(0.,0.,0.));
#60461=CARTESIAN_POINT('',(-2.94555278480659,-0.00176380088044714,24.3221761170896));
#60462=CARTESIAN_POINT('',(-2.93722802281203,0.000281837720408654,24.1778238829105));
#60463=CARTESIAN_POINT('',(-2.942,-3.60291088309151E-16,0.));
#60464=CARTESIAN_POINT('Ctrl Pts',(-2.94555278480659,-0.00176380088044714,
24.3221761170896));
#60465=CARTESIAN_POINT('Ctrl Pts',(-2.93937087079276,0.87249287190428,24.2747187985947));
#60466=CARTESIAN_POINT('Ctrl Pts',(-2.525406696364,1.75183148857115,24.2272614800999));
#60467=CARTESIAN_POINT('Ctrl Pts',(-1.84436353069014,2.29835012543712,24.179804161605));
#60468=CARTESIAN_POINT('Ctrl Pts',(-1.08306369508132,2.90927255939407,24.1267542954739));
#60469=CARTESIAN_POINT('Ctrl Pts',(0.0119712680674577,3.10431159537625,
24.0737044293427));
#60470=CARTESIAN_POINT('Ctrl Pts',(0.93738725442356,2.79381374964061,24.0206545632115));
#60471=CARTESIAN_POINT('Ctrl Pts',(1.86280324077969,2.48331590390496,23.9676046970803));
#60472=CARTESIAN_POINT('Ctrl Pts',(2.61860025034316,1.66728117645145,23.9145548309491));
#60473=CARTESIAN_POINT('Ctrl Pts',(2.85736149770633,0.720815790519383,23.8615049648179));
#60474=CARTESIAN_POINT('Ctrl Pts',(3.09612274506951,-0.225649595412714,
23.8084550986867));
#60475=CARTESIAN_POINT('Ctrl Pts',(2.8178482302324,-1.30254563982334,23.7554052325555));
#60476=CARTESIAN_POINT('Ctrl Pts',(2.1504522425905,-2.01485614493296,23.7023553664243));
#60477=CARTESIAN_POINT('Ctrl Pts',(1.48305625494865,-2.72716665004254,23.6493055002931));
#60478=CARTESIAN_POINT('Ctrl Pts',(0.42653879450204,-3.07489161585109,23.596255634162));
#60479=CARTESIAN_POINT('Ctrl Pts',(-0.533451353174756,-2.89819250330834,
23.5432057680308));
#60480=CARTESIAN_POINT('Ctrl Pts',(-1.49344150085158,-2.72149339076559,
23.4901559018996));
#60481=CARTESIAN_POINT('Ctrl Pts',(-2.35690433575861,-2.02037019987151,
23.4371060357684));
#60482=CARTESIAN_POINT('Ctrl Pts',(-2.7269323832346,-1.11710783262096,23.3840561696372));
#60483=CARTESIAN_POINT('Ctrl Pts',(-2.87080553939092,-0.765904164412539,
23.3634294854547));
#60484=CARTESIAN_POINT('Ctrl Pts',(-2.94008192646617,-0.384141383135884,
23.3428028012721));
#60485=CARTESIAN_POINT('Ctrl Pts',(-2.93809596128261,-0.00168714029618489,
23.3221761170896));
#60486=CARTESIAN_POINT('Ctrl Pts',(-2.94367738520799,0.0024475330369777,
23.1778238829105));
#60487=CARTESIAN_POINT('Ctrl Pts',(-2.93649908877625,-0.801522104392271,
23.2213933646358));
#60488=CARTESIAN_POINT('Ctrl Pts',(-2.59451675492149,-1.61086329021898,
23.2649628463611));
#60489=CARTESIAN_POINT('Ctrl Pts',(-2.00764029345905,-2.15708136536191,
23.3085323280865));
#60490=CARTESIAN_POINT('Ctrl Pts',(-1.29570481527567,-2.81969445696598,
23.3613861428894));
#60491=CARTESIAN_POINT('Ctrl Pts',(-0.223384706979118,-3.0950972636835,
23.4142399576923));
#60492=CARTESIAN_POINT('Ctrl Pts',(0.719737744845044,-2.8575508995217,23.4670937724952));
#60493=CARTESIAN_POINT('Ctrl Pts',(1.66286019666921,-2.62000453535991,23.5199475872981));
#60494=CARTESIAN_POINT('Ctrl Pts',(2.47678499202095,-1.8695090003188,23.5728014021011));
#60495=CARTESIAN_POINT('Ctrl Pts',(2.78990372839629,-0.948713207978274,
23.625655216904));
#60496=CARTESIAN_POINT('Ctrl Pts',(3.10302246477162,-0.0279174156377443,
23.6785090317069));
#60497=CARTESIAN_POINT('Ctrl Pts',(2.91533514217051,1.06317863400226,23.7313628465098));
#60498=CARTESIAN_POINT('Ctrl Pts',(2.31253295285098,1.82642024372548,23.7842166613127));
#60499=CARTESIAN_POINT('Ctrl Pts',(1.70973076353145,2.58966185344871,23.8370704761156));
#60500=CARTESIAN_POINT('Ctrl Pts',(0.691813707493536,3.02504902325521,23.8899242909186));
#60501=CARTESIAN_POINT('Ctrl Pts',(-0.276474379915739,2.93379983672406,
23.9427781057215));
#60502=CARTESIAN_POINT('Ctrl Pts',(-1.24476246732499,2.84255065019292,23.9956319205244));
#60503=CARTESIAN_POINT('Ctrl Pts',(-2.16342158610557,2.22466510732416,24.0484857353273));
#60504=CARTESIAN_POINT('Ctrl Pts',(-2.61302545814756,1.36224723152027,24.1013395501302));
#60505=CARTESIAN_POINT('Ctrl Pts',(-2.82989818087518,0.946247894136707,
24.1268343277236));
#60506=CARTESIAN_POINT('Ctrl Pts',(-2.9376334601039,0.473351988907629,24.1523291053171));
#60507=CARTESIAN_POINT('Ctrl Pts',(-2.93722802281203,0.000281837720408654,
24.1778238829105));
#60508=CARTESIAN_POINT('Origin',(0.,0.,0.));
#60509=CARTESIAN_POINT('',(-2.94363848369983,0.00251143626685393,25.3221761170896));
#60510=CARTESIAN_POINT('',(-2.94264856609968,-0.00262420787473867,25.1778238829105));
#60511=CARTESIAN_POINT('',(-2.942,-3.60291088309151E-16,0.));
#60512=CARTESIAN_POINT('Ctrl Pts',(-2.94363848369983,0.00251143626685393,
25.3221761170896));
#60513=CARTESIAN_POINT('Ctrl Pts',(-2.94521862476287,0.176738668532974,
25.3127345281798));
#60514=CARTESIAN_POINT('Ctrl Pts',(-2.93108735667538,0.350709910061776,
25.3032929392699));
#60515=CARTESIAN_POINT('Ctrl Pts',(-2.90033250031881,0.521691019695654,
25.2938513503601));
#60516=CARTESIAN_POINT('Ctrl Pts',(-2.72752885167656,1.48239001471223,25.2408014842289));
#60517=CARTESIAN_POINT('Ctrl Pts',(-2.02991389507056,2.34868971365866,25.1877516180977));
#60518=CARTESIAN_POINT('Ctrl Pts',(-1.12815990441773,2.72237862217966,25.1347017519665));
#60519=CARTESIAN_POINT('Ctrl Pts',(-0.226405913764866,3.09606753070067,
25.0816518858353));
#60520=CARTESIAN_POINT('Ctrl Pts',(0.879487110934829,2.9771456487962,25.0286020197041));
#60521=CARTESIAN_POINT('Ctrl Pts',(1.68117394631541,2.42027773089514,24.9755521535729));
#60522=CARTESIAN_POINT('Ctrl Pts',(2.48286078169597,1.86340981299409,24.9225022874417));
#60523=CARTESIAN_POINT('Ctrl Pts',(2.98034142775742,0.868595859096418,24.8694524213105));
#60524=CARTESIAN_POINT('Ctrl Pts',(2.94493923631214,-0.10687856130158,24.8164025551794));
#60525=CARTESIAN_POINT('Ctrl Pts',(2.90953704486686,-1.08235298169963,24.7633526890482));
#60526=CARTESIAN_POINT('Ctrl Pts',(2.34125201591485,-2.03848786859804,24.710302822917));
#60527=CARTESIAN_POINT('Ctrl Pts',(1.50130740842057,-2.53577723742803,24.6572529567858));
#60528=CARTESIAN_POINT('Ctrl Pts',(0.66136280092637,-3.03306660625799,24.6042030906546));
#60529=CARTESIAN_POINT('Ctrl Pts',(-0.450241385110007,-3.0715104570196,
24.5511532245234));
#60530=CARTESIAN_POINT('Ctrl Pts',(-1.32253468000992,-2.6334373265008,24.4981033583922));
#60531=CARTESIAN_POINT('Ctrl Pts',(-2.1948279749099,-2.19536419598197,24.445053492261));
#60532=CARTESIAN_POINT('Ctrl Pts',(-2.82781037867336,-1.28077408418266,
24.3920036261298));
#60533=CARTESIAN_POINT('Ctrl Pts',(-2.93051922652061,-0.310076112317096,
24.3389537599986));
#60534=CARTESIAN_POINT('Ctrl Pts',(-2.94134685279283,-0.207744569486468,
24.3333612123623));
#60535=CARTESIAN_POINT('Ctrl Pts',(-2.94628128463976,-0.104789472031122,
24.3277686647259));
#60536=CARTESIAN_POINT('Ctrl Pts',(-2.94555278480659,-0.00176380088044714,
24.3221761170896));
#60537=CARTESIAN_POINT('Ctrl Pts',(-2.93722802281203,0.000281837720408654,
24.1778238829105));
#60538=CARTESIAN_POINT('Ctrl Pts',(-2.93679293864966,-0.507380714800876,
24.20518292012));
#60539=CARTESIAN_POINT('Ctrl Pts',(-2.81182371976808,-1.01524392781641,
24.2325419573295));
#60540=CARTESIAN_POINT('Ctrl Pts',(-2.56355212294478,-1.45321026615464,
24.259900994539));
#60541=CARTESIAN_POINT('Ctrl Pts',(-2.08392629039663,-2.2992996792865,24.3127548093419));
#60542=CARTESIAN_POINT('Ctrl Pts',(-1.14412599999694,-2.88452829681116,
24.3656086241448));
#60543=CARTESIAN_POINT('Ctrl Pts',(-0.17322981844223,-2.94170205743451,
24.4184624389477));
#60544=CARTESIAN_POINT('Ctrl Pts',(0.797666363112456,-2.99887581805785,
24.4713162537506));
#60545=CARTESIAN_POINT('Ctrl Pts',(1.7996584358222,-2.52799472177994,24.5241700685536));
#60546=CARTESIAN_POINT('Ctrl Pts',(2.37527333142833,-1.74404591846582,24.5770238833565));
#60547=CARTESIAN_POINT('Ctrl Pts',(2.95088822703446,-0.960097115151713,
24.6298776981594));
#60548=CARTESIAN_POINT('Ctrl Pts',(3.100125945537,0.136919395198534,24.6827315129623));
#60549=CARTESIAN_POINT('Ctrl Pts',(2.75484998282307,1.04614584874751,24.7355853277652));
#60550=CARTESIAN_POINT('Ctrl Pts',(2.40957402010914,1.95537230229652,24.7884391425681));
#60551=CARTESIAN_POINT('Ctrl Pts',(1.56978437617865,2.67680869904419,24.8412929573711));
#60552=CARTESIAN_POINT('Ctrl Pts',(0.618898400893287,2.88107346905344,24.894146772174));
#60553=CARTESIAN_POINT('Ctrl Pts',(-0.331987574392054,3.08533823906269,
24.9470005869769));
#60554=CARTESIAN_POINT('Ctrl Pts',(-1.3939698810323,2.77243138233356,24.9998544017798));
#60555=CARTESIAN_POINT('Ctrl Pts',(-2.08218609597328,2.0852147674634,25.0527082165827));
#60556=CARTESIAN_POINT('Ctrl Pts',(-2.62523507380622,1.54295454145717,25.094413438692));
#60557=CARTESIAN_POINT('Ctrl Pts',(-2.93556705736549,0.767638819576851,
25.1361186608012));
#60558=CARTESIAN_POINT('Ctrl Pts',(-2.94264856609968,-0.00262420787473867,
25.1778238829105));
#60559=CARTESIAN_POINT('Origin',(0.,0.,0.));
#60560=CARTESIAN_POINT('',(-2.93724345526557,0.000625155175501269,26.3221761170896));
#60561=CARTESIAN_POINT('',(-2.94570126337859,0.00159745694066759,26.1778238829105));
#60562=CARTESIAN_POINT('',(-2.942,-3.60291088309151E-16,0.));
#60563=CARTESIAN_POINT('Ctrl Pts',(-2.93724345526557,0.000625155175501269,
26.3221761170896));
#60564=CARTESIAN_POINT('Ctrl Pts',(-2.93810221353313,0.454776386691649,
26.2977003916336));
#60565=CARTESIAN_POINT('Ctrl Pts',(-2.83926083141474,0.9085735093724,26.2732246661775));
#60566=CARTESIAN_POINT('Ctrl Pts',(-2.63878026210633,1.31184178190614,26.2487489407215));
#60567=CARTESIAN_POINT('Ctrl Pts',(-2.20424902082298,2.18590485763848,26.1956990745903));
#60568=CARTESIAN_POINT('Ctrl Pts',(-1.29223400116845,2.82259190792271,26.1426492084591));
#60569=CARTESIAN_POINT('Ctrl Pts',(-0.321960633202111,2.92923735520096,
26.0895993423279));
#60570=CARTESIAN_POINT('Ctrl Pts',(0.648312734764256,3.03588280247922,26.0365494761968));
#60571=CARTESIAN_POINT('Ctrl Pts',(1.67684445104244,2.61248664675148,25.9834996100656));
#60572=CARTESIAN_POINT('Ctrl Pts',(2.29084992130659,1.85367116028875,25.9304497439344));
#60573=CARTESIAN_POINT('Ctrl Pts',(2.90485539157074,1.09485567382602,25.8773998778032));
#60574=CARTESIAN_POINT('Ctrl Pts',(3.10433461582086,0.000620856628295308,
25.824350011672));
#60575=CARTESIAN_POINT('Ctrl Pts',(2.79759309147536,-0.926046989610136,
25.7713001455408));
#60576=CARTESIAN_POINT('Ctrl Pts',(2.49085156712986,-1.85271483584854,25.7182502794096));
#60577=CARTESIAN_POINT('Ctrl Pts',(1.67788929418876,-2.61181571112766,25.6652004132784));
#60578=CARTESIAN_POINT('Ctrl Pts',(0.732400182457275,-2.85441414394849,
25.6121505471472));
#60579=CARTESIAN_POINT('Ctrl Pts',(-0.213088929274242,-3.09701257676932,
25.5591006810161));
#60580=CARTESIAN_POINT('Ctrl Pts',(-1.29110487979616,-2.82310856713184,
25.5060508148848));
#60581=CARTESIAN_POINT('Ctrl Pts',(-2.00611668471787,-2.15860741676972,
25.4530009487536));
#60582=CARTESIAN_POINT('Ctrl Pts',(-2.59387373821273,-1.61237134697007,
25.4093926715323));
#60583=CARTESIAN_POINT('Ctrl Pts',(-2.93634021746692,-0.802199456859896,
25.3657843943109));
#60584=CARTESIAN_POINT('Ctrl Pts',(-2.94363848369983,0.00251143626685393,
25.3221761170896));
#60585=CARTESIAN_POINT('Ctrl Pts',(-2.94264856609968,-0.00262420787473867,
25.1778238829105));
#60586=CARTESIAN_POINT('Ctrl Pts',(-2.94454158698631,-0.208530047137775,
25.1889724756041));
#60587=CARTESIAN_POINT('Ctrl Pts',(-2.92476451808285,-0.414074824008361,
25.2001210682978));
#60588=CARTESIAN_POINT('Ctrl Pts',(-2.88196999784739,-0.61471009119703,
25.2112696609915));
#60589=CARTESIAN_POINT('Ctrl Pts',(-2.67908756153879,-1.56589196197611,
25.2641234757944));
#60590=CARTESIAN_POINT('Ctrl Pts',(-1.95887256567987,-2.40672933052306,
25.3169772905973));
#60591=CARTESIAN_POINT('Ctrl Pts',(-1.05014893306918,-2.75332649409503,
25.3698311054002));
#60592=CARTESIAN_POINT('Ctrl Pts',(-0.141425300458436,-3.09992365766701,
25.4226849202032));
#60593=CARTESIAN_POINT('Ctrl Pts',(0.9558069689041,-2.95228061626393,25.4755387350061));
#60594=CARTESIAN_POINT('Ctrl Pts',(1.74059160347801,-2.37780580254439,25.528392549809));
#60595=CARTESIAN_POINT('Ctrl Pts',(2.52537623805186,-1.8033309888249,25.5812463646119));
#60596=CARTESIAN_POINT('Ctrl Pts',(2.99771323783714,-0.802024402789044,
25.6341001794148));
#60597=CARTESIAN_POINT('Ctrl Pts',(2.94195074047982,0.168953855541036,25.6869539942177));
#60598=CARTESIAN_POINT('Ctrl Pts',(2.88618824312249,1.13993211387114,25.7398078090207));
#60599=CARTESIAN_POINT('Ctrl Pts',(2.30232624862252,2.08058204449547,25.7926616238236));
#60600=CARTESIAN_POINT('Ctrl Pts',(1.45693486800003,2.5614371659515,25.8455154386265));
#60601=CARTESIAN_POINT('Ctrl Pts',(0.61154348737756,3.04229228740752,25.8983692534294));
#60602=CARTESIAN_POINT('Ctrl Pts',(-0.495377279367419,3.06335259969526,
25.9512230682323));
#60603=CARTESIAN_POINT('Ctrl Pts',(-1.35844774583423,2.61500273165246,26.0040768830352));
#60604=CARTESIAN_POINT('Ctrl Pts',(-2.2215182123011,2.16665286360963,26.0569306978382));
#60605=CARTESIAN_POINT('Ctrl Pts',(-2.84073837848977,1.2488928152362,26.1097845126411));
#60606=CARTESIAN_POINT('Ctrl Pts',(-2.93339488062293,0.280738381855969,
26.162638327444));
#60607=CARTESIAN_POINT('Ctrl Pts',(-2.94226866742349,0.188017462826645,
26.1677001792662));
#60608=CARTESIAN_POINT('Ctrl Pts',(-2.94631278858676,0.0948343242288374,
26.1727620310883));
#60609=CARTESIAN_POINT('Ctrl Pts',(-2.94570126337859,0.00159745694066759,
26.1778238829105));
#60610=CARTESIAN_POINT('Origin',(0.,0.,0.));
#60611=CARTESIAN_POINT('',(-2.94133724676478,-0.0027142933295754,27.3221761170896));
#60612=CARTESIAN_POINT('',(-2.9379441153396,0.0014763941512189,27.1778238829104));
#60613=CARTESIAN_POINT('',(-2.942,-3.60291088309151E-16,0.));
#60614=CARTESIAN_POINT('Ctrl Pts',(-2.94133724676478,-0.0027142933295754,
27.3221761170896));
#60615=CARTESIAN_POINT('Ctrl Pts',(-2.93472634309306,0.727831082166025,
27.2826662550874));
#60616=CARTESIAN_POINT('Ctrl Pts',(-2.65946238238259,1.46282296367726,27.2431563930852));
#60617=CARTESIAN_POINT('Ctrl Pts',(-2.16672707396524,1.99734421654923,27.203646531083));
#60618=CARTESIAN_POINT('Ctrl Pts',(-1.50513169435615,2.71504555672481,27.1505966649518));
#60619=CARTESIAN_POINT('Ctrl Pts',(-0.451469932853536,3.07133011774635,
27.0975467988206));
#60620=CARTESIAN_POINT('Ctrl Pts',(0.509922102492116,2.90242477625634,27.0444969326894));
#60621=CARTESIAN_POINT('Ctrl Pts',(1.47131413783779,2.73351943476633,26.9914470665582));
#60622=CARTESIAN_POINT('Ctrl Pts',(2.34043644702647,2.03942419076481,26.938397200427));
#60623=CARTESIAN_POINT('Ctrl Pts',(2.71778006804373,1.13919341385949,26.8853473342958));
#60624=CARTESIAN_POINT('Ctrl Pts',(3.09512368906099,0.238962636954171,26.8322974681646));
#60625=CARTESIAN_POINT('Ctrl Pts',(2.98068862190676,-0.86740367285492,26.7792476020334));
#60626=CARTESIAN_POINT('Ctrl Pts',(2.42707716940252,-1.6713427375023,26.7261977359022));
#60627=CARTESIAN_POINT('Ctrl Pts',(1.87346571689831,-2.47528180214964,26.6731478697711));
#60628=CARTESIAN_POINT('Ctrl Pts',(0.880677879044135,-2.97679362163533,
26.6200980036398));
#60629=CARTESIAN_POINT('Ctrl Pts',(-0.0949321182835713,-2.94534854055591,
26.5670481375087));
#60630=CARTESIAN_POINT('Ctrl Pts',(-1.07054211561136,-2.91390345947649,
26.5139982713775));
#60631=CARTESIAN_POINT('Ctrl Pts',(-2.0289742724127,-2.34950147783184,26.4609484052463));
#60632=CARTESIAN_POINT('Ctrl Pts',(-2.52966661935728,-1.51158093641926,
26.4078985391151));
#60633=CARTESIAN_POINT('Ctrl Pts',(-2.79935351208561,-1.06025351241171,
26.3793243984399));
#60634=CARTESIAN_POINT('Ctrl Pts',(-2.93624089950528,-0.529572864918339,
26.3507502577648));
#60635=CARTESIAN_POINT('Ctrl Pts',(-2.93724345526557,0.000625155175501269,
26.3221761170896));
#60636=CARTESIAN_POINT('Ctrl Pts',(-2.94570126337859,0.00159745694066759,
26.1778238829105));
#60637=CARTESIAN_POINT('Ctrl Pts',(-2.93992748904903,-0.8787074327395,26.2256158458912));
#60638=CARTESIAN_POINT('Ctrl Pts',(-2.51913195498579,-1.76380189917085,
26.273407808872));
#60639=CARTESIAN_POINT('Ctrl Pts',(-1.82977959360776,-2.30987579829058,
26.3211997718528));
#60640=CARTESIAN_POINT('Ctrl Pts',(-1.0674149663818,-2.91378672666985,26.3740535866557));
#60641=CARTESIAN_POINT('Ctrl Pts',(0.0234071261477989,-3.10305976504139,
26.4269074014586));
#60642=CARTESIAN_POINT('Ctrl Pts',(0.944657065598613,-2.79127974110918,
26.4797612162615));
#60643=CARTESIAN_POINT('Ctrl Pts',(1.86590700504943,-2.47949971717697,26.5326150310644));
#60644=CARTESIAN_POINT('Ctrl Pts',(2.61758479142146,-1.66666663094102,26.5854688458673));
#60645=CARTESIAN_POINT('Ctrl Pts',(2.85650173825782,-0.723890450304441,
26.6383226606703));
#60646=CARTESIAN_POINT('Ctrl Pts',(3.09541868509418,0.218885730332135,26.6911764754732));
#60647=CARTESIAN_POINT('Ctrl Pts',(2.82157479239486,1.29160500536933,26.7440302902761));
#60648=CARTESIAN_POINT('Ctrl Pts',(2.15999720281805,2.00450284323323,26.796884105079));
#60649=CARTESIAN_POINT('Ctrl Pts',(1.49841961324124,2.71740068109714,26.8497379198819));
#60650=CARTESIAN_POINT('Ctrl Pts',(0.449108326786933,3.07047708178776,26.9025917346849));
#60651=CARTESIAN_POINT('Ctrl Pts',(-0.508859359581332,2.90253022669505,
26.9554455494878));
#60652=CARTESIAN_POINT('Ctrl Pts',(-1.4668270459496,2.73458337160234,27.0082993642907));
#60653=CARTESIAN_POINT('Ctrl Pts',(-2.33345113223182,2.0456132607263,27.0611531790936));
#60654=CARTESIAN_POINT('Ctrl Pts',(-2.7130626400236,1.15017854093185,27.1140069938965));
#60655=CARTESIAN_POINT('Ctrl Pts',(-2.86584647440086,0.789789176761778,
27.1352792902345));
#60656=CARTESIAN_POINT('Ctrl Pts',(-2.9397413453216,0.395955545015464,27.1565515865725));
#60657=CARTESIAN_POINT('Ctrl Pts',(-2.9379441153396,0.0014763941512189,
27.1778238829104));
#60658=CARTESIAN_POINT('Origin',(0.,0.,0.));
#60659=CARTESIAN_POINT('',(-2.94676864247139,0.000515229547840817,28.3221761170896));
#60660=CARTESIAN_POINT('',(-2.94035116299482,-0.00254728619478539,28.1778238829105));
#60661=CARTESIAN_POINT('',(-2.942,-3.60291088309151E-16,0.));
#60662=CARTESIAN_POINT('Ctrl Pts',(-2.94676864247139,0.000515229547840817,
28.3221761170896));
#60663=CARTESIAN_POINT('Ctrl Pts',(-2.94683491423248,0.0280099856412504,
28.3206819846724));
#60664=CARTESIAN_POINT('Ctrl Pts',(-2.9464835583305,0.0555030051240508,
28.3191878522552));
#60665=CARTESIAN_POINT('Ctrl Pts',(-2.94570938304831,0.0829841132854057,
28.317693719838));
#60666=CARTESIAN_POINT('Ctrl Pts',(-2.9182219297212,1.05871363519171,28.2646438537068));
#60667=CARTESIAN_POINT('Ctrl Pts',(-2.35771228185992,2.01942729218297,28.2115939875756));
#60668=CARTESIAN_POINT('Ctrl Pts',(-1.52182959338531,2.52351437902251,28.1585441214444));
#60669=CARTESIAN_POINT('Ctrl Pts',(-0.685946904910668,3.02760146586206,
28.1054942553132));
#60670=CARTESIAN_POINT('Ctrl Pts',(0.425308824177326,3.07506198254987,28.052444389182));
#60671=CARTESIAN_POINT('Ctrl Pts',(1.30112729920903,2.6440797801295,27.9993945230508));
#60672=CARTESIAN_POINT('Ctrl Pts',(2.17694577424074,2.21309757770913,27.9463446569197));
#60673=CARTESIAN_POINT('Ctrl Pts',(2.81732699521616,1.30367265618058,27.8932947907884));
#60674=CARTESIAN_POINT('Ctrl Pts',(2.92790728721788,0.333839856657492,27.8402449246573));
#60675=CARTESIAN_POINT('Ctrl Pts',(3.03848757921959,-0.635992942865569,
27.7871950585261));
#60676=CARTESIAN_POINT('Ctrl Pts',(2.61926694224765,-1.66623362038317,27.7341451923949));
#60677=CARTESIAN_POINT('Ctrl Pts',(1.86294829021996,-2.28331202431976,27.6810953262637));
#60678=CARTESIAN_POINT('Ctrl Pts',(1.10662963819224,-2.90039042825636,27.6280454601325));
#60679=CARTESIAN_POINT('Ctrl Pts',(0.0132129711087428,-3.10430655861194,
27.5749955940013));
#60680=CARTESIAN_POINT('Ctrl Pts',(-0.914691487938128,-2.80132640267609,
27.5219457278701));
#60681=CARTESIAN_POINT('Ctrl Pts',(-1.84259594698497,-2.49834624674026,
27.4688958617389));
#60682=CARTESIAN_POINT('Ctrl Pts',(-2.6049881979952,-1.68846980451303,27.4158459956077));
#60683=CARTESIAN_POINT('Ctrl Pts',(-2.85141982464256,-0.74397252373459,
27.3627961294765));
#60684=CARTESIAN_POINT('Ctrl Pts',(-2.91431697190524,-0.502906937443884,
27.3492561253476));
#60685=CARTESIAN_POINT('Ctrl Pts',(-2.9436027991731,-0.253071720547933,
27.3357161212186));
#60686=CARTESIAN_POINT('Ctrl Pts',(-2.94133724676478,-0.0027142933295754,
27.3221761170896));
#60687=CARTESIAN_POINT('Ctrl Pts',(-2.9379441153396,0.0014763941512189,
27.1778238829104));
#60688=CARTESIAN_POINT('Ctrl Pts',(-2.93527589132841,-0.58417972821138,
27.2094054013754));
#60689=CARTESIAN_POINT('Ctrl Pts',(-2.76577241378268,-1.17125865882499,
27.2409869198403));
#60690=CARTESIAN_POINT('Ctrl Pts',(-2.43989484316183,-1.65243236443258,
27.2725684383053));
#60691=CARTESIAN_POINT('Ctrl Pts',(-1.89451660920699,-2.45770922128962,
27.3254222531082));
#60692=CARTESIAN_POINT('Ctrl Pts',(-0.911161211996041,-2.96636360629089,
27.3782760679111));
#60693=CARTESIAN_POINT('Ctrl Pts',(0.0612071071330964,-2.94616246238192,
27.431129882714));
#60694=CARTESIAN_POINT('Ctrl Pts',(1.03357542626229,-2.92596131847296,27.4839836975169));
#60695=CARTESIAN_POINT('Ctrl Pts',(1.99495666730963,-2.3769046456537,27.5368375123199));
#60696=CARTESIAN_POINT('Ctrl Pts',(2.5064191879131,-1.54967171335511,27.5896913271228));
#60697=CARTESIAN_POINT('Ctrl Pts',(3.01788170851653,-0.722438781056572,
27.6425451419257));
#60698=CARTESIAN_POINT('Ctrl Pts',(3.07942550867611,0.38297041072131,27.6953989567286));
#60699=CARTESIAN_POINT('Ctrl Pts',(2.66295193186737,1.26186630562661,27.7482527715315));
#60700=CARTESIAN_POINT('Ctrl Pts',(2.24647835505861,2.14076220053196,27.8011065863344));
#60701=CARTESIAN_POINT('Ctrl Pts',(1.35198740128158,2.79314479856472,27.8539604011373));
#60702=CARTESIAN_POINT('Ctrl Pts',(0.387871045182579,2.92115997799177,27.9068142159403));
#60703=CARTESIAN_POINT('Ctrl Pts',(-0.576245310916365,3.04917515741882,
27.9596680307432));
#60704=CARTESIAN_POINT('Ctrl Pts',(-1.60998706933728,2.6528229182401,28.0125218455461));
#60705=CARTESIAN_POINT('Ctrl Pts',(-2.24138541226995,1.91306324996728,28.065375660349));
#60706=CARTESIAN_POINT('Ctrl Pts',(-2.68915896564396,1.38844227334775,28.1028584012028));
#60707=CARTESIAN_POINT('Ctrl Pts',(-2.93458079833888,0.691110419661017,
28.1403411420566));
#60708=CARTESIAN_POINT('Ctrl Pts',(-2.94035116299482,-0.00254728619478539,
28.1778238829105));
#60709=CARTESIAN_POINT('Origin',(0.,0.,0.));
#60710=CARTESIAN_POINT('',(-2.93977218479318,0.00247205850073318,29.3221761170896));
#60711=CARTESIAN_POINT('',(-2.94676321920776,0.000286364410989904,29.1778238829104));
#60712=CARTESIAN_POINT('',(-2.942,-3.60291088309151E-16,0.));
#60713=CARTESIAN_POINT('Ctrl Pts',(-2.93977218479318,0.00247205850073318,
29.3221761170896));
#60714=CARTESIAN_POINT('Ctrl Pts',(-2.94219100511596,0.308495628903927,
29.3056478481262));
#60715=CARTESIAN_POINT('Ctrl Pts',(-2.89823697117032,0.613841578117692,
29.2891195791628));
#60716=CARTESIAN_POINT('Ctrl Pts',(-2.80501362181614,0.903320936247213,
29.2725913101994));
#60717=CARTESIAN_POINT('Ctrl Pts',(-2.50579981942117,1.8324467406818,29.2195414440682));
#60718=CARTESIAN_POINT('Ctrl Pts',(-1.69902253333613,2.59811782328335,29.166491577937));
#60719=CARTESIAN_POINT('Ctrl Pts',(-0.755532623944009,2.84837858905605,
29.1134417118058));
#60720=CARTESIAN_POINT('Ctrl Pts',(0.187957285448161,3.09863935482876,29.0603918456747));
#60721=CARTESIAN_POINT('Ctrl Pts',(1.26815981814739,2.83348980377255,29.0073419795435));
#60722=CARTESIAN_POINT('Ctrl Pts',(1.98853888476605,2.1748110805792,28.9542921134123));
#60723=CARTESIAN_POINT('Ctrl Pts',(2.7089179513847,1.51613235738584,28.9012422472811));
#60724=CARTESIAN_POINT('Ctrl Pts',(3.06947355192275,0.463924462055363,28.8481923811499));
#60725=CARTESIAN_POINT('Ctrl Pts',(2.90446929669537,-0.498144795205691,
28.7951425150187));
#60726=CARTESIAN_POINT('Ctrl Pts',(2.73946504146801,-1.46021405246669,28.7420926488875));
#60727=CARTESIAN_POINT('Ctrl Pts',(2.04890093047521,-2.33214467165833,28.6890427827563));
#60728=CARTESIAN_POINT('Ctrl Pts',(1.15020817940491,-2.71313679648975,28.6359929166252));
#60729=CARTESIAN_POINT('Ctrl Pts',(0.251515428334551,-3.0941289213212,28.582943050494));
#60730=CARTESIAN_POINT('Ctrl Pts',(-0.855305962813357,-2.98418255179246,
28.5298931843628));
#60731=CARTESIAN_POINT('Ctrl Pts',(-1.66148402899086,-2.43383667361739,
28.4768433182316));
#60732=CARTESIAN_POINT('Ctrl Pts',(-2.4449563492249,-1.89899111009379,28.4252875845176));
#60733=CARTESIAN_POINT('Ctrl Pts',(-2.94448190454346,-0.948204112437949,
28.3737318508036));
#60734=CARTESIAN_POINT('Ctrl Pts',(-2.94676864247139,0.000515229547840817,
28.3221761170896));
#60735=CARTESIAN_POINT('Ctrl Pts',(-2.94035116299482,-0.00254728619478539,
28.1778238829105));
#60736=CARTESIAN_POINT('Ctrl Pts',(-2.94271749746822,-0.287005243355917,
28.1931949568596));
#60737=CARTESIAN_POINT('Ctrl Pts',(-2.90478190263403,-0.570845323032888,
28.2085660308087));
#60738=CARTESIAN_POINT('Ctrl Pts',(-2.82397206139089,-0.841903415598018,
28.2239371047578));
#60739=CARTESIAN_POINT('Ctrl Pts',(-2.54610544013462,-1.7739433155234,28.2767909195607));
#60740=CARTESIAN_POINT('Ctrl Pts',(-1.76131727017756,-2.55485601800717,
28.3296447343636));
#60741=CARTESIAN_POINT('Ctrl Pts',(-0.827913232594077,-2.82810523920302,
28.3824985491665));
#60742=CARTESIAN_POINT('Ctrl Pts',(0.10549080498941,-3.10135446039886,28.4353523639694));
#60743=CARTESIAN_POINT('Ctrl Pts',(1.18751071019935,-2.86694020030677,28.4882061787723));
#60744=CARTESIAN_POINT('Ctrl Pts',(1.92413562263573,-2.23188746813457,28.5410599935753));
#60745=CARTESIAN_POINT('Ctrl Pts',(2.66076053507213,-1.59683473596234,28.5939138083782));
#60746=CARTESIAN_POINT('Ctrl Pts',(3.05199045473495,-0.561143531710042,
28.6467676231811));
#60747=CARTESIAN_POINT('Ctrl Pts',(2.91920405654855,0.402327280882647,28.699621437984));
#60748=CARTESIAN_POINT('Ctrl Pts',(2.78641765836215,1.36579809347531,28.7524752527869));
#60749=CARTESIAN_POINT('Ctrl Pts',(2.12961494232652,2.25704851440832,28.8053290675899));
#60750=CARTESIAN_POINT('Ctrl Pts',(1.24866809498787,2.66916607824828,28.8581828823928));
#60751=CARTESIAN_POINT('Ctrl Pts',(0.367721247649218,3.08128364208823,28.9110366971957));
#60752=CARTESIAN_POINT('Ctrl Pts',(-0.737369730992477,3.01426834883514,
28.9638905119986));
#60753=CARTESIAN_POINT('Ctrl Pts',(-1.5620605691078,2.4987169393812,29.0167443268015));
#60754=CARTESIAN_POINT('Ctrl Pts',(-2.38675140722314,1.98316552992725,29.0695981416044));
#60755=CARTESIAN_POINT('Ctrl Pts',(-2.93104210481211,1.01907800427242,29.1224519564074));
#60756=CARTESIAN_POINT('Ctrl Pts',(-2.94642936306387,0.0466215957147753,
29.1753057712103));
#60757=CARTESIAN_POINT('Ctrl Pts',(-2.94667372786,0.0311780314270079,29.176145141777));
#60758=CARTESIAN_POINT('Ctrl Pts',(-2.94678470022545,0.0157323564597679,
29.1769845123437));
#60759=CARTESIAN_POINT('Ctrl Pts',(-2.94676321920776,0.000286364410989904,
29.1778238829104));
#60760=CARTESIAN_POINT('Origin',(0.,0.,0.));
#60761=CARTESIAN_POINT('',(-2.93783810979555,-0.00147013671584123,30.3221761170896));
#60762=CARTESIAN_POINT('',(-2.93953450219412,0.00234327334966803,30.1778238829105));
#60763=CARTESIAN_POINT('',(-2.942,-3.60291088309151E-16,0.));
#60764=CARTESIAN_POINT('Ctrl Pts',(-2.93783810979555,-0.00147013671584123,
30.3221761170896));
#60765=CARTESIAN_POINT('Ctrl Pts',(-2.93520375456558,0.583879716040712,
30.29061371158));
#60766=CARTESIAN_POINT('Ctrl Pts',(-2.7660401693521,1.17063223301724,30.2590513060705));
#60767=CARTESIAN_POINT('Ctrl Pts',(-2.44055613232114,1.65159798299293,30.2274889005609));
#60768=CARTESIAN_POINT('Ctrl Pts',(-1.89348488367694,2.46000178612405,30.1744390344297));
#60769=CARTESIAN_POINT('Ctrl Pts',(-0.904798249272084,2.96955113115784,
30.1213891682985));
#60770=CARTESIAN_POINT('Ctrl Pts',(0.0710347428950288,2.94602175785218,
30.0683393021673));
#60771=CARTESIAN_POINT('Ctrl Pts',(1.04686773506211,2.92249238454653,30.0152894360361));
#60772=CARTESIAN_POINT('Ctrl Pts',(2.00984708499145,2.36588429290148,29.9622395699049));
#60773=CARTESIAN_POINT('Ctrl Pts',(2.51732061765051,1.5320532106909,29.9091897037737));
#60774=CARTESIAN_POINT('Ctrl Pts',(3.02479415030958,0.698222128480303,29.8561398376426));
#60775=CARTESIAN_POINT('Ctrl Pts',(3.07676186569834,-0.412831944295833,
29.8030899715113));
#60776=CARTESIAN_POINT('Ctrl Pts',(2.64933579337382,-1.29039140821108,29.7500401053801));
#60777=CARTESIAN_POINT('Ctrl Pts',(2.22190972104931,-2.16795087212629,29.6969902392489));
#60778=CARTESIAN_POINT('Ctrl Pts',(1.31508986101154,-2.81201572718063,29.6439403731178));
#60779=CARTESIAN_POINT('Ctrl Pts',(0.345713587226916,-2.92652904445579,
29.5908905069866));
#60780=CARTESIAN_POINT('Ctrl Pts',(-0.623662686557708,-3.04104236173095,
29.5378406408554));
#60781=CARTESIAN_POINT('Ctrl Pts',(-1.65559537408919,-2.62600414122694,
29.4847907747242));
#60782=CARTESIAN_POINT('Ctrl Pts',(-2.27573655850254,-1.87219476784112,
29.431740908593));
#60783=CARTESIAN_POINT('Ctrl Pts',(-2.70266593978139,-1.35324299126101,
29.3952193114252));
#60784=CARTESIAN_POINT('Ctrl Pts',(-2.93442745198144,-0.673731214018755,
29.3586977142574));
#60785=CARTESIAN_POINT('Ctrl Pts',(-2.93977218479318,0.00247205850073318,
29.3221761170896));
#60786=CARTESIAN_POINT('Ctrl Pts',(-2.94676321920776,0.000286364410989904,
29.1778238829104));
#60787=CARTESIAN_POINT('Ctrl Pts',(-2.94543207508477,-0.956876924304651,
29.2298383271466));
#60788=CARTESIAN_POINT('Ctrl Pts',(-2.43546913201457,-1.9152578319996,29.2818527713828));
#60789=CARTESIAN_POINT('Ctrl Pts',(-1.64033359579244,-2.44804519141836,
29.333867215619));
#60790=CARTESIAN_POINT('Ctrl Pts',(-0.832366751354701,-2.98943027853342,
29.386721030422));
#60791=CARTESIAN_POINT('Ctrl Pts',(0.270050756435348,-3.09137516130311,
29.4395748452249));
#60792=CARTESIAN_POINT('Ctrl Pts',(1.16359526511913,-2.70733552108051,29.4924286600278));
#60793=CARTESIAN_POINT('Ctrl Pts',(2.05713977380296,-2.32329588085788,29.5452824748307));
#60794=CARTESIAN_POINT('Ctrl Pts',(2.74181128338049,-1.45327171764289,29.5981362896336));
#60795=CARTESIAN_POINT('Ctrl Pts',(2.90501373170058,-0.494484361070186,
29.6509901044365));
#60796=CARTESIAN_POINT('Ctrl Pts',(3.06821618002067,0.464302995502493,29.7038439192394));
#60797=CARTESIAN_POINT('Ctrl Pts',(2.70994956708335,1.51185354543288,29.7566977340424));
#60798=CARTESIAN_POINT('Ctrl Pts',(1.99378537328151,2.16989387989381,29.8095515488453));
#60799=CARTESIAN_POINT('Ctrl Pts',(1.27762117947965,2.82793421435476,29.8624053636482));
#60800=CARTESIAN_POINT('Ctrl Pts',(0.203559404813244,3.09646433334624,29.9152591784511));
#60801=CARTESIAN_POINT('Ctrl Pts',(-0.738022482733161,2.85288316965352,
29.968112993254));
#60802=CARTESIAN_POINT('Ctrl Pts',(-1.67960437027954,2.6093020059608,30.0209668080569));
#60803=CARTESIAN_POINT('Ctrl Pts',(-2.48870637070592,1.85360955958394,30.0738206228599));
#60804=CARTESIAN_POINT('Ctrl Pts',(-2.79592199393075,0.930827464445613,
30.1266744376628));
#60805=CARTESIAN_POINT('Ctrl Pts',(-2.89502495529665,0.633152374345404,
30.1437242527454));
#60806=CARTESIAN_POINT('Ctrl Pts',(-2.94190127783126,0.318089821395596,
30.1607740678279));
#60807=CARTESIAN_POINT('Ctrl Pts',(-2.93953450219412,0.00234327334966803,
30.1778238829105));
#60808=CARTESIAN_POINT('Origin',(0.,0.,0.));
#60809=CARTESIAN_POINT('',(-2.94517042509113,-0.00197354254748233,31.3221761170896));
#60810=CARTESIAN_POINT('',(-2.93848416988746,-0.00187374481244229,31.1778238829104));
#60811=CARTESIAN_POINT('',(-2.942,-3.60291088309151E-16,0.));
#60812=CARTESIAN_POINT('Ctrl Pts',(-2.94517042509113,-0.00197354254748233,
31.3221761170896));
#60813=CARTESIAN_POINT('Ctrl Pts',(-2.93855277029816,0.856718198839958,
31.2755795750338));
#60814=CARTESIAN_POINT('Ctrl Pts',(-2.54130670618931,1.72073915113778,31.2289830329781));
#60815=CARTESIAN_POINT('Ctrl Pts',(-1.88141044101362,2.26812364849925,31.1823864909223));
#60816=CARTESIAN_POINT('Ctrl Pts',(-1.13012274918965,2.89131740979965,31.1293366247911));
#60817=CARTESIAN_POINT('Ctrl Pts',(-0.0383963406818305,3.10409721392047,
31.0762867586599));
#60818=CARTESIAN_POINT('Ctrl Pts',(0.891935521624298,2.80865468822734,31.0232368925287));
#60819=CARTESIAN_POINT('Ctrl Pts',(1.82226738393048,2.5132121625342,30.9701870263976));
#60820=CARTESIAN_POINT('Ctrl Pts',(2.59120470003495,1.70954730702706,30.9171371602664));
#60821=CARTESIAN_POINT('Ctrl Pts',(2.84529048722843,0.767080292879461,30.8640872941352));
#60822=CARTESIAN_POINT('Ctrl Pts',(3.09937627442189,-0.175386721268062,
30.811037428004));
#60823=CARTESIAN_POINT('Ctrl Pts',(2.83861053270447,-1.25665589405602,30.7579875618728));
#60824=CARTESIAN_POINT('Ctrl Pts',(2.18285930359996,-1.97970083424839,30.7049376957416));
#60825=CARTESIAN_POINT('Ctrl Pts',(1.5271080744954,-2.70274577444079,30.6518878296104));
#60826=CARTESIAN_POINT('Ctrl Pts',(0.476371358003699,-3.06756648203756,
30.5988379634792));
#60827=CARTESIAN_POINT('Ctrl Pts',(-0.486359291616223,-2.90646602799606,
30.545788097348));
#60828=CARTESIAN_POINT('Ctrl Pts',(-1.44908994123612,-2.74536557395456,
30.4927382312169));
#60829=CARTESIAN_POINT('Ctrl Pts',(-2.32381452398424,-2.05834395827482,
30.4396883650856));
#60830=CARTESIAN_POINT('Ctrl Pts',(-2.70844888391655,-1.16120401982074,
30.3866384989544));
#60831=CARTESIAN_POINT('Ctrl Pts',(-2.86424222074291,-0.797824043480206,
30.3651510383328));
#60832=CARTESIAN_POINT('Ctrl Pts',(-2.93963156005239,-0.399972142754944,
30.3436635777112));
#60833=CARTESIAN_POINT('Ctrl Pts',(-2.93783810979555,-0.00147013671584123,
30.3221761170896));
#60834=CARTESIAN_POINT('Ctrl Pts',(-2.93953450219412,0.00234327334966803,
30.1778238829105));
#60835=CARTESIAN_POINT('Ctrl Pts',(-2.93456435830457,-0.660713144752601,
30.2136278826308));
#60836=CARTESIAN_POINT('Ctrl Pts',(-2.71243957464638,-1.32678587811968,
30.2494318823512));
#60837=CARTESIAN_POINT('Ctrl Pts',(-2.30078930455155,-1.84119204342544,
30.2852358820715));
#60838=CARTESIAN_POINT('Ctrl Pts',(-1.69311174592427,-2.60055771225837,
30.3380896968744));
#60839=CARTESIAN_POINT('Ctrl Pts',(-0.67242738264646,-3.02941730602445,
30.3909435116774));
#60840=CARTESIAN_POINT('Ctrl Pts',(0.295256498288523,-2.93196916166087,
30.4437973264803));
#60841=CARTESIAN_POINT('Ctrl Pts',(1.26294037922351,-2.83452101729728,30.4966511412832));
#60842=CARTESIAN_POINT('Ctrl Pts',(2.17762377781566,-2.21076513480403,30.5495049560861));
#60843=CARTESIAN_POINT('Ctrl Pts',(2.62169558491961,-1.34548572074361,30.602358770889));
#60844=CARTESIAN_POINT('Ctrl Pts',(3.06576739202355,-0.480206306683199,
30.6552125856919));
#60845=CARTESIAN_POINT('Ctrl Pts',(3.03922760763929,0.626596638944376,30.7080664004949));
#60846=CARTESIAN_POINT('Ctrl Pts',(2.55419333021886,1.46959722256727,30.7609202152978));
#60847=CARTESIAN_POINT('Ctrl Pts',(2.06915905279841,2.31259780619018,30.8137740301007));
#60848=CARTESIAN_POINT('Ctrl Pts',(1.12563028234178,2.8917960278084,30.8666278449037));
#60849=CARTESIAN_POINT('Ctrl Pts',(0.154387873675291,2.94275108515381,30.9194816597066));
#60850=CARTESIAN_POINT('Ctrl Pts',(-0.816854534991167,2.99370614249923,
30.9723354745095));
#60851=CARTESIAN_POINT('Ctrl Pts',(-1.81581058186747,2.51641803557186,31.0251892893124));
#60852=CARTESIAN_POINT('Ctrl Pts',(-2.38639333745911,1.72879912183073,31.0780431041153));
#60853=CARTESIAN_POINT('Ctrl Pts',(-2.74545409105091,1.23316016685073,31.1113033637137));
#60854=CARTESIAN_POINT('Ctrl Pts',(-2.93487769090008,0.614629248581725,
31.1445636233121));
#60855=CARTESIAN_POINT('Ctrl Pts',(-2.93848416988746,-0.00187374481244229,
31.1778238829104));
#60856=CARTESIAN_POINT('Origin',(0.,0.,0.));
#60857=CARTESIAN_POINT('',(-2.94410448200555,0.00238870800367233,32.3221761170895));
#60858=CARTESIAN_POINT('',(-2.94627736789538,-0.00111514688795235,32.1778238829105));
#60859=CARTESIAN_POINT('',(-2.942,-3.60291088309151E-16,0.));
#60860=CARTESIAN_POINT('Ctrl Pts',(-2.94410448200555,0.00238870800367233,
32.3221761170895));
#60861=CARTESIAN_POINT('Ctrl Pts',(-2.94549825313968,0.160667033072669,
32.3135953046188));
#60862=CARTESIAN_POINT('Ctrl Pts',(-2.93384105715144,0.318739746346453,
32.3050144921481));
#60863=CARTESIAN_POINT('Ctrl Pts',(-2.90841493730487,0.474565785638333,
32.2964336796773));
#60864=CARTESIAN_POINT('Ctrl Pts',(-2.75122093514068,1.4379419871783,32.2433838135461));
#60865=CARTESIAN_POINT('Ctrl Pts',(-2.06775311879117,2.31544614106569,32.190333947415));
#60866=CARTESIAN_POINT('Ctrl Pts',(-1.17218075418514,2.70371640745745,32.1372840812838));
#60867=CARTESIAN_POINT('Ctrl Pts',(-0.276608389579133,3.09198667384919,
32.0842342151526));
#60868=CARTESIAN_POINT('Ctrl Pts',(0.831068523283415,2.99102305274535,32.0311843490214));
#60869=CARTESIAN_POINT('Ctrl Pts',(1.64168476217013,2.44723543495411,31.9781344828902));
#60870=CARTESIAN_POINT('Ctrl Pts',(2.45230100105687,1.90344781716287,31.925084616759));
#60871=CARTESIAN_POINT('Ctrl Pts',(2.96585656596776,0.91683620268427,31.8720347506278));
#60872=CARTESIAN_POINT('Ctrl Pts',(2.94628565982781,-0.0590842037233539,
31.8189848844966));
#60873=CARTESIAN_POINT('Ctrl Pts',(2.92671475368787,-1.03500461013098,31.7659350183654));
#60874=CARTESIAN_POINT('Ctrl Pts',(2.37401737649702,-2.0002338084676,31.7128851522342));
#60875=CARTESIAN_POINT('Ctrl Pts',(1.54225162012017,-2.5110854371513,31.659835286103));
#60876=CARTESIAN_POINT('Ctrl Pts',(0.710485863743306,-3.02193706583501,
31.6067854199718));
#60877=CARTESIAN_POINT('Ctrl Pts',(-0.400348271819595,-3.07841112486583,
31.5537355538407));
#60878=CARTESIAN_POINT('Ctrl Pts',(-1.27963428555693,-2.65454821535866,
31.5006856877095));
#60879=CARTESIAN_POINT('Ctrl Pts',(-2.15892029929426,-2.2306853058515,31.4476358215783));
#60880=CARTESIAN_POINT('Ctrl Pts',(-2.80665819120605,-1.32648542780635,
31.3945859554471));
#60881=CARTESIAN_POINT('Ctrl Pts',(-2.92510264959188,-0.357581629543773,
31.3415360893159));
#60882=CARTESIAN_POINT('Ctrl Pts',(-2.93951098896476,-0.239717991723232,
31.3350827652405));
#60883=CARTESIAN_POINT('Ctrl Pts',(-2.94608692810003,-0.120896875558947,
31.328629441165));
#60884=CARTESIAN_POINT('Ctrl Pts',(-2.94517042509113,-0.00197354254748233,
31.3221761170896));
#60885=CARTESIAN_POINT('Ctrl Pts',(-2.93848416988746,-0.00187374481244229,
31.1778238829104));
#60886=CARTESIAN_POINT('Ctrl Pts',(-2.9406087397491,-0.365054477034348,
31.197417438115));
#60887=CARTESIAN_POINT('Ctrl Pts',(-2.87824797656616,-0.727531445198681,
31.2170109933195));
#60888=CARTESIAN_POINT('Ctrl Pts',(-2.74809407102639,-1.06376620622274,
31.2366045485241));
#60889=CARTESIAN_POINT('Ctrl Pts',(-2.39700258469507,-1.9707628999802,31.289458363327));
#60890=CARTESIAN_POINT('Ctrl Pts',(-1.55261014772547,-2.68680656694023,
31.3423121781299));
#60891=CARTESIAN_POINT('Ctrl Pts',(-0.600435577557133,-2.88497776107816,
31.3951659929328));
#60892=CARTESIAN_POINT('Ctrl Pts',(0.351738992611175,-3.08314895521609,
31.4480198077357));
#60893=CARTESIAN_POINT('Ctrl Pts',(1.41169569597818,-2.76344767653195,31.5008736225387));
#60894=CARTESIAN_POINT('Ctrl Pts',(2.09549692613227,-2.07183787910206,31.5537274373416));
#60895=CARTESIAN_POINT('Ctrl Pts',(2.7792981562864,-1.38022808167213,31.6065812521445));
#60896=CARTESIAN_POINT('Ctrl Pts',(3.08694391322754,-0.31670976549634,31.6594350669474));
#60897=CARTESIAN_POINT('Ctrl Pts',(2.8779743548094,0.633153360388591,31.7122888817503));
#60898=CARTESIAN_POINT('Ctrl Pts',(2.66900479639126,1.5830164862735,31.7651426965532));
#60899=CARTESIAN_POINT('Ctrl Pts',(1.94341992261392,2.41922442186759,31.8179965113562));
#60900=CARTESIAN_POINT('Ctrl Pts',(1.03249534685752,2.75999509481983,31.8708503261591));
#60901=CARTESIAN_POINT('Ctrl Pts',(0.121570771101085,3.10076576777208,31.923704140962));
#60902=CARTESIAN_POINT('Ctrl Pts',(-0.97469350663439,2.94609917808244,31.9765579557649));
#60903=CARTESIAN_POINT('Ctrl Pts',(-1.75578316451228,2.36661045462222,32.0294117705678));
#60904=CARTESIAN_POINT('Ctrl Pts',(-2.48687618959725,1.82421412461807,32.078882474682));
#60905=CARTESIAN_POINT('Ctrl Pts',(-2.94185119889749,0.909639842305583,
32.1283531787962));
#60906=CARTESIAN_POINT('Ctrl Pts',(-2.94627736789538,-0.00111514688795235,
32.1778238829105));
#60907=CARTESIAN_POINT('Origin',(0.,0.,0.));
#60908=CARTESIAN_POINT('',(-2.93736495050316,0.000879932274083783,33.3221761170896));
#60909=CARTESIAN_POINT('',(-2.94171210674826,0.00267199037597989,33.1778238829104));
#60910=CARTESIAN_POINT('',(-2.942,-3.60291088309151E-16,0.));
#60911=CARTESIAN_POINT('Ctrl Pts',(-2.93736495050316,0.000879932274083783,
33.3221761170896));
#60912=CARTESIAN_POINT('Ctrl Pts',(-2.93853387350149,0.439014109857465,
33.2985611680727));
#60913=CARTESIAN_POINT('Ctrl Pts',(-2.84680871230498,0.87668310875137,33.2749462190557));
#60914=CARTESIAN_POINT('Ctrl Pts',(-2.65971696032059,1.26885610824061,33.2513312700388));
#60915=CARTESIAN_POINT('Ctrl Pts',(-2.2394241877252,2.14985420433057,33.1982814039076));
#60916=CARTESIAN_POINT('Ctrl Pts',(-1.33785916906647,2.80125447544335,33.1452315377764));
#60917=CARTESIAN_POINT('Ctrl Pts',(-0.36944378833565,2.92362812609551,33.0921816716452));
#60918=CARTESIAN_POINT('Ctrl Pts',(0.598971592395111,3.04600177674767,33.039131805514));
#60919=CARTESIAN_POINT('Ctrl Pts',(1.63423733519791,2.63934880693927,32.9860819393828));
#60920=CARTESIAN_POINT('Ctrl Pts',(2.26047341956974,1.89059515810641,32.9330320732517));
#60921=CARTESIAN_POINT('Ctrl Pts',(2.88670950394163,1.14184150927349,32.8799822071205));
#60922=CARTESIAN_POINT('Ctrl Pts',(3.10391592988244,0.0509871814159728,
32.8269323409893));
#60923=CARTESIAN_POINT('Ctrl Pts',(2.81224954200074,-0.880535431401397,
32.7738824748581));
#60924=CARTESIAN_POINT('Ctrl Pts',(2.52058315411905,-1.81205804421874,32.7208326087269));
#60925=CARTESIAN_POINT('Ctrl Pts',(1.72004395241494,-2.584248941996,32.6677827425957));
#60926=CARTESIAN_POINT('Ctrl Pts',(0.778615340539899,-2.84215556997019,
32.6147328764645));
#60927=CARTESIAN_POINT('Ctrl Pts',(-0.162813271335088,-3.10006219794436,
32.5616830103333));
#60928=CARTESIAN_POINT('Ctrl Pts',(-1.24513129338095,-2.84368455611553,
32.5086331442021));
#60929=CARTESIAN_POINT('Ctrl Pts',(-1.97083021041444,-2.19087161060488,
32.4555832780709));
#60930=CARTESIAN_POINT('Ctrl Pts',(-2.57914737379974,-1.64365111748691,
32.4111142244105));
#60931=CARTESIAN_POINT('Ctrl Pts',(-2.93688142666368,-0.817870137505501,
32.36664517075));
#60932=CARTESIAN_POINT('Ctrl Pts',(-2.94410448200555,0.00238870800367233,
32.3221761170895));
#60933=CARTESIAN_POINT('Ctrl Pts',(-2.94627736789538,-0.00111514688795235,
32.1778238829105));
#60934=CARTESIAN_POINT('Ctrl Pts',(-2.94658005652525,-0.0633981686056019,
32.1812069935992));
#60935=CARTESIAN_POINT('Ctrl Pts',(-2.94477567931027,-0.125663328770047,
32.1845901042879));
#60936=CARTESIAN_POINT('Ctrl Pts',(-2.94080844994758,-0.187790376294515,
32.1879732149766));
#60937=CARTESIAN_POINT('Ctrl Pts',(-2.87882903948476,-1.15839162652036,
32.2408270297795));
#60938=CARTESIAN_POINT('Ctrl Pts',(-2.28895518053886,-2.09528326974124,
32.2936808445824));
#60939=CARTESIAN_POINT('Ctrl Pts',(-1.4405017823663,-2.57071472157287,32.3465346593853));
#60940=CARTESIAN_POINT('Ctrl Pts',(-0.592048384193733,-3.04614617340449,
32.3993884741882));
#60941=CARTESIAN_POINT('Ctrl Pts',(0.514984553205557,-3.06011743384676,
32.4522422889911));
#60942=CARTESIAN_POINT('Ctrl Pts',(1.3751661303974,-2.60624973448819,32.5050961037941));
#60943=CARTESIAN_POINT('Ctrl Pts',(2.23534770758924,-2.15238203512962,32.557949918597));
#60944=CARTESIAN_POINT('Ctrl Pts',(2.84867792457375,-1.23067537597021,32.6108037333999));
#60945=CARTESIAN_POINT('Ctrl Pts',(2.93513255375312,-0.261947431005922,
32.6636575482028));
#60946=CARTESIAN_POINT('Ctrl Pts',(3.0215871829325,0.706780513958397,32.7165113630057));
#60947=CARTESIAN_POINT('Ctrl Pts',(2.58116622430677,1.72252974472756,32.7693651778086));
#60948=CARTESIAN_POINT('Ctrl Pts',(1.81494983884269,2.32154617597773,32.8222189926116));
#60949=CARTESIAN_POINT('Ctrl Pts',(1.04873345337863,2.92056260722789,32.8750728074145));
#60950=CARTESIAN_POINT('Ctrl Pts',(-0.0432783589237744,3.10284623895901,
32.9279266222174));
#60951=CARTESIAN_POINT('Ctrl Pts',(-0.962512796986673,2.78517300725625,
32.9807804370203));
#60952=CARTESIAN_POINT('Ctrl Pts',(-1.88174723504962,2.46749977555347,33.0336342518232));
#60953=CARTESIAN_POINT('Ctrl Pts',(-2.62820429887308,1.64986968041674,33.0864880666261));
#60954=CARTESIAN_POINT('Ctrl Pts',(-2.86107889367498,0.705582829212486,
33.1393418814291));
#60955=CARTESIAN_POINT('Ctrl Pts',(-2.91759629319511,0.476409538426898,
33.1521692152562));
#60956=CARTESIAN_POINT('Ctrl Pts',(-2.94386334938736,0.239776081870586,
33.1649965490833));
#60957=CARTESIAN_POINT('Ctrl Pts',(-2.94171210674826,0.00267199037597989,
33.1778238829104));
#60958=CARTESIAN_POINT('Origin',(0.,0.,0.));
#60959=CARTESIAN_POINT('',(-2.94086681343003,-0.0026768557490095,34.3221761170896));
#60960=CARTESIAN_POINT('',(-2.93739638408601,-0.000779703272701529,34.1778238829104));
#60961=CARTESIAN_POINT('',(-2.942,-3.60291088309151E-16,0.));
#60962=CARTESIAN_POINT('Ctrl Pts',(-2.94086681343003,-0.0026768557490095,
34.3221761170896));
#60963=CARTESIAN_POINT('Ctrl Pts',(-2.93457120391373,0.712243215688969,
34.2835270315264));
#60964=CARTESIAN_POINT('Ctrl Pts',(-2.67230139772352,1.43129977251953,34.2448779459633));
#60965=CARTESIAN_POINT('Ctrl Pts',(-2.19884786976029,1.96192715921988,34.2062288604002));
#60966=CARTESIAN_POINT('Ctrl Pts',(-1.54898394900133,2.69026811269557,34.153178994269));
#60967=CARTESIAN_POINT('Ctrl Pts',(-0.501241431081312,3.06360095642591,
34.1001291281379));
#60968=CARTESIAN_POINT('Ctrl Pts',(0.462764471317297,2.91031599255435,34.0470792620067));
#60969=CARTESIAN_POINT('Ctrl Pts',(1.42677037371591,2.75703102868279,33.9940293958755));
#60970=CARTESIAN_POINT('Ctrl Pts',(2.30703966059311,2.07712825720934,33.9409795297443));
#60971=CARTESIAN_POINT('Ctrl Pts',(2.69893944497945,1.18313820189125,33.8879296636131));
#60972=CARTESIAN_POINT('Ctrl Pts',(3.09083922936579,0.289148146573163,33.8348797974819));
#60973=CARTESIAN_POINT('Ctrl Pts',(2.99436951126127,-0.818929192589566,
33.7818299313507));
#60974=CARTESIAN_POINT('Ctrl Pts',(2.45387447161704,-1.63174452963146,33.7287800652195));
#60975=CARTESIAN_POINT('Ctrl Pts',(1.91337943197281,-2.44455986667332,33.6757301990883));
#60976=CARTESIAN_POINT('Ctrl Pts',(0.928859070788909,-2.96211320159438,
33.6226803329571));
#60977=CARTESIAN_POINT('Ctrl Pts',(-0.0471326924005423,-2.94650108463293,
33.569630466826));
#60978=CARTESIAN_POINT('Ctrl Pts',(-1.02312445559002,-2.93088896767149,
33.5165806006948));
#60979=CARTESIAN_POINT('Ctrl Pts',(-1.99058762078505,-2.38211139882752,
33.4635307345636));
#60980=CARTESIAN_POINT('Ctrl Pts',(-2.50480894011653,-1.55242465387196,
33.4104808684324));
#60981=CARTESIAN_POINT('Ctrl Pts',(-2.79012656703532,-1.09206985282163,
33.3810459513181));
#60982=CARTESIAN_POINT('Ctrl Pts',(-2.93590794326828,-0.545233599152603,
33.3516110342038));
#60983=CARTESIAN_POINT('Ctrl Pts',(-2.93736495050316,0.000879932274083783,
33.3221761170896));
#60984=CARTESIAN_POINT('Ctrl Pts',(-2.94171210674826,0.00267199037597989,
33.1778238829104));
#60985=CARTESIAN_POINT('Ctrl Pts',(-2.93499935772893,-0.737188882927786,
33.2178503638862));
#60986=CARTESIAN_POINT('Ctrl Pts',(-2.65157963682834,-1.4816322954402,33.257876844862));
#60987=CARTESIAN_POINT('Ctrl Pts',(-2.14711625751622,-2.01829416622589,
33.2979033258378));
#60988=CARTESIAN_POINT('Ctrl Pts',(-1.48098690077514,-2.72694070318839,
33.3507571406407));
#60989=CARTESIAN_POINT('Ctrl Pts',(-0.429436061512542,-3.07329016984171,
33.4036109554436));
#60990=CARTESIAN_POINT('Ctrl Pts',(0.527436465104114,-2.89921202053081,
33.4564647702466));
#60991=CARTESIAN_POINT('Ctrl Pts',(1.4843089917208,-2.72513387121991,33.5093185850495));
#60992=CARTESIAN_POINT('Ctrl Pts',(2.34650320569153,-2.03062810594474,33.5621723998524));
#60993=CARTESIAN_POINT('Ctrl Pts',(2.72037264688675,-1.13278074965211,33.6150262146553));
#60994=CARTESIAN_POINT('Ctrl Pts',(3.09424208808199,-0.234933393359419,
33.6678800294583));
#60995=CARTESIAN_POINT('Ctrl Pts',(2.97978675650164,0.866255553950765,33.7207338442612));
#60996=CARTESIAN_POINT('Ctrl Pts',(2.42926278584456,1.66802334576665,33.7735876590641));
#60997=CARTESIAN_POINT('Ctrl Pts',(1.8787388151875,2.46979113758252,33.826441473867));
#60998=CARTESIAN_POINT('Ctrl Pts',(0.892146205453725,2.9721377739041,33.8792952886699));
#60999=CARTESIAN_POINT('Ctrl Pts',(-0.0800728087435554,2.94571008587262,
33.9321491034728));
#61000=CARTESIAN_POINT('Ctrl Pts',(-1.05229182294078,2.91928239784113,33.9850029182758));
#61001=CARTESIAN_POINT('Ctrl Pts',(-2.01013724160151,2.36408038545666,34.0378567330786));
#61002=CARTESIAN_POINT('Ctrl Pts',(-2.51629175002141,1.53358905626203,34.0907105478816));
#61003=CARTESIAN_POINT('Ctrl Pts',(-2.79437200738008,1.07731880930218,34.1197483262245));
#61004=CARTESIAN_POINT('Ctrl Pts',(-2.93611472733982,0.537955751140718,
34.1487861045675));
#61005=CARTESIAN_POINT('Ctrl Pts',(-2.93739638408601,-0.000779703272701529,
34.1778238829104));
#61006=CARTESIAN_POINT('Origin',(0.,0.,0.));
#61007=CARTESIAN_POINT('',(-2.94685781061061,0.00021972601725095,35.3221761170896));
#61008=CARTESIAN_POINT('',(-2.94455392252949,-0.00218017528262053,35.1778238829104));
#61009=CARTESIAN_POINT('',(-2.942,-3.60291088309151E-16,0.));
#61010=CARTESIAN_POINT('Ctrl Pts',(-2.94685781061061,0.00021972601725095,
35.3221761170896));
#61011=CARTESIAN_POINT('Ctrl Pts',(-2.9468702780931,0.0118736808740626,
35.3215427611115));
#61012=CARTESIAN_POINT('Ctrl Pts',(-2.94680715351256,0.0235274968392718,
35.3209094051333));
#61013=CARTESIAN_POINT('Ctrl Pts',(-2.94666802890093,0.0351804054366583,
35.3202760491553));
#61014=CARTESIAN_POINT('Ctrl Pts',(-2.93501495815129,1.01122746665534,35.2672261830241));
#61015=CARTESIAN_POINT('Ctrl Pts',(-2.39016622670584,1.9809086806671,35.2141763168929));
#61016=CARTESIAN_POINT('Ctrl Pts',(-1.56257214446959,2.49849122988862,35.1611264507617));
#61017=CARTESIAN_POINT('Ctrl Pts',(-0.734978062233343,3.01607377911014,
35.1080765846305));
#61018=CARTESIAN_POINT('Ctrl Pts',(0.375361370793731,3.08155766354144,35.0550267184993));
#61019=CARTESIAN_POINT('Ctrl Pts',(1.25805705355367,2.66484194317754,35.0019768523681));
#61020=CARTESIAN_POINT('Ctrl Pts',(2.14075273631365,2.24812622281361,34.9489269862369));
#61021=CARTESIAN_POINT('Ctrl Pts',(2.79580466880647,1.3492108976545,34.8958771201057));
#61022=CARTESIAN_POINT('Ctrl Pts',(2.92210549825361,0.381299868446144,34.8428272539745));
#61023=CARTESIAN_POINT('Ctrl Pts',(3.04840632770075,-0.586611160762127,
34.7897773878434));
#61024=CARTESIAN_POINT('Ctrl Pts',(2.64595605410225,-1.62351789401957,34.7367275217122));
#61025=CARTESIAN_POINT('Ctrl Pts',(1.89974876798349,-2.25278599759881,34.683677655581));
#61026=CARTESIAN_POINT('Ctrl Pts',(1.15354148186467,-2.8820541011781,34.6306277894498));
#61027=CARTESIAN_POINT('Ctrl Pts',(0.0635771832255068,-3.10368357507913,
34.5775779233186));
#61028=CARTESIAN_POINT('Ctrl Pts',(-0.869120853144318,-2.81579812398257,
34.5245280571874));
#61029=CARTESIAN_POINT('Ctrl Pts',(-1.80181888951409,-2.52791267288603,
34.4714781910562));
#61030=CARTESIAN_POINT('Ctrl Pts',(-2.57725066361456,-1.73051229679197,
34.418428324925));
#61031=CARTESIAN_POINT('Ctrl Pts',(-2.83897388886586,-0.790137577134433,
34.3653784587938));
#61032=CARTESIAN_POINT('Ctrl Pts',(-2.91002060417886,-0.534865868133838,
34.3509776782257));
#61033=CARTESIAN_POINT('Ctrl Pts',(-2.94321257892139,-0.269058502882331,
34.3365768976577));
#61034=CARTESIAN_POINT('Ctrl Pts',(-2.94086681343003,-0.0026768557490095,
34.3221761170896));
#61035=CARTESIAN_POINT('Ctrl Pts',(-2.93739638408601,-0.000779703272701529,
34.1778238829104));
#61036=CARTESIAN_POINT('Ctrl Pts',(-2.93844756587532,-0.442636620597825,
34.2016399193704));
#61037=CARTESIAN_POINT('Ctrl Pts',(-2.84501259774457,-0.88407135785061,
34.2254559558304));
#61038=CARTESIAN_POINT('Ctrl Pts',(-2.65481645025957,-1.27889373293584,
34.2492719922903));
#61039=CARTESIAN_POINT('Ctrl Pts',(-2.23272304389876,-2.15510454693423,
34.3021258070933));
#61040=CARTESIAN_POINT('Ctrl Pts',(-1.33407263299811,-2.80174552892622,
34.3549796218961));
#61041=CARTESIAN_POINT('Ctrl Pts',(-0.369156248756929,-2.92358396984159,
34.4078334366991));
#61042=CARTESIAN_POINT('Ctrl Pts',(0.595760135484311,-3.04542241075698,
34.460687251502));
#61043=CARTESIAN_POINT('Ctrl Pts',(1.6269424930661,-2.64245831059566,34.5135410663049));
#61044=CARTESIAN_POINT('Ctrl Pts',(2.25359053533617,-1.89867039365946,34.5663948811079));
#61045=CARTESIAN_POINT('Ctrl Pts',(2.88023857760625,-1.15488247672325,34.6192486959108));
#61046=CARTESIAN_POINT('Ctrl Pts',(3.10235230456463,-0.0702707430121562,
34.6721025107136));
#61047=CARTESIAN_POINT('Ctrl Pts',(2.81852268221,0.859970612622888,34.7249563255166));
#61048=CARTESIAN_POINT('Ctrl Pts',(2.53469305985538,1.79021196825791,34.7778101403195));
#61049=CARTESIAN_POINT('Ctrl Pts',(1.7449200881878,2.56608294581688,34.8306639551225));
#61050=CARTESIAN_POINT('Ctrl Pts',(0.809785327091873,2.83334912934047,34.8835177699254));
#61051=CARTESIAN_POINT('Ctrl Pts',(-0.125349434004051,3.10061531286405,
34.9363715847283));
#61052=CARTESIAN_POINT('Ctrl Pts',(-1.20584598452831,2.85927670235226,34.9892253995312));
#61053=CARTESIAN_POINT('Ctrl Pts',(-1.93838897230708,2.21951971308571,35.0420792143341));
#61054=CARTESIAN_POINT('Ctrl Pts',(-2.56552002213284,1.67182288299433,35.0873274371928));
#61055=CARTESIAN_POINT('Ctrl Pts',(-2.93763258542781,0.832121421151534,
35.1325756600516));
#61056=CARTESIAN_POINT('Ctrl Pts',(-2.94455392252949,-0.00218017528262053,
35.1778238829104));
#61057=CARTESIAN_POINT('Origin',(0.,0.,0.));
#61058=CARTESIAN_POINT('',(-2.9402011249149,0.00257356892240088,36.3221761170896));
#61059=CARTESIAN_POINT('',(-2.94404018584088,0.00235134841817481,36.1778238829104));
#61060=CARTESIAN_POINT('',(-2.942,-3.60291088309151E-16,0.));
#61061=CARTESIAN_POINT('Ctrl Pts',(-2.9402011249149,0.00257356892240088,
36.3221761170896));
#61062=CARTESIAN_POINT('Ctrl Pts',(-2.94261307060905,0.292552802751825,
36.3065086245653));
#61063=CARTESIAN_POINT('Ctrl Pts',(-2.90320504514716,0.581890802336307,
36.290841132041));
#61064=CARTESIAN_POINT('Ctrl Pts',(-2.81930038436528,0.857691968114813,
36.2751736395167));
#61065=CARTESIAN_POINT('Ctrl Pts',(-2.53520061438846,1.79155007595818,36.2221237733855));
#61066=CARTESIAN_POINT('Ctrl Pts',(-1.74095216738676,2.57020998044168,36.1690739072543));
#61067=CARTESIAN_POINT('Ctrl Pts',(-0.801646808582714,2.83574549969904,
36.1160240411231));
#61068=CARTESIAN_POINT('Ctrl Pts',(0.13765855022133,3.1012810189564,36.0629741749919));
#61069=CARTESIAN_POINT('Ctrl Pts',(1.22202082082772,2.85369215298764,36.0099243088607));
#61070=CARTESIAN_POINT('Ctrl Pts',(1.95299182479538,2.20678794802801,35.9568744427296));
#61071=CARTESIAN_POINT('Ctrl Pts',(2.68396282876302,1.55988374306839,35.9038245765984));
#61072=CARTESIAN_POINT('Ctrl Pts',(3.06154256609195,0.513664199117923,35.8507747104672));
#61073=CARTESIAN_POINT('Ctrl Pts',(2.91216916370067,-0.450955541884665,
35.797724844336));
#61074=CARTESIAN_POINT('Ctrl Pts',(2.76279576130938,-1.41557528288728,35.7446749782048));
#61075=CARTESIAN_POINT('Ctrl Pts',(2.0864692191978,-2.29859522094207,35.6916251120736));
#61076=CARTESIAN_POINT('Ctrl Pts',(1.19407618200127,-2.69411807557552,35.6385752459424));
#61077=CARTESIAN_POINT('Ctrl Pts',(0.301683144804796,-3.08964093020895,
35.5855253798112));
#61078=CARTESIAN_POINT('Ctrl Pts',(-0.80677638747653,-2.99766670142119,
35.53247551368));
#61079=CARTESIAN_POINT('Ctrl Pts',(-1.62177744859037,-2.46047313281454,
35.4794256475489));
#61080=CARTESIAN_POINT('Ctrl Pts',(-2.4270483099534,-1.92969305368267,35.4270091373957));
#61081=CARTESIAN_POINT('Ctrl Pts',(-2.94582600236185,-0.964261014983614,
35.3745926272426));
#61082=CARTESIAN_POINT('Ctrl Pts',(-2.94685781061061,0.00021972601725095,
35.3221761170896));
#61083=CARTESIAN_POINT('Ctrl Pts',(-2.94455392252949,-0.00218017528262053,
35.1778238829104));
#61084=CARTESIAN_POINT('Ctrl Pts',(-2.94571730226857,-0.142414577871742,
35.1854294748546));
#61085=CARTESIAN_POINT('Ctrl Pts',(-2.93656297186098,-0.282496418618953,
35.1930350667987));
#61086=CARTESIAN_POINT('Ctrl Pts',(-2.91656773022714,-0.421013348566901,
35.2006406587428));
#61087=CARTESIAN_POINT('Ctrl Pts',(-2.77761407533517,-1.38361405293164,
35.2534944735458));
#61088=CARTESIAN_POINT('Ctrl Pts',(-2.11511734051801,-2.27064009363985,
35.3063482883487));
#61089=CARTESIAN_POINT('Ctrl Pts',(-1.23154939376283,-2.67710770336558,
35.3592021031516));
#61090=CARTESIAN_POINT('Ctrl Pts',(-0.347981447007576,-3.08357531309134,
35.4120559179545));
#61091=CARTESIAN_POINT('Ctrl Pts',(0.756657711685735,-3.00948449183453,
35.4649097327574));
#61092=CARTESIAN_POINT('Ctrl Pts',(1.57803009492198,-2.4886624086851,35.5177635475603));
#61093=CARTESIAN_POINT('Ctrl Pts',(2.39940247815818,-1.9678403255357,35.5706173623633));
#61094=CARTESIAN_POINT('Ctrl Pts',(2.93750808593735,-1.00028698049375,35.6234711771662));
#61095=CARTESIAN_POINT('Ctrl Pts',(2.94666750624564,-0.0277519738104105,
35.6763249919691));
#61096=CARTESIAN_POINT('Ctrl Pts',(2.95582692655392,0.944783032872932,35.729178806772));
#61097=CARTESIAN_POINT('Ctrl Pts',(2.43604015939132,1.92229970119767,35.7820326215749));
#61098=CARTESIAN_POINT('Ctrl Pts',(1.62462290152057,2.4584995408919,35.8348864363779));
#61099=CARTESIAN_POINT('Ctrl Pts',(0.813205643649837,2.99469938058611,35.8877402511808));
#61100=CARTESIAN_POINT('Ctrl Pts',(-0.289842104929023,3.08958239164985,
35.9405940659837));
#61101=CARTESIAN_POINT('Ctrl Pts',(-1.18090893615386,2.69982844831109,35.9934478807866));
#61102=CARTESIAN_POINT('Ctrl Pts',(-2.07197576737872,2.31007450497232,36.0463016955895));
#61103=CARTESIAN_POINT('Ctrl Pts',(-2.75106168124954,1.43568360723102,36.0991555103924));
#61104=CARTESIAN_POINT('Ctrl Pts',(-2.90812079627098,0.475870777375731,
36.1520093251953));
#61105=CARTESIAN_POINT('Ctrl Pts',(-2.93369076761249,0.319608681099053,
36.160614177767));
#61106=CARTESIAN_POINT('Ctrl Pts',(-2.945424215324,0.161082443240333,36.1692190303387));
#61107=CARTESIAN_POINT('Ctrl Pts',(-2.94404018584088,0.00235134841817481,
36.1778238829104));
#61108=CARTESIAN_POINT('Origin',(0.,0.,0.));
#61109=CARTESIAN_POINT('',(-2.93761702632781,-0.00123893643864781,37.3221761170896));
#61110=CARTESIAN_POINT('',(-2.93727713413294,0.00048555243809314,37.1778238829104));
#61111=CARTESIAN_POINT('',(-2.942,-3.60291088309151E-16,0.));
#61112=CARTESIAN_POINT('Ctrl Pts',(-2.93761702632781,-0.00123893643864781,
37.3221761170896));
#61113=CARTESIAN_POINT('Ctrl Pts',(-2.93546619409942,0.568253609984608,
37.2914744880191));
#61114=CARTESIAN_POINT('Ctrl Pts',(-2.77600657644893,1.13885954810213,37.2607728589486));
#61115=CARTESIAN_POINT('Ctrl Pts',(-2.4670317237215,1.61178336717249,37.2300712298781));
#61116=CARTESIAN_POINT('Ctrl Pts',(-1.93314882983744,2.42895646356918,37.177021363747));
#61117=CARTESIAN_POINT('Ctrl Pts',(-0.952858734605018,2.95448034199031,
37.1239714976158));
#61118=CARTESIAN_POINT('Ctrl Pts',(0.0232277563561131,2.94678665544818,
37.0709216314846));
#61119=CARTESIAN_POINT('Ctrl Pts',(0.999314247317216,2.93909296890604,37.0178717653534));
#61120=CARTESIAN_POINT('Ctrl Pts',(1.97119713400707,2.39818171740062,36.9648218992222));
#61121=CARTESIAN_POINT('Ctrl Pts',(2.49213229674678,1.57269383816965,36.911772033091));
#61122=CARTESIAN_POINT('Ctrl Pts',(3.01306745948649,0.747205958938681,36.8587221669598));
#61123=CARTESIAN_POINT('Ctrl Pts',(3.08305489827613,-0.362858548017857,
36.8056723008286));
#61124=CARTESIAN_POINT('Ctrl Pts',(2.6699231391851,-1.24723725369426,36.7526224346974));
#61125=CARTESIAN_POINT('Ctrl Pts',(2.25679138009406,-2.13161595937069,36.6995725685662));
#61126=CARTESIAN_POINT('Ctrl Pts',(1.36054042312233,-2.79030886376693,36.646522702435));
#61127=CARTESIAN_POINT('Ctrl Pts',(0.393149643570355,-2.92053481496036,
36.5934728363039));
#61128=CARTESIAN_POINT('Ctrl Pts',(-0.574241135981621,-3.05076076615379,
36.5404229701727));
#61129=CARTESIAN_POINT('Ctrl Pts',(-1.61277173811382,-2.65251976414439,
36.4873731040414));
#61130=CARTESIAN_POINT('Ctrl Pts',(-2.24506149270394,-1.90887110753806,
36.4343232379103));
#61131=CARTESIAN_POINT('Ctrl Pts',(-2.69061382973445,-1.38484807146129,
36.3969408643033));
#61132=CARTESIAN_POINT('Ctrl Pts',(-2.93444626306201,-0.689312005010758,
36.3595584906965));
#61133=CARTESIAN_POINT('Ctrl Pts',(-2.9402011249149,0.00257356892240088,
36.3221761170896));
#61134=CARTESIAN_POINT('Ctrl Pts',(-2.94404018584088,0.00235134841817481,
36.1778238829104));
#61135=CARTESIAN_POINT('Ctrl Pts',(-2.93692305422064,-0.813895782045558,
36.2220728451417));
#61136=CARTESIAN_POINT('Ctrl Pts',(-2.58293361510877,-1.63556005229609,
36.2663218073729));
#61137=CARTESIAN_POINT('Ctrl Pts',(-1.97984868768892,-2.18261740561111,
36.3105707696041));
#61138=CARTESIAN_POINT('Ctrl Pts',(-1.25948514791341,-2.83605799677329,
36.363424584407));
#61139=CARTESIAN_POINT('Ctrl Pts',(-0.183725752190359,-3.09770441712838,
36.4162783992099));
#61140=CARTESIAN_POINT('Ctrl Pts',(0.756276955239686,-2.84809844254033,
36.4691322140128));
#61141=CARTESIAN_POINT('Ctrl Pts',(1.69627966266973,-2.59849246795229,36.5219860288158));
#61142=CARTESIAN_POINT('Ctrl Pts',(2.50052568180677,-1.83763409842111,36.5748398436187));
#61143=CARTESIAN_POINT('Ctrl Pts',(2.80182559496105,-0.912903545632631,
36.6276936584216));
#61144=CARTESIAN_POINT('Ctrl Pts',(3.10312550811534,0.011827007155906,36.6805474732246));
#61145=CARTESIAN_POINT('Ctrl Pts',(2.90147931528681,1.10042974320177,36.7334012880274));
#61146=CARTESIAN_POINT('Ctrl Pts',(2.28895130441658,1.85588833190484,36.7862551028303));
#61147=CARTESIAN_POINT('Ctrl Pts',(1.67642329354638,2.61134692060786,36.8391089176332));
#61148=CARTESIAN_POINT('Ctrl Pts',(0.653013464634534,3.03366136196813,36.8919627324362));
#61149=CARTESIAN_POINT('Ctrl Pts',(-0.314026516870114,2.93001825100472,
36.9448165472391));
#61150=CARTESIAN_POINT('Ctrl Pts',(-1.28106649837473,2.82637514004131,36.997670362042));
#61151=CARTESIAN_POINT('Ctrl Pts',(-2.19173663247216,2.19677447675427,37.0505241768449));
#61152=CARTESIAN_POINT('Ctrl Pts',(-2.63025817789325,1.32866901980392,37.1033779916479));
#61153=CARTESIAN_POINT('Ctrl Pts',(-2.83614761973355,0.921086428124407,
37.1281932887354));
#61154=CARTESIAN_POINT('Ctrl Pts',(-2.93795761448107,0.460928338712189,
37.1530085858229));
#61155=CARTESIAN_POINT('Ctrl Pts',(-2.93727713413294,0.00048555243809314,
37.1778238829104));
#61156=CARTESIAN_POINT('Origin',(0.,0.,0.));
#61157=CARTESIAN_POINT('',(-2.94471098031246,-0.00212455505907094,38.3221761170895));
#61158=CARTESIAN_POINT('',(-2.9422704459833,-0.00265502083472174,38.1778238829104));
#61159=CARTESIAN_POINT('',(-2.942,-3.60291088309151E-16,0.));
#61160=CARTESIAN_POINT('Ctrl Pts',(-2.94471098031246,-0.00212455505907094,
38.3221761170895));
#61161=CARTESIAN_POINT('Ctrl Pts',(-2.93776546270216,0.841018236135255,
38.2764403514729));
#61162=CARTESIAN_POINT('Ctrl Pts',(-2.55687059036142,1.68958573147536,38.2307045858562));
#61163=CARTESIAN_POINT('Ctrl Pts',(-1.91798197858352,2.23728479977708,38.1849688202396));
#61164=CARTESIAN_POINT('Ctrl Pts',(-1.17692178486893,2.87257234469591,38.1319189541084));
#61165=CARTESIAN_POINT('Ctrl Pts',(-0.0887526147754901,3.10306661066995,
38.0788690879772));
#61166=CARTESIAN_POINT('Ctrl Pts',(0.846259422451992,2.82276424963368,38.025819221846));
#61167=CARTESIAN_POINT('Ctrl Pts',(1.78127145967947,2.54246188859742,37.9727693557148));
#61168=CARTESIAN_POINT('Ctrl Pts',(2.56312636404104,1.75136290055085,37.9197194895836));
#61169=CARTESIAN_POINT('Ctrl Pts',(2.83246497394273,0.813138660625782,37.8666696234524));
#61170=CARTESIAN_POINT('Ctrl Pts',(3.10180358384444,-0.125085579299313,
37.8136197573212));
#61171=CARTESIAN_POINT('Ctrl Pts',(2.8586258992863,-1.21043507110287,37.7605698911901));
#61172=CARTESIAN_POINT('Ctrl Pts',(2.21469458797494,-1.94402216064632,37.7075200250589));
#61173=CARTESIAN_POINT('Ctrl Pts',(1.57076327666364,-2.67760925018972,37.6544701589277));
#61174=CARTESIAN_POINT('Ctrl Pts',(0.526078338599165,-3.05943393747302,
37.6014202927965));
#61175=CARTESIAN_POINT('Ctrl Pts',(-0.439140697634978,-2.9139755699834,
37.5483704266653));
#61176=CARTESIAN_POINT('Ctrl Pts',(-1.40435973386915,-2.76851720249378,
37.4953205605341));
#61177=CARTESIAN_POINT('Ctrl Pts',(-2.29011286827302,-2.09577578023121,
37.4422706944029));
#61178=CARTESIAN_POINT('Ctrl Pts',(-2.68925158920712,-1.20499391191384,
37.3892208282717));
#61179=CARTESIAN_POINT('Ctrl Pts',(-2.85739615593405,-0.829735578305169,
37.366872591211));
#61180=CARTESIAN_POINT('Ctrl Pts',(-2.93918265362425,-0.415782229974393,
37.3445243541503));
#61181=CARTESIAN_POINT('Ctrl Pts',(-2.93761702632781,-0.00123893643864781,
37.3221761170896));
#61182=CARTESIAN_POINT('Ctrl Pts',(-2.93727713413294,0.00048555243809314,
37.1778238829104));
#61183=CARTESIAN_POINT('Ctrl Pts',(-2.93650826724294,-0.519763436495626,
37.2058624006258));
#61184=CARTESIAN_POINT('Ctrl Pts',(-2.80489514815729,-1.04037588308685,
37.2339009183412));
#61185=CARTESIAN_POINT('Ctrl Pts',(-2.54472982091734,-1.48592388881374,
37.2619394360566));
#61186=CARTESIAN_POINT('Ctrl Pts',(-2.05430696177559,-2.32580108986735,
37.3147932508595));
#61187=CARTESIAN_POINT('Ctrl Pts',(-1.10708828674735,-2.89894524136082,
37.3676470656625));
#61188=CARTESIAN_POINT('Ctrl Pts',(-0.13553953614123,-2.94367946988174,
37.4205008804654));
#61189=CARTESIAN_POINT('Ctrl Pts',(0.836009214464838,-2.98841369840265,
37.4733546952683));
#61190=CARTESIAN_POINT('Ctrl Pts',(1.83188804064887,-2.50473800395102,37.5262085100712));
#61191=CARTESIAN_POINT('Ctrl Pts',(2.39741535950944,-1.71348134882026,37.5790623248741));
#61192=CARTESIAN_POINT('Ctrl Pts',(2.96294267837005,-0.922224693689448,
37.631916139677));
#61193=CARTESIAN_POINT('Ctrl Pts',(3.09811848990726,0.176612922120487,37.6847699544799));
#61194=CARTESIAN_POINT('Ctrl Pts',(2.74122568156945,1.08134279025845,37.7376237692829));
#61195=CARTESIAN_POINT('Ctrl Pts',(2.38433287323164,1.9860726583964,37.7904775840858));
#61196=CARTESIAN_POINT('Ctrl Pts',(1.53537144501881,2.6966947788623,37.8433313988887));
#61197=CARTESIAN_POINT('Ctrl Pts',(0.581947704629053,2.88876402096991,37.8961852136916));
#61198=CARTESIAN_POINT('Ctrl Pts',(-0.371476035760709,3.08083326307753,
37.9490390284945));
#61199=CARTESIAN_POINT('Ctrl Pts',(-1.4293620883274,2.75434962682684,38.0018928432975));
#61200=CARTESIAN_POINT('Ctrl Pts',(-2.10872100721019,2.05837548530462,38.0547466581004));
#61201=CARTESIAN_POINT('Ctrl Pts',(-2.636047247822,1.5181523169454,38.0957723997037));
#61202=CARTESIAN_POINT('Ctrl Pts',(-2.93530923507167,0.755309503360123,
38.1367981413071));
#61203=CARTESIAN_POINT('Ctrl Pts',(-2.9422704459833,-0.00265502083472174,
38.1778238829104));
#61204=CARTESIAN_POINT('Origin',(0.,0.,-1.84858989190508));
#61205=CARTESIAN_POINT('',(-2.37393550902653,-0.00171275100589707,38.6514101080949));
#61206=CARTESIAN_POINT('',(-2.37498223974761,0.00116593724452961,38.848589891905));
#61207=CARTESIAN_POINT('',(-2.37175,1.07555357745099E-12,-1.84858989190508));
#61208=CARTESIAN_POINT('',(-2.34668236863844,0.343918483396126,39.62825));
#61209=CARTESIAN_POINT('Ctrl Pts',(-2.37393550902653,-0.00171275100589735,
38.6514101080949));
#61210=CARTESIAN_POINT('Ctrl Pts',(-2.37483094766103,-0.110413451510199,
38.6587242086095));
#61211=CARTESIAN_POINT('Ctrl Pts',(-2.31859051736089,-1.00660760499401,
38.7190881752552));
#61212=CARTESIAN_POINT('Ctrl Pts',(-1.17732869269255,-2.54685292441361,
38.8325020080321));
#61213=CARTESIAN_POINT('Ctrl Pts',(1.50731350036759,-2.36620050995552,38.9916516064257));
#61214=CARTESIAN_POINT('Ctrl Pts',(2.80472045702593,-0.0113602674063951,
39.1508012048193));
#61215=CARTESIAN_POINT('Ctrl Pts',(1.52653968516444,2.35613848946071,39.3099508032129));
#61216=CARTESIAN_POINT('Ctrl Pts',(-1.16086793848797,2.55318010173628,39.4691004016064));
#61217=CARTESIAN_POINT('Ctrl Pts',(-2.23204672396583,1.1261196710573,39.5752001338688));
#61218=CARTESIAN_POINT('Ctrl Pts',(-2.34668236863851,0.343918483395665,
39.62825));
#61219=CARTESIAN_POINT('',(-0.439445221992216,2.33068358199225,39.6282499999999));
#61220=CARTESIAN_POINT('Origin',(0.,0.,39.62825));
#61221=CARTESIAN_POINT('Ctrl Pts',(-2.37498223974761,0.00116593724452945,
38.848589891905));
#61222=CARTESIAN_POINT('Ctrl Pts',(-2.37064629607478,-0.718482336400258,
38.8970613353916));
#61223=CARTESIAN_POINT('Ctrl Pts',(-1.63815568977571,-2.23050835538683,
38.9983865936812));
#61224=CARTESIAN_POINT('Ctrl Pts',(0.931334562612731,-2.64189543289012,
39.1525656667738));
#61225=CARTESIAN_POINT('Ctrl Pts',(2.72641926444476,-0.654580598253606,
39.3111271111825));
#61226=CARTESIAN_POINT('Ctrl Pts',(2.02601511878175,1.93446865908499,39.4696885555913));
#61227=CARTESIAN_POINT('Ctrl Pts',(0.334552217316969,2.47661908313362,39.5753961851971));
#61228=CARTESIAN_POINT('Ctrl Pts',(-0.439445221993938,2.33068358199192,
39.62825));
#61229=CARTESIAN_POINT('Origin',(0.,0.,-1.84858989190508));
#61230=CARTESIAN_POINT('',(-2.36821658130285,-0.000998792486933048,37.6514101080949));
#61231=CARTESIAN_POINT('',(-2.37196802524163,-0.00214039621392242,37.848589891905));
#61232=CARTESIAN_POINT('',(-2.37175,1.07555357745099E-12,-1.84858989190508));
#61233=CARTESIAN_POINT('Ctrl Pts',(-2.36821658130285,-0.000998792486933131,
37.6514101080949));
#61234=CARTESIAN_POINT('Ctrl Pts',(-2.36947874192167,-0.335190857899489,
37.6737583451556));
#61235=CARTESIAN_POINT('Ctrl Pts',(-2.14703253604354,-1.46107782393166,
37.7491564483476));
#61236=CARTESIAN_POINT('Ctrl Pts',(-0.41808470505867,-2.7742369623609,37.8776044176707));
#61237=CARTESIAN_POINT('Ctrl Pts',(2.10849398479986,-1.85079097113315,38.0367540160642));
#61238=CARTESIAN_POINT('Ctrl Pts',(2.69662111602106,0.774135259850986,38.1959036144578));
#61239=CARTESIAN_POINT('Ctrl Pts',(0.805698917428903,2.68741434710406,38.3550532128514));
#61240=CARTESIAN_POINT('Ctrl Pts',(-1.70509856072161,2.15558121155782,38.5068887107304));
#61241=CARTESIAN_POINT('Ctrl Pts',(-2.36833624614658,0.678003059672109,
38.6056743424783));
#61242=CARTESIAN_POINT('Ctrl Pts',(-2.37393550902653,-0.00171275100589735,
38.6514101080949));
#61243=CARTESIAN_POINT('Ctrl Pts',(-2.37196802524163,-0.00214039621392275,
37.848589891905));
#61244=CARTESIAN_POINT('Ctrl Pts',(-2.37358598828088,-0.178310691973696,
37.8604179651045));
#61245=CARTESIAN_POINT('Ctrl Pts',(-2.27532136204516,-1.13991136271545,
37.925099853107));
#61246=CARTESIAN_POINT('Ctrl Pts',(-0.964945338256294,-2.63066900551404,
38.0426355559125));
#61247=CARTESIAN_POINT('Ctrl Pts',(1.68390204706478,-2.23961789871709,38.2011970003212));
#61248=CARTESIAN_POINT('Ctrl Pts',(2.79519402126786,0.196448450834139,38.35975844473));
#61249=CARTESIAN_POINT('Ctrl Pts',(1.35400172213932,2.45320986049924,38.5183198891387));
#61250=CARTESIAN_POINT('Ctrl Pts',(-1.3233434007851,2.46973099698168,38.6768813335475));
#61251=CARTESIAN_POINT('Ctrl Pts',(-2.34354795942612,0.915615981906982,
38.7869713344696));
#61252=CARTESIAN_POINT('Ctrl Pts',(-2.37537425850781,0.066230348892728,
38.8442075205887));
#61253=CARTESIAN_POINT('Ctrl Pts',(-2.37498223974761,0.00116593724452945,
38.848589891905));
#61254=CARTESIAN_POINT('Origin',(0.,0.,-1.84858989190508));
#61255=CARTESIAN_POINT('',(-2.37029980218114,0.00207473218684835,36.6514101080949));
#61256=CARTESIAN_POINT('',(-2.36794257065935,0.000391437457186727,36.848589891905));
#61257=CARTESIAN_POINT('',(-2.37175,1.07555357745099E-12,-1.84858989190508));
#61258=CARTESIAN_POINT('Ctrl Pts',(-2.37029980218114,0.0020747321868483,
36.6514101080949));
#61259=CARTESIAN_POINT('Ctrl Pts',(-2.36566040938742,-0.555702157675974,
36.6887924817018));
#61260=CARTESIAN_POINT('Ctrl Pts',(-1.89013456310209,-1.91214753332761,
36.7792247214399));
#61261=CARTESIAN_POINT('Ctrl Pts',(0.374295901203924,-2.78047924664893,
36.9227068273092));
#61262=CARTESIAN_POINT('Ctrl Pts',(2.54188584736079,-1.18742530783014,37.0818564257028));
#61263=CARTESIAN_POINT('Ctrl Pts',(2.37262067949971,1.49727438051885,37.2410060240964));
#61264=CARTESIAN_POINT('Ctrl Pts',(0.0221143200437823,2.8054724710268,37.40015562249));
#61265=CARTESIAN_POINT('Ctrl Pts',(-2.01580497986092,1.71296397828207,37.5369569838228));
#61266=CARTESIAN_POINT('Ctrl Pts',(-2.36648264644968,0.458108599416178,
37.6207084790244));
#61267=CARTESIAN_POINT('Ctrl Pts',(-2.36821658130285,-0.000998792486933131,
37.6514101080949));
#61268=CARTESIAN_POINT('Ctrl Pts',(-2.36794257065935,0.000391437457186762,
36.848589891905));
#61269=CARTESIAN_POINT('Ctrl Pts',(-2.36732273379814,-0.419017311524687,
36.8766284096204));
#61270=CARTESIAN_POINT('Ctrl Pts',(-2.06121258368243,-1.62987497742847,
36.9575207421387));
#61271=CARTESIAN_POINT('Ctrl Pts',(-0.128881968591299,-2.79909178025225,
37.09126688946));
#61272=CARTESIAN_POINT('Ctrl Pts',(2.27965875812724,-1.62931833193606,37.2498283338687));
#61273=CARTESIAN_POINT('Ctrl Pts',(2.60658251510917,1.02822903240515,37.4083897782775));
#61274=CARTESIAN_POINT('Ctrl Pts',(0.553362663956598,2.74687418626157,37.5669512226862));
#61275=CARTESIAN_POINT('Ctrl Pts',(-1.81428835189544,2.01617231988166,37.7136845938954));
#61276=CARTESIAN_POINT('Ctrl Pts',(-2.36635611090427,0.608907312915311,
37.8075641503016));
#61277=CARTESIAN_POINT('Ctrl Pts',(-2.37196802524163,-0.00214039621392275,
37.848589891905));
#61278=CARTESIAN_POINT('Origin',(0.,0.,-1.84858989190508));
#61279=CARTESIAN_POINT('',(-2.3756662176464,0.000177136364110247,35.6514101080949));
#61280=CARTESIAN_POINT('',(-2.37339473513533,0.00189558484520333,35.848589891905));
#61281=CARTESIAN_POINT('',(-2.37175,1.07555357745099E-12,-1.84858989190508));
#61282=CARTESIAN_POINT('Ctrl Pts',(-2.3756662176464,0.000177136364110169,
35.6514101080949));
#61283=CARTESIAN_POINT('Ctrl Pts',(-2.37483440554125,-0.777357601048919,
35.703826618248));
#61284=CARTESIAN_POINT('Ctrl Pts',(-1.53333569344657,-2.34336521677519,
35.8092929945323));
#61285=CARTESIAN_POINT('Ctrl Pts',(1.13681369625387,-2.5649203784333,35.9678092369478));
#61286=CARTESIAN_POINT('Ctrl Pts',(2.77251472574384,-0.429329754965117,
36.1269588353414));
#61287=CARTESIAN_POINT('Ctrl Pts',(1.859335179167,2.10096039122589,36.2861084337349));
#61288=CARTESIAN_POINT('Ctrl Pts',(-0.763203449633773,2.69975599917453,
36.4452580321285));
#61289=CARTESIAN_POINT('Ctrl Pts',(-2.23290357408391,1.25890136125407,36.5670252569152));
#61290=CARTESIAN_POINT('Ctrl Pts',(-2.37224423868689,0.235847080193127,
36.6357426155706));
#61291=CARTESIAN_POINT('Ctrl Pts',(-2.37029980218114,0.0020747321868483,
36.6514101080949));
#61292=CARTESIAN_POINT('Ctrl Pts',(-2.37339473513533,0.00189558484520345,
35.8485898919049));
#61293=CARTESIAN_POINT('Ctrl Pts',(-2.36765712231437,-0.656137770585933,
35.8928388541362));
#61294=CARTESIAN_POINT('Ctrl Pts',(-1.74141091723484,-2.10975212807994,
35.9899416311704));
#61295=CARTESIAN_POINT('Ctrl Pts',(0.719130113544572,-2.70820542107464,
36.1398982230075));
#61296=CARTESIAN_POINT('Ctrl Pts',(2.66420539827102,-0.86806350611665,36.2984596674162));
#61297=CARTESIAN_POINT('Ctrl Pts',(2.17652250448365,1.76473072150059,36.457021111825));
#61298=CARTESIAN_POINT('Ctrl Pts',(-0.298602167564159,2.78610149950517,
36.6155825562337));
#61299=CARTESIAN_POINT('Ctrl Pts',(-2.11160214823684,1.53266631190897,36.746105482927));
#61300=CARTESIAN_POINT('Ctrl Pts',(-2.36849115300642,0.371586263542998,
36.8237745948175));
#61301=CARTESIAN_POINT('Ctrl Pts',(-2.36794257065935,0.000391437457186762,
36.848589891905));
#61302=CARTESIAN_POINT('Origin',(0.,0.,-1.84858989190508));
#61303=CARTESIAN_POINT('',(-2.37083645980716,-0.00215799885136332,34.6514101080949));
#61304=CARTESIAN_POINT('',(-2.37380889386788,-0.00175759032045419,34.848589891905));
#61305=CARTESIAN_POINT('',(-2.37175,1.07555357745099E-12,-1.84858989190508));
#61306=CARTESIAN_POINT('Ctrl Pts',(-2.37083645980716,-0.00215799885136286,
34.6514101080949));
#61307=CARTESIAN_POINT('Ctrl Pts',(-2.37272754386709,-0.216906697555937,
34.665810888663));
#61308=CARTESIAN_POINT('Ctrl Pts',(-2.24739628056231,-1.22058222879963,
34.7332615353623));
#61309=CARTESIAN_POINT('Ctrl Pts',(-0.827441754243024,-2.68076520187573,
34.8537620481927));
#61310=CARTESIAN_POINT('Ctrl Pts',(1.8086454231506,-2.14475258658905,35.0129116465864));
#61311=CARTESIAN_POINT('Ctrl Pts',(2.78197455612906,0.363014454134983,35.1720612449799));
#61312=CARTESIAN_POINT('Ctrl Pts',(1.19772633632314,2.53704819558261,35.3312108433735));
#61313=CARTESIAN_POINT('Ctrl Pts',(-1.48763826287672,2.37867490914512,35.4903604417671));
#61314=CARTESIAN_POINT('Ctrl Pts',(-2.37136291112883,0.80588756412244,35.5970935300075));
#61315=CARTESIAN_POINT('Ctrl Pts',(-2.37567626854769,0.00957219667382547,
35.6507767521168));
#61316=CARTESIAN_POINT('Ctrl Pts',(-2.3756662176464,0.000177136364110169,
35.6514101080949));
#61317=CARTESIAN_POINT('Ctrl Pts',(-2.37380889386788,-0.00175759032045452,
34.848589891905));
#61318=CARTESIAN_POINT('Ctrl Pts',(-2.37474677486596,-0.114810256650096,
34.8561954838491));
#61319=CARTESIAN_POINT('Ctrl Pts',(-2.31608115217637,-1.01252620627014,
34.9166548905962));
#61320=CARTESIAN_POINT('Ctrl Pts',(-1.17105809706712,-2.54561341065258,
35.0299681121462));
#61321=CARTESIAN_POINT('Ctrl Pts',(1.50052034409269,-2.36642418021518,35.188529556555));
#61322=CARTESIAN_POINT('Ctrl Pts',(2.80193296331482,-0.0263888510821259,
35.3470910009637));
#61323=CARTESIAN_POINT('Ctrl Pts',(1.54482460333755,2.33774285330196,35.5056524453724));
#61324=CARTESIAN_POINT('Ctrl Pts',(-1.12290500001934,2.56721815733726,35.6642138897812));
#61325=CARTESIAN_POINT('Ctrl Pts',(-2.30695019422284,1.04264178315749,35.7785263719587));
#61326=CARTESIAN_POINT('Ctrl Pts',(-2.37451049717692,0.129859716097185,
35.8399850393333));
#61327=CARTESIAN_POINT('Ctrl Pts',(-2.37339473513533,0.00189558484520345,
35.8485898919049));
#61328=CARTESIAN_POINT('Origin',(0.,0.,-1.84858989190508));
#61329=CARTESIAN_POINT('',(-2.36801336551865,0.000709374362088072,33.6514101080949));
#61330=CARTESIAN_POINT('',(-2.36803870630727,-0.000628572818909962,33.848589891905));
#61331=CARTESIAN_POINT('',(-2.37175,1.07555357745099E-12,-1.84858989190508));
#61332=CARTESIAN_POINT('Ctrl Pts',(-2.36801336551865,0.000709374362087983,
33.6514101080949));
#61333=CARTESIAN_POINT('Ctrl Pts',(-2.36683877105606,-0.439550574027366,
33.6808450252092));
#61334=CARTESIAN_POINT('Ctrl Pts',(-2.03750269480847,-1.674913490657,33.7633298084547));
#61335=CARTESIAN_POINT('Ctrl Pts',(-0.0448724219901618,-2.805200240646,
33.8988644578313));
#61336=CARTESIAN_POINT('Ctrl Pts',(2.33619776832739,-1.55349345400542,34.0580140562249));
#61337=CARTESIAN_POINT('Ctrl Pts',(2.56951053574539,1.1264002534988,34.2171636546184));
#61338=CARTESIAN_POINT('Ctrl Pts',(0.440572383654118,2.77075042165889,34.3763132530121));
#61339=CARTESIAN_POINT('Ctrl Pts',(-1.86411244105769,1.94954241988793,34.5210620708375));
#61340=CARTESIAN_POINT('Ctrl Pts',(-2.36576113286264,0.574188595109401,
34.6127610225318));
#61341=CARTESIAN_POINT('Ctrl Pts',(-2.37083645980716,-0.00215799885136286,
34.6514101080949));
#61342=CARTESIAN_POINT('Ctrl Pts',(-2.36803870630727,-0.000628572818910204,
33.848589891905));
#61343=CARTESIAN_POINT('Ctrl Pts',(-2.36888613676592,-0.356840042454167,
33.872405928365));
#61344=CARTESIAN_POINT('Ctrl Pts',(-2.12639782110154,-1.5024792828138,33.9490757796279));
#61345=CARTESIAN_POINT('Ctrl Pts',(-0.351024016063958,-2.77998324516326,
34.0785994456937));
#61346=CARTESIAN_POINT('Ctrl Pts',(2.14289857733639,-1.80541141862616,34.2371608901025));
#61347=CARTESIAN_POINT('Ctrl Pts',(2.68008236242858,0.817730538643591,34.3957223345112));
#61348=CARTESIAN_POINT('Ctrl Pts',(0.770010256154827,2.69418056348283,34.55428377892));
#61349=CARTESIAN_POINT('Ctrl Pts',(-1.71783430240134,2.13849813336335,34.7052396313845));
#61350=CARTESIAN_POINT('Ctrl Pts',(-2.3682291245708,0.670830720808595,34.8033416690462));
#61351=CARTESIAN_POINT('Ctrl Pts',(-2.37380889386788,-0.00175759032045452,
34.848589891905));
#61352=CARTESIAN_POINT('Origin',(0.,0.,-1.84858989190508));
#61353=CARTESIAN_POINT('',(-2.37344656872762,0.00192570299439512,32.6514101080949));
#61354=CARTESIAN_POINT('',(-2.37151790930666,0.002154076539162,32.848589891905));
#61355=CARTESIAN_POINT('',(-2.37175,1.07555357745099E-12,-1.84858989190508));
#61356=CARTESIAN_POINT('Ctrl Pts',(-2.37344656872762,0.00192570299439525,
32.6514101080949));
#61357=CARTESIAN_POINT('Ctrl Pts',(-2.36762356345687,-0.659341773836592,
32.6958791617554));
#61358=CARTESIAN_POINT('Ctrl Pts',(-1.73518620177463,-2.11923842087366,
32.793398081547));
#61359=CARTESIAN_POINT('Ctrl Pts',(0.741276476036008,-2.70585866416802,
32.9439668674699));
#61360=CARTESIAN_POINT('Ctrl Pts',(2.67738679382172,-0.838308941051334,
33.1031164658635));
#61361=CARTESIAN_POINT('Ctrl Pts',(2.15207135460536,1.79993077896479,33.262266064257));
#61362=CARTESIAN_POINT('Ctrl Pts',(-0.351726937875201,2.78342416558279,
33.4214156626506));
#61363=CARTESIAN_POINT('Ctrl Pts',(-2.12889350245117,1.49938279527832,33.5511303439299));
#61364=CARTESIAN_POINT('Ctrl Pts',(-2.36895571532184,0.353919685607108,
33.627795159078));
#61365=CARTESIAN_POINT('Ctrl Pts',(-2.36801336551865,0.000709374362087983,
33.6514101080949));
#61366=CARTESIAN_POINT('Ctrl Pts',(-2.37151790930666,0.00215407653916203,
32.848589891905));
#61367=CARTESIAN_POINT('Ctrl Pts',(-2.36610629731291,-0.594299025520429,
32.8886163728808));
#61368=CARTESIAN_POINT('Ctrl Pts',(-1.83591513178192,-1.9869237846516,32.9814966686595));
#61369=CARTESIAN_POINT('Ctrl Pts',(0.5015298178546,-2.75680839831995,33.1272307792412));
#61370=CARTESIAN_POINT('Ctrl Pts',(2.58675326481436,-1.07714077548725,33.2857922236499));
#61371=CARTESIAN_POINT('Ctrl Pts',(2.30994215059737,1.58609330246939,33.4443536680588));
#61372=CARTESIAN_POINT('Ctrl Pts',(-0.076139789038159,2.80102256966442,
33.6029151124674));
#61373=CARTESIAN_POINT('Ctrl Pts',(-2.04474804530386,1.65994568587728,33.7376605204162));
#61374=CARTESIAN_POINT('Ctrl Pts',(-2.36700547402024,0.433683396591004,
33.8195521135621));
#61375=CARTESIAN_POINT('Ctrl Pts',(-2.36803870630727,-0.000628572818910204,
33.848589891905));
#61376=CARTESIAN_POINT('Origin',(0.,0.,-1.84858989190508));
#61377=CARTESIAN_POINT('',(-2.37430589928956,-0.0015910093592776,31.6514101080949));
#61378=CARTESIAN_POINT('',(-2.37519828256487,-0.000898997154156478,31.848589891905));
#61379=CARTESIAN_POINT('',(-2.37175,1.07555357745099E-12,-1.84858989190508));
#61380=CARTESIAN_POINT('Ctrl Pts',(-2.37430589928956,-0.0015910093592772,
31.6514101080949));
#61381=CARTESIAN_POINT('Ctrl Pts',(-2.37504475585361,-0.0974633462288916,
31.6578634321704));
#61382=CARTESIAN_POINT('Ctrl Pts',(-2.32616367491842,-0.98069910565149,
31.717366622377));
#61383=CARTESIAN_POINT('Ctrl Pts',(-1.21826882213122,-2.52724810839787,
31.8299196787149));
#61384=CARTESIAN_POINT('Ctrl Pts',(1.46829221901895,-2.39066515512857,31.9890692771084));
#61385=CARTESIAN_POINT('Ctrl Pts',(2.80499514663885,-0.0562507929721938,
32.148218875502));
#61386=CARTESIAN_POINT('Ctrl Pts',(1.56295699802168,2.32987710978769,32.3073684738957));
#61387=CARTESIAN_POINT('Ctrl Pts',(-1.11596827534518,2.57405841674206,32.4665180722891));
#61388=CARTESIAN_POINT('Ctrl Pts',(-2.30707249918363,1.04480000964771,32.5811986170223));
#61389=CARTESIAN_POINT('Ctrl Pts',(-2.37457018418897,0.129524825184061,
32.6428292956242));
#61390=CARTESIAN_POINT('Ctrl Pts',(-2.37344656872762,0.00192570299439525,
32.6514101080949));
#61391=CARTESIAN_POINT('Ctrl Pts',(-2.37519828256487,-0.000898997154156859,
31.848589891905));
#61392=CARTESIAN_POINT('Ctrl Pts',(-2.37544230083747,-0.051109655468214,
31.8519730025937));
#61393=CARTESIAN_POINT('Ctrl Pts',(-2.35126215380067,-0.885514299668502,
31.9082099280854));
#61394=CARTESIAN_POINT('Ctrl Pts',(-1.3697471531232,-2.44444624398976,32.0173006683799));
#61395=CARTESIAN_POINT('Ctrl Pts',(1.30762066055104,-2.47823584659426,32.1758621127887));
#61396=CARTESIAN_POINT('Ctrl Pts',(2.79096458522799,-0.249081085688892,
32.3344235571974));
#61397=CARTESIAN_POINT('Ctrl Pts',(1.72580305366397,2.20751636986205,32.4929850016062));
#61398=CARTESIAN_POINT('Ctrl Pts',(-0.915236051531332,2.64837075826291,
32.6515464460149));
#61399=CARTESIAN_POINT('Ctrl Pts',(-2.26482404050824,1.17010253722111,32.7700814094479));
#61400=CARTESIAN_POINT('Ctrl Pts',(-2.37325217502012,0.193300109510363,
32.8357625580779));
#61401=CARTESIAN_POINT('Ctrl Pts',(-2.37151790930666,0.00215407653916203,
32.848589891905));
#61402=CARTESIAN_POINT('Origin',(0.,0.,-1.84858989190508));
#61403=CARTESIAN_POINT('',(-2.36839481200122,-0.00118517904615592,30.6514101080949));
#61404=CARTESIAN_POINT('',(-2.36891564579557,-0.00151055549120149,30.848589891905));
#61405=CARTESIAN_POINT('',(-2.37175,1.07555357745099E-12,-1.84858989190508));
#61406=CARTESIAN_POINT('Ctrl Pts',(-2.36839481200122,-0.00118517904615575,
30.6514101080949));
#61407=CARTESIAN_POINT('Ctrl Pts',(-2.36984063649032,-0.322445251385961,
30.6728975687166));
#61408=CARTESIAN_POINT('Ctrl Pts',(-2.15901428293454,-1.43503844100005,
30.7474348954694));
#61409=CARTESIAN_POINT('Ctrl Pts',(-0.463035703261235,-2.76708508396162,
30.8750220883534));
#61410=CARTESIAN_POINT('Ctrl Pts',(2.07817926003504,-1.88476335053973,31.034171686747));
#61411=CARTESIAN_POINT('Ctrl Pts',(2.70884324499614,0.730294597006095,31.1933212851405));
#61412=CARTESIAN_POINT('Ctrl Pts',(0.849162334591095,2.67396433295012,31.3524708835341));
#61413=CARTESIAN_POINT('Ctrl Pts',(-1.68412356093239,2.18022151201017,31.5051671578522));
#61414=CARTESIAN_POINT('Ctrl Pts',(-2.36897094933856,0.690659887185638,
31.6048135660392));
#61415=CARTESIAN_POINT('Ctrl Pts',(-2.37430589928956,-0.0015910093592772,
31.6514101080949));
#61416=CARTESIAN_POINT('Ctrl Pts',(-2.36891564579557,-0.00151055549120167,
30.848589891905));
#61417=CARTESIAN_POINT('Ctrl Pts',(-2.37062840873568,-0.294295702210565,
30.8681834471096));
#61418=CARTESIAN_POINT('Ctrl Pts',(-2.18474225478032,-1.37477397204726,
30.940630817117));
#61419=CARTESIAN_POINT('Ctrl Pts',(-0.570943356725327,-2.74327329784255,
31.0659320019274));
#61420=CARTESIAN_POINT('Ctrl Pts',(1.99257021690915,-1.97007325598095,31.2244934463362));
#61421=CARTESIAN_POINT('Ctrl Pts',(2.73661388518784,0.602054106075114,31.3830548907449));
#61422=CARTESIAN_POINT('Ctrl Pts',(0.981781195472087,2.62442953562526,31.5416163351537));
#61423=CARTESIAN_POINT('Ctrl Pts',(-1.6129731567046,2.25834827685961,31.6967946688737));
#61424=CARTESIAN_POINT('Ctrl Pts',(-2.37163004112299,0.733323690003802,
31.7991191877908));
#61425=CARTESIAN_POINT('Ctrl Pts',(-2.37519828256487,-0.000898997154156859,
31.848589891905));
#61426=CARTESIAN_POINT('Origin',(0.,0.,-1.84858989190508));
#61427=CARTESIAN_POINT('',(-2.36995400383523,0.0019928976040509,29.6514101080949));
#61428=CARTESIAN_POINT('',(-2.36976239142724,0.00188907497310223,29.848589891905));
#61429=CARTESIAN_POINT('',(-2.37175,1.07555357745099E-12,-1.84858989190508));
#61430=CARTESIAN_POINT('Ctrl Pts',(-2.36995400383523,0.00199289760405105,
29.6514101080949));
#61431=CARTESIAN_POINT('Ctrl Pts',(-2.36564524447228,-0.543141402735341,
29.6879317052627));
#61432=CARTESIAN_POINT('Ctrl Pts',(-1.907411081712,-1.8866583110207,29.7775031685617));
#61433=CARTESIAN_POINT('Ctrl Pts',(0.32913472971066,-2.78618596904008,29.920124497992));
#61434=CARTESIAN_POINT('Ctrl Pts',(2.52228565055847,-1.22851008191401,30.0792740963855));
#61435=CARTESIAN_POINT('Ctrl Pts',(2.39660132461721,1.4585828791058,30.2384236947791));
#61436=CARTESIAN_POINT('Ctrl Pts',(0.067628238422609,2.80474390020647,30.3975732931727));
#61437=CARTESIAN_POINT('Ctrl Pts',(-2.00067933025812,1.73877948815203,30.5352354309446));
#61438=CARTESIAN_POINT('Ctrl Pts',(-2.36627107576156,0.470705885969103,
30.6198477025854));
#61439=CARTESIAN_POINT('Ctrl Pts',(-2.36839481200122,-0.00118517904615575,
30.6514101080949));
#61440=CARTESIAN_POINT('Ctrl Pts',(-2.36976239142724,0.0018890749731023,
29.848589891905));
#61441=CARTESIAN_POINT('Ctrl Pts',(-2.36575561414334,-0.532646635303957,
29.8843938916254));
#61442=CARTESIAN_POINT('Ctrl Pts',(-1.9223422941335,-1.86228449563888,29.9730517061487));
#61443=CARTESIAN_POINT('Ctrl Pts',(0.28075407675448,-2.78795657276624,30.1145633354749));
#61444=CARTESIAN_POINT('Ctrl Pts',(2.49292302707169,-1.27939809455089,30.2731247798837));
#61445=CARTESIAN_POINT('Ctrl Pts',(2.42873635105556,1.39741348222569,30.4316862242924));
#61446=CARTESIAN_POINT('Ctrl Pts',(0.146804643376738,2.79820890927176,30.5902476687012));
#61447=CARTESIAN_POINT('Ctrl Pts',(-1.97063355459528,1.78652468932462,30.7292155579053));
#61448=CARTESIAN_POINT('Ctrl Pts',(-2.3660082132534,0.495495214251002,30.8153296323066));
#61449=CARTESIAN_POINT('Ctrl Pts',(-2.36891564579557,-0.00151055549120167,
30.848589891905));
#61450=CARTESIAN_POINT('Origin',(0.,0.,-1.84858989190508));
#61451=CARTESIAN_POINT('',(-2.37559433303246,0.000415362230552236,28.6514101080949));
#61452=CARTESIAN_POINT('',(-2.37558996096397,0.000230858190189672,28.848589891905));
#61453=CARTESIAN_POINT('',(-2.37175,1.07555357745099E-12,-1.84858989190508));
#61454=CARTESIAN_POINT('Ctrl Pts',(-2.37559433303246,0.000415362230552201,
28.6514101080949));
#61455=CARTESIAN_POINT('Ctrl Pts',(-2.37375083518073,-0.76441301960334,
28.7029658418089));
#61456=CARTESIAN_POINT('Ctrl Pts',(-1.55667585051139,-2.31961727945024,
28.8075714416541));
#61457=CARTESIAN_POINT('Ctrl Pts',(1.09504940571272,-2.58302704659199,28.9652269076305));
#61458=CARTESIAN_POINT('Ctrl Pts',(2.76518410684866,-0.474256027488414,
29.1243765060241));
#61459=CARTESIAN_POINT('Ctrl Pts',(1.89317756819207,2.07051699333089,29.2835261044177));
#61460=CARTESIAN_POINT('Ctrl Pts',(-0.719300701960229,2.71178325544964,
29.4426757028112));
#61461=CARTESIAN_POINT('Ctrl Pts',(-2.22273779394574,1.28494796187104,29.565303704037));
#61462=CARTESIAN_POINT('Ctrl Pts',(-2.37190398245533,0.248699696755391,
29.6348818391316));
#61463=CARTESIAN_POINT('Ctrl Pts',(-2.36995400383523,0.00199289760405105,
29.6514101080949));
#61464=CARTESIAN_POINT('Ctrl Pts',(-2.37558996096397,0.000230858190189351,
28.848589891905));
#61465=CARTESIAN_POINT('Ctrl Pts',(-2.37451683347506,-0.771404774036993,
28.9006043361412));
#61466=CARTESIAN_POINT('Ctrl Pts',(-1.54564963095845,-2.32910717712637,
29.0054725951804));
#61467=CARTESIAN_POINT('Ctrl Pts',(1.10644174224207,-2.57435649712099,29.1631946690224));
#61468=CARTESIAN_POINT('Ctrl Pts',(2.7623251407879,-0.470196256701246,29.3217561134311));
#61469=CARTESIAN_POINT('Ctrl Pts',(1.89585453653854,2.06331293785769,29.4803175578399));
#61470=CARTESIAN_POINT('Ctrl Pts',(-0.701772262303996,2.71275512995654,
29.6388790022487));
#61471=CARTESIAN_POINT('Ctrl Pts',(-2.21673174114633,1.29779949503705,29.761636446937));
#61472=CARTESIAN_POINT('Ctrl Pts',(-2.37167041322091,0.256434239938047,
29.8315400768225));
#61473=CARTESIAN_POINT('Ctrl Pts',(-2.36976239142724,0.0018890749731023,
29.848589891905));
#61474=CARTESIAN_POINT('Origin',(0.,0.,-1.84858989190508));
#61475=CARTESIAN_POINT('',(-2.37121570870644,-0.00218817987852429,27.6514101080949));
#61476=CARTESIAN_POINT('',(-2.37042075827088,-0.00205354385727247,27.848589891905));
#61477=CARTESIAN_POINT('',(-2.37175,1.07555357745099E-12,-1.84858989190508));
#61478=CARTESIAN_POINT('Ctrl Pts',(-2.37121570870644,-0.0021881798785239,
27.6514101080949));
#61479=CARTESIAN_POINT('Ctrl Pts',(-2.37304212744356,-0.204018644870209,
27.6649501122239));
#61480=CARTESIAN_POINT('Ctrl Pts',(-2.25693119590959,-1.19455237637443,
27.7315399824841));
#61481=CARTESIAN_POINT('Ctrl Pts',(-0.870827027847972,-2.66698747877582,
27.8511797188755));
#61482=CARTESIAN_POINT('Ctrl Pts',(1.77360972961834,-2.17381472333333,28.0103293172691));
#61483=CARTESIAN_POINT('Ctrl Pts',(2.7874981175229,0.317830409469884,28.1694789156627));
#61484=CARTESIAN_POINT('Ctrl Pts',(1.23873112821468,2.51728169189892,28.3286285140562));
#61485=CARTESIAN_POINT('Ctrl Pts',(-1.44884954017187,2.40249806125235,28.4877781124498));
#61486=CARTESIAN_POINT('Ctrl Pts',(-2.36530750122204,0.831688918896625,
28.5953719771294));
#61487=CARTESIAN_POINT('Ctrl Pts',(-2.37564775928989,0.0225807897506126,
28.6499159756778));
#61488=CARTESIAN_POINT('Ctrl Pts',(-2.37559433303246,0.000415362230552201,
28.6514101080949));
#61489=CARTESIAN_POINT('Ctrl Pts',(-2.37042075827088,-0.00205354385727267,
27.848589891905));
#61490=CARTESIAN_POINT('Ctrl Pts',(-2.37232842441219,-0.231374808268618,
27.8639609658541));
#61491=CARTESIAN_POINT('Ctrl Pts',(-2.23658719967056,-1.24701197475112,
27.9321858546062));
#61492=CARTESIAN_POINT('Ctrl Pts',(-0.787247754401329,-2.68919424297219,
28.0532645581612));
#61493=CARTESIAN_POINT('Ctrl Pts',(1.82962584537607,-2.12226152233333,28.2118260025699));
#61494=CARTESIAN_POINT('Ctrl Pts',(2.77581846464243,0.382565751988956,28.3703874469787));
#61495=CARTESIAN_POINT('Ctrl Pts',(1.18733596115095,2.53806186264293,28.5289488913874));
#61496=CARTESIAN_POINT('Ctrl Pts',(-1.48533521008643,2.37598485199765,28.6875103357962));
#61497=CARTESIAN_POINT('Ctrl Pts',(-2.36988450532629,0.809206391250685,
28.7940573359687));
#61498=CARTESIAN_POINT('Ctrl Pts',(-2.37560727830038,0.0126829423644369,
28.8477505213383));
#61499=CARTESIAN_POINT('Ctrl Pts',(-2.37558996096397,0.000230858190189351,
28.848589891905));
#61500=CARTESIAN_POINT('Origin',(0.,0.,-1.84858989190508));
#61501=CARTESIAN_POINT('',(-2.36791541979134,0.000503980893847333,26.6514101080949));
#61502=CARTESIAN_POINT('',(-2.36848027041357,0.00119022360032209,26.848589891905));
#61503=CARTESIAN_POINT('',(-2.37175,1.07555357745099E-12,-1.84858989190508));
#61504=CARTESIAN_POINT('Ctrl Pts',(-2.36791541979134,0.000503980893847393,
26.6514101080949));
#61505=CARTESIAN_POINT('Ctrl Pts',(-2.36710719014345,-0.426925371301292,
26.6799842487701));
#61506=CARTESIAN_POINT('Ctrl Pts',(-2.05187220716749,-1.64901827578131,
26.7616082555765));
#61507=CARTESIAN_POINT('Ctrl Pts',(-0.0903796039458558,-2.80410296736195,
26.896282128514));
#61508=CARTESIAN_POINT('Ctrl Pts',(2.3106855433324,-1.59119271121138,27.0554317269076));
#61509=CARTESIAN_POINT('Ctrl Pts',(2.58744764787687,1.08456285842457,27.2145813253012));
#61510=CARTESIAN_POINT('Ctrl Pts',(0.48546854847008,2.76323763234795,27.3737309236948));
#61511=CARTESIAN_POINT('Ctrl Pts',(-1.84601931779875,1.97486971266958,27.5193405179593));
#61512=CARTESIAN_POINT('Ctrl Pts',(-2.36588620130201,0.586755054088587,
27.6119002460927));
#61513=CARTESIAN_POINT('Ctrl Pts',(-2.37121570870644,-0.0021881798785239,
27.6514101080949));
#61514=CARTESIAN_POINT('Ctrl Pts',(-2.36848027041357,0.00119022360032195,
26.848589891905));
#61515=CARTESIAN_POINT('Ctrl Pts',(-2.36632923020358,-0.470947746561001,
26.88017141037));
#61516=CARTESIAN_POINT('Ctrl Pts',(-2.00099020303499,-1.73630730429607,
26.9646067436378));
#61517=CARTESIAN_POINT('Ctrl Pts',(0.0582007337807619,-2.8014527263247,
27.1018958917086));
#61518=CARTESIAN_POINT('Ctrl Pts',(2.38330878115067,-1.47355487069022,27.2604573361174));
#61519=CARTESIAN_POINT('Ctrl Pts',(2.53215294297463,1.19988590150465,27.4190187805261));
#61520=CARTESIAN_POINT('Ctrl Pts',(0.368819578303693,2.77767831505101,27.5775802249349));
#61521=CARTESIAN_POINT('Ctrl Pts',(-1.88893002712957,1.91202293803979,27.7207705953945));
#61522=CARTESIAN_POINT('Ctrl Pts',(-2.3657688675932,0.557151984308005,27.8111071510512));
#61523=CARTESIAN_POINT('Ctrl Pts',(-2.37042075827088,-0.00205354385727267,
27.848589891905));
#61524=CARTESIAN_POINT('Origin',(0.,0.,-1.84858989190508));
#61525=CARTESIAN_POINT('',(-2.37307089521247,0.00202464274905245,25.6514101080949));
#61526=CARTESIAN_POINT('',(-2.37473384480564,0.00128782070115716,25.848589891905));
#61527=CARTESIAN_POINT('',(-2.37175,1.07555357745099E-12,-1.84858989190508));
#61528=CARTESIAN_POINT('Ctrl Pts',(-2.37307089521247,0.00202464274905237,
25.6514101080949));
#61529=CARTESIAN_POINT('Ctrl Pts',(-2.36718725723238,-0.646708552619323,
25.6950183853163));
#61530=CARTESIAN_POINT('Ctrl Pts',(-1.7552402308422,-2.09438973910438,25.7916765286689));
#61531=CARTESIAN_POINT('Ctrl Pts',(0.697277587574235,-2.71752937247129,
25.9413845381526));
#61532=CARTESIAN_POINT('Ctrl Pts',(2.66343320026788,-0.881637971101683,
26.1005341365462));
#61533=CARTESIAN_POINT('Ctrl Pts',(2.18099113692833,1.76477748881203,26.2596837349398));
#61534=CARTESIAN_POINT('Ctrl Pts',(-0.306520859756921,2.78876440147091,
26.4188333333333));
#61535=CARTESIAN_POINT('Ctrl Pts',(-2.11621631635713,1.52539742028699,26.5494087910517));
#61536=CARTESIAN_POINT('Ctrl Pts',(-2.36860772431913,0.366626748857101,
26.6269343826389));
#61537=CARTESIAN_POINT('Ctrl Pts',(-2.36791541979134,0.000503980893847393,
26.6514101080949));
#61538=CARTESIAN_POINT('Ctrl Pts',(-2.37473384480564,0.00128782070115717,
25.848589891905));
#61539=CARTESIAN_POINT('Ctrl Pts',(-2.3700792053546,-0.708386931882113,
25.8963818548858));
#61540=CARTESIAN_POINT('Ctrl Pts',(-1.65568478423942,-2.21103251101488,
25.9970276326695));
#61541=CARTESIAN_POINT('Ctrl Pts',(0.898257358734679,-2.65417754129669,
26.1505272252561));
#61542=CARTESIAN_POINT('Ctrl Pts',(2.71619596155049,-0.688334367659731,
26.3090886696649));
#61543=CARTESIAN_POINT('Ctrl Pts',(2.05390236619762,1.90604558533434,26.4676501140736));
#61544=CARTESIAN_POINT('Ctrl Pts',(-0.483865183409376,2.7599636206894,26.6262115584824));
#61545=CARTESIAN_POINT('Ctrl Pts',(-2.16234346834408,1.42556571001596,26.7531914844262));
#61546=CARTESIAN_POINT('Ctrl Pts',(-2.36992914200068,0.319207193709481,
26.827317595567));
#61547=CARTESIAN_POINT('Ctrl Pts',(-2.36848027041357,0.00119022360032195,
26.848589891905));
#61548=CARTESIAN_POINT('Origin',(0.,0.,-1.84858989190508));
#61549=CARTESIAN_POINT('',(-2.37461414594325,-0.0014219220721963,24.6514101080949));
#61550=CARTESIAN_POINT('',(-2.37227285406081,-0.00211555575218542,24.848589891905));
#61551=CARTESIAN_POINT('',(-2.37175,1.07555357745099E-12,-1.84858989190508));
#61552=CARTESIAN_POINT('Ctrl Pts',(-2.37461414594325,-0.00142192207219587,
24.6514101080949));
#61553=CARTESIAN_POINT('Ctrl Pts',(-2.37520144012387,-0.0844780524433969,
24.6570026557313));
#61554=CARTESIAN_POINT('Ctrl Pts',(-2.33348900523777,-0.95479259564346,
24.7156450694988));
#61555=CARTESIAN_POINT('Ctrl Pts',(-1.25911190801061,-2.50714960213454,
24.8273373493976));
#61556=CARTESIAN_POINT('Ctrl Pts',(1.42931150622999,-2.41417284852102,24.9864869477912));
#61557=CARTESIAN_POINT('Ctrl Pts',(2.80371329149552,-0.101753149675579,
25.1456365461847));
#61558=CARTESIAN_POINT('Ctrl Pts',(1.60055245978652,2.30421217509344,25.3047861445783));
#61559=CARTESIAN_POINT('Ctrl Pts',(-1.07405846611233,2.59182567618851,25.4639357429719));
#61560=CARTESIAN_POINT('Ctrl Pts',(-2.29894274585785,1.07076183898232,25.5794770641441));
#61561=CARTESIAN_POINT('Ctrl Pts',(-2.37434475638383,0.142481283852646,
25.6419685191851));
#61562=CARTESIAN_POINT('Ctrl Pts',(-2.37307089521247,0.00202464274905237,
25.6514101080949));
#61563=CARTESIAN_POINT('Ctrl Pts',(-2.37227285406081,-0.00211555575218592,
24.848589891905));
#61564=CARTESIAN_POINT('Ctrl Pts',(-2.3737989493321,-0.168110516416099,
24.8597384845987));
#61565=CARTESIAN_POINT('Ctrl Pts',(-2.28226874561123,-1.11939179033149,
24.9237408920953));
#61566=CARTESIAN_POINT('Ctrl Pts',(-0.998567672067767,-2.61808848352113,
25.0405971143948));
#61567=CARTESIAN_POINT('Ctrl Pts',(1.65509714933991,-2.26101263364264,25.1991585588037));
#61568=CARTESIAN_POINT('Ctrl Pts',(2.79744787596231,0.16065517271071,25.3577200032123));
#61569=CARTESIAN_POINT('Ctrl Pts',(1.3853730777416,2.43562438374916,25.5162814476211));
#61570=CARTESIAN_POINT('Ctrl Pts',(-1.29172345032858,2.48655891366281,25.6748428920299));
#61571=CARTESIAN_POINT('Ctrl Pts',(-2.33792441559412,0.935961079615963,
25.7856123734578));
#61572=CARTESIAN_POINT('Ctrl Pts',(-2.37522683763784,0.0764525181823475,
25.8435280400829));
#61573=CARTESIAN_POINT('Ctrl Pts',(-2.37473384480564,0.00128782070115717,
25.848589891905));
#61574=CARTESIAN_POINT('Origin',(0.,0.,-1.84858989190508));
#61575=CARTESIAN_POINT('',(-2.36860268394698,-0.00136012066467478,23.6514101080949));
#61576=CARTESIAN_POINT('',(-2.3679029786215,0.000227208911412896,23.848589891905));
#61577=CARTESIAN_POINT('',(-2.37175,1.07555357745099E-12,-1.84858989190508));
#61578=CARTESIAN_POINT('Ctrl Pts',(-2.36860268394698,-0.00136012066467461,
23.651410108095));
#61579=CARTESIAN_POINT('Ctrl Pts',(-2.37020370805452,-0.309682979419102,
23.6720367922775));
#61580=CARTESIAN_POINT('Ctrl Pts',(-2.17071820741675,-1.40899174483152,
23.7457133425912));
#61581=CARTESIAN_POINT('Ctrl Pts',(-0.507869442880617,-2.75920832003777,
23.8724397590362));
#61582=CARTESIAN_POINT('Ctrl Pts',(2.04732629486344,-1.91823277178195,24.0315893574297));
#61583=CARTESIAN_POINT('Ctrl Pts',(2.7203353844948,0.686248730594912,24.1907389558233));
#61584=CARTESIAN_POINT('Ctrl Pts',(0.892434408187573,2.6598350985466,24.3498885542168));
#61585=CARTESIAN_POINT('Ctrl Pts',(-1.6628526585275,2.2047074150282,24.5034456049741));
#61586=CARTESIAN_POINT('Ctrl Pts',(-2.36963047681923,0.703376943895443,
24.6039527896001));
#61587=CARTESIAN_POINT('Ctrl Pts',(-2.37461414594325,-0.00142192207219587,
24.6514101080949));
#61588=CARTESIAN_POINT('Ctrl Pts',(-2.3679029786215,0.000227208911412861,
23.848589891905));
#61589=CARTESIAN_POINT('Ctrl Pts',(-2.36755222713902,-0.409034741783179,
23.8759489291145));
#61590=CARTESIAN_POINT('Ctrl Pts',(-2.07217810476315,-1.6094075389743,23.956161781127));
#61591=CARTESIAN_POINT('Ctrl Pts',(-0.164721108680563,-2.79721140774162,
24.0892284479423));
#61592=CARTESIAN_POINT('Ctrl Pts',(2.25860455255274,-1.6583817951343,24.2477898923511));
#61593=CARTESIAN_POINT('Ctrl Pts',(2.61953714146364,0.99476121141571,24.4063513367598));
#61594=CARTESIAN_POINT('Ctrl Pts',(0.588499322301271,2.73956077700343,24.5649127811686));
#61595=CARTESIAN_POINT('Ctrl Pts',(-1.79932587717851,2.03600208971102,24.7123256328836));
#61596=CARTESIAN_POINT('Ctrl Pts',(-2.36656395931527,0.61884682880159,24.8068846697958));
#61597=CARTESIAN_POINT('Ctrl Pts',(-2.37227285406081,-0.00211555575218592,
24.848589891905));
#61598=CARTESIAN_POINT('Origin',(0.,0.,-1.84858989190508));
#61599=CARTESIAN_POINT('',(-2.36962670248717,0.00189177622211031,22.651410108095));
#61600=CARTESIAN_POINT('',(-2.37310225641301,0.0019731259294458,22.848589891905));
#61601=CARTESIAN_POINT('',(-2.37175,1.07555357745099E-12,-1.84858989190508));
#61602=CARTESIAN_POINT('Ctrl Pts',(-2.36962670248717,0.00189177622211021,
22.651410108095));
#61603=CARTESIAN_POINT('Ctrl Pts',(-2.36567043422174,-0.530579655077376,
22.6870709288237));
#61604=CARTESIAN_POINT('Ctrl Pts',(-1.9243615988136,-1.86111040461567,22.7757816156835));
#61605=CARTESIAN_POINT('Ctrl Pts',(0.283886816331191,-2.79115929317747,
22.9175421686747));
#61606=CARTESIAN_POINT('Ctrl Pts',(2.50202163773962,-1.26927130616756,23.0766917670682));
#61607=CARTESIAN_POINT('Ctrl Pts',(2.41995070706164,1.41950713269408,23.2358413654619));
#61608=CARTESIAN_POINT('Ctrl Pts',(0.113125021193992,2.80327748429537,23.3949909638554));
#61609=CARTESIAN_POINT('Ctrl Pts',(-1.98524427925328,1.76455614662456,23.5335138780665));
#61610=CARTESIAN_POINT('Ctrl Pts',(-2.36608602661693,0.483294032172269,
23.6189869261463));
#61611=CARTESIAN_POINT('Ctrl Pts',(-2.36860268394698,-0.00136012066467461,
23.651410108095));
#61612=CARTESIAN_POINT('Ctrl Pts',(-2.37310225641302,0.00197312592944565,
22.848589891905));
#61613=CARTESIAN_POINT('Ctrl Pts',(-2.36731533440048,-0.646162491872702,
22.8921593736304));
#61614=CARTESIAN_POINT('Ctrl Pts',(-1.7571753397551,-2.09013014137335,22.9885826701586));
#61615=CARTESIAN_POINT('Ctrl Pts',(0.684385634967381,-2.71719359006588,
23.1378597814898));
#61616=CARTESIAN_POINT('Ctrl Pts',(2.65286911563599,-0.902114271336809,
23.2964212258986));
#61617=CARTESIAN_POINT('Ctrl Pts',(2.19894585862139,1.73671005470014,23.4549826703074));
#61618=CARTESIAN_POINT('Ctrl Pts',(-0.262894499289412,2.789697328652,23.6135441147161));
#61619=CARTESIAN_POINT('Ctrl Pts',(-2.10132025508898,1.55318133166961,23.7447465219153));
#61620=CARTESIAN_POINT('Ctrl Pts',(-2.36822982970795,0.381601828584115,
23.8230951143116));
#61621=CARTESIAN_POINT('Ctrl Pts',(-2.3679029786215,0.000227208911412861,
23.848589891905));
#61622=CARTESIAN_POINT('Origin',(0.,0.,-1.84858989190508));
#61623=CARTESIAN_POINT('',(-2.37546973462112,0.000647720784673299,21.651410108095));
#61624=CARTESIAN_POINT('',(-2.37407662519319,-0.00164808854746207,21.848589891905));
#61625=CARTESIAN_POINT('',(-2.37175,1.07555357745099E-12,-1.84858989190508));
#61626=CARTESIAN_POINT('Ctrl Pts',(-2.37546973462112,0.000647720784673306,
21.651410108095));
#61627=CARTESIAN_POINT('Ctrl Pts',(-2.37274529400723,-0.751516627875191,
21.7021050653699));
#61628=CARTESIAN_POINT('Ctrl Pts',(-1.57965287445059,-2.29572849416704,
21.8058498887759));
#61629=CARTESIAN_POINT('Ctrl Pts',(1.05299683804908,-2.60045372645548,21.9626445783133));
#61630=CARTESIAN_POINT('Ctrl Pts',(2.75712554852525,-0.519057447732828,
22.1217941767068));
#61631=CARTESIAN_POINT('Ctrl Pts',(1.92652156513405,2.03952851989154,22.2809437751004));
#61632=CARTESIAN_POINT('Ctrl Pts',(-0.675208582315117,2.72309663705597,
22.440093373494));
#61633=CARTESIAN_POINT('Ctrl Pts',(-2.21231188343661,1.31099872606338,22.5635821511589));
#61634=CARTESIAN_POINT('Ctrl Pts',(-2.37155587088784,0.261537227593486,
22.6340210626925));
#61635=CARTESIAN_POINT('Ctrl Pts',(-2.36962670248717,0.00189177622211021,
22.651410108095));
#61636=CARTESIAN_POINT('Ctrl Pts',(-2.37407662519319,-0.00164808854746259,
21.848589891905));
#61637=CARTESIAN_POINT('Ctrl Pts',(-2.37489245732554,-0.104570379898861,
21.8555160033433));
#61638=CARTESIAN_POINT('Ctrl Pts',(-2.32211136907176,-0.992060131910626,
21.9152959295845));
#61639=CARTESIAN_POINT('Ctrl Pts',(-1.20356513206848,-2.53040622748872,
22.0279296706286));
#61640=CARTESIAN_POINT('Ctrl Pts',(1.47008916186248,-2.38544808357241,22.1864911150373));
#61641=CARTESIAN_POINT('Ctrl Pts',(2.80136517195679,-0.0622725990490076,
22.3450525594461));
#61642=CARTESIAN_POINT('Ctrl Pts',(1.5746386679948,2.31776568455491,22.5036140038548));
#61643=CARTESIAN_POINT('Ctrl Pts',(-1.08993310932985,2.58138926170217,22.6621754482636));
#61644=CARTESIAN_POINT('Ctrl Pts',(-2.30056081128665,1.06313136545322,22.777167410947));
#61645=CARTESIAN_POINT('Ctrl Pts',(-2.37433540652935,0.140086014052276,
22.8393055588275));
#61646=CARTESIAN_POINT('Ctrl Pts',(-2.37310225641302,0.00197312592944565,
22.848589891905));
#61647=CARTESIAN_POINT('Origin',(0.,0.,-1.84858989190508));
#61648=CARTESIAN_POINT('',(-2.37160301736592,-0.00219628840535642,20.651410108095));
#61649=CARTESIAN_POINT('',(-2.3681294836508,-0.000785534163144364,20.848589891905));
#61650=CARTESIAN_POINT('',(-2.37175,1.07555357745099E-12,-1.84858989190508));
#61651=CARTESIAN_POINT('Ctrl Pts',(-2.37160301736592,-0.00219628840535644,
20.651410108095));
#61652=CARTESIAN_POINT('Ctrl Pts',(-2.37334397584842,-0.191117152306352,
20.6640893357849));
#61653=CARTESIAN_POINT('Ctrl Pts',(-2.26621572573114,-1.16853165787267,
20.7298184296059));
#61654=CARTESIAN_POINT('Ctrl Pts',(-0.91398305353419,-2.65250766299173,
20.8485973895582));
#61655=CARTESIAN_POINT('Ctrl Pts',(1.73810712782103,-2.20230459668849,21.0077469879518));
#61656=CARTESIAN_POINT('Ctrl Pts',(2.79228786153128,0.272562695031161,21.1668965863454));
#61657=CARTESIAN_POINT('Ctrl Pts',(1.2794098201712,2.49685250594164,21.326046184739));
#61658=CARTESIAN_POINT('Ctrl Pts',(-1.40967940307629,2.42568874856607,21.4851957831325));
#61659=CARTESIAN_POINT('Ctrl Pts',(-2.35903719972994,0.857509241612945,
21.5936504242512));
#61660=CARTESIAN_POINT('Ctrl Pts',(-2.37559629177148,0.0355876552723523,
21.6490551992387));
#61661=CARTESIAN_POINT('Ctrl Pts',(-2.37546973462112,0.000647720784673306,
21.651410108095));
#61662=CARTESIAN_POINT('Ctrl Pts',(-2.3681294836508,-0.000785534163144468,
20.848589891905));
#61663=CARTESIAN_POINT('Ctrl Pts',(-2.36916056635605,-0.346801018693284,
20.8717264478591));
#61664=CARTESIAN_POINT('Ctrl Pts',(-2.1362394959101,-1.48194260514544,20.9477168186161));
#61665=CARTESIAN_POINT('Ctrl Pts',(-0.386600015079116,-2.7752594710379,
21.0765610041761));
#61666=CARTESIAN_POINT('Ctrl Pts',(2.11959990940443,-1.83270863131529,21.2351224485848));
#61667=CARTESIAN_POINT('Ctrl Pts',(2.69033567115523,0.783338164367446,21.3936838929936));
#61668=CARTESIAN_POINT('Ctrl Pts',(0.804452967251542,2.68409763733083,21.5522453374023));
#61669=CARTESIAN_POINT('Ctrl Pts',(-1.70153384115788,2.1579663888224,21.7038806703728));
#61670=CARTESIAN_POINT('Ctrl Pts',(-2.36866676476808,0.680839409513659,
21.8026621885404));
#61671=CARTESIAN_POINT('Ctrl Pts',(-2.37407662519319,-0.00164808854746259,
21.848589891905));
#61672=CARTESIAN_POINT('Origin',(0.,0.,-1.84858989190508));
#61673=CARTESIAN_POINT('',(-2.36785111718193,0.000293968609762033,19.651410108095));
#61674=CARTESIAN_POINT('',(-2.37121668396496,0.00214562610995388,19.848589891905));
#61675=CARTESIAN_POINT('',(-2.37175,1.07555357745099E-12,-1.84858989190508));
#61676=CARTESIAN_POINT('Ctrl Pts',(-2.36785111718192,0.000293968609762288,
19.651410108095));
#61677=CARTESIAN_POINT('Ctrl Pts',(-2.36739457070405,-0.414287432580937,
19.679123472331));
#61678=CARTESIAN_POINT('Ctrl Pts',(-2.065941122802,-1.62309576599104,19.7598867026983));
#61679=CARTESIAN_POINT('Ctrl Pts',(-0.135862993192047,-2.80226750533537,
19.8936997991968));
#61680=CARTESIAN_POINT('Ctrl Pts',(2.28456502325081,-1.62847308203622,20.0528493975903));
#61681=CARTESIAN_POINT('Ctrl Pts',(2.60470360644785,1.04243994883883,20.211998995984));
#61682=CARTESIAN_POINT('Ctrl Pts',(0.530236912192428,2.75499741221771,20.3711485943775));
#61683=CARTESIAN_POINT('Ctrl Pts',(-1.82759145210684,2.0001243501166,20.5176189650812));
#61684=CARTESIAN_POINT('Ctrl Pts',(-2.36605980865027,0.599327406656931,
20.6110394696537));
#61685=CARTESIAN_POINT('Ctrl Pts',(-2.37160301736592,-0.00219628840535644,
20.651410108095));
#61686=CARTESIAN_POINT('Ctrl Pts',(-2.37121668396496,0.00214562610995377,
19.848589891905));
#61687=CARTESIAN_POINT('Ctrl Pts',(-2.36597598747472,-0.584372248785578,
19.8879368923749));
#61688=CARTESIAN_POINT('Ctrl Pts',(-1.850360793774,-1.96697607918093,19.9801377076478));
#61689=CARTESIAN_POINT('Ctrl Pts',(0.466180705424317,-2.76300565564655,
20.1251923377236));
#61690=CARTESIAN_POINT('Ctrl Pts',(2.57274555864665,-1.11018241460974,20.2837537821323));
#61691=CARTESIAN_POINT('Ctrl Pts',(2.33006666709568,1.55637849835264,20.4423152265411));
#61692=CARTESIAN_POINT('Ctrl Pts',(-0.0402592916836527,2.80176799408478,
20.6008766709498));
#61693=CARTESIAN_POINT('Ctrl Pts',(-2.03332046845351,1.68037126807848,20.7363015594045));
#61694=CARTESIAN_POINT('Ctrl Pts',(-2.36680513132683,0.443646720139554,
20.8188726330562));
#61695=CARTESIAN_POINT('Ctrl Pts',(-2.3681294836508,-0.000785534163144468,
20.848589891905));
#61696=CARTESIAN_POINT('Origin',(0.,0.,-1.84858989190508));
#61697=CARTESIAN_POINT('',(-2.37268542712431,0.00210147159002048,18.651410108095));
#61698=CARTESIAN_POINT('',(-2.37534353148036,-0.000727847436731155,18.848589891905));
#61699=CARTESIAN_POINT('',(-2.37175,1.07555357745099E-12,-1.84858989190508));
#61700=CARTESIAN_POINT('Ctrl Pts',(-2.37268542712431,0.00210147159002057,
18.651410108095));
#61701=CARTESIAN_POINT('Ctrl Pts',(-2.36681038593963,-0.634092970239114,
18.6941576088772));
#61702=CARTESIAN_POINT('Ctrl Pts',(-1.77494844826955,-2.06944727531261,
18.7899549757907));
#61703=CARTESIAN_POINT('Ctrl Pts',(0.653095138640082,-2.7284846827978,18.9388022088353));
#61704=CARTESIAN_POINT('Ctrl Pts',(2.64877844972125,-0.924734907240888,
19.0979518072289));
#61705=CARTESIAN_POINT('Ctrl Pts',(2.20933676661749,1.7291596155502,19.2571014056225));
#61706=CARTESIAN_POINT('Ctrl Pts',(-0.261234089078342,2.79337048654149,
19.416251004016));
#61707=CARTESIAN_POINT('Ctrl Pts',(-2.10325227673128,1.55139759182543,19.5476872381736));
#61708=CARTESIAN_POINT('Ctrl Pts',(-2.36826850752845,0.379318412104361,
19.6260736061998));
#61709=CARTESIAN_POINT('Ctrl Pts',(-2.36785111718192,0.000293968609762288,
19.651410108095));
#61710=CARTESIAN_POINT('Ctrl Pts',(-2.37534353148036,-0.000727847436731129,
18.848589891905));
#61711=CARTESIAN_POINT('Ctrl Pts',(-2.37550564871799,-0.0408474181895097,
18.8512935220879));
#61712=CARTESIAN_POINT('Ctrl Pts',(-2.35642199299718,-0.865115184557848,
18.9068509670736));
#61713=CARTESIAN_POINT('Ctrl Pts',(-1.40094218755544,-2.42670263740165,
19.0152622268623));
#61714=CARTESIAN_POINT('Ctrl Pts',(1.27577326591705,-2.49478000577529,19.1738236712711));
#61715=CARTESIAN_POINT('Ctrl Pts',(2.7875455501625,-0.284806090198347,19.3323851156798));
#61716=CARTESIAN_POINT('Ctrl Pts',(1.75393439181258,2.18523199053596,19.4909465600886));
#61717=CARTESIAN_POINT('Ctrl Pts',(-0.88124182797927,2.65987547525528,19.6495080044973));
#61718=CARTESIAN_POINT('Ctrl Pts',(-2.25749629369168,1.19063929439144,19.7687224484361));
#61719=CARTESIAN_POINT('Ctrl Pts',(-2.37301568042272,0.203482143368676,
19.835083077572));
#61720=CARTESIAN_POINT('Ctrl Pts',(-2.37121668396496,0.00214562610995377,
19.848589891905));
#61721=CARTESIAN_POINT('Origin',(0.,0.,-1.84858989190508));
#61722=CARTESIAN_POINT('',(-2.37489284321081,-0.00123559705226072,17.651410108095));
#61723=CARTESIAN_POINT('',(-2.36912129924534,-0.00162542170875829,17.848589891905));
#61724=CARTESIAN_POINT('',(-2.37175,1.07555357745099E-12,-1.84858989190508));
#61725=CARTESIAN_POINT('Ctrl Pts',(-2.37489284321081,-0.00123559705226036,
17.651410108095));
#61726=CARTESIAN_POINT('Ctrl Pts',(-2.3753368409954,-0.0714864407096927,
17.6561418792922));
#61727=CARTESIAN_POINT('Ctrl Pts',(-2.34058824250688,-0.928903408008142,
17.7139235166207));
#61728=CARTESIAN_POINT('Ctrl Pts',(-1.29962352880245,-2.48639108101694,
17.8247550200804));
#61729=CARTESIAN_POINT('Ctrl Pts',(1.38995452278499,-2.43704500347595,17.9839046184738));
#61730=CARTESIAN_POINT('Ctrl Pts',(2.80169335019333,-0.147228719548932,
18.1430542168675));
#61731=CARTESIAN_POINT('Ctrl Pts',(1.63772657118694,2.27794064944762,18.302203815261));
#61732=CARTESIAN_POINT('Ctrl Pts',(-1.0318659076804,2.60891062954338,18.4613534136547));
#61733=CARTESIAN_POINT('Ctrl Pts',(-2.2905754966375,1.09673789523524,18.5777555112659));
#61734=CARTESIAN_POINT('Ctrl Pts',(-2.37410134196417,0.155427571425982,
18.641107742746));
#61735=CARTESIAN_POINT('Ctrl Pts',(-2.37268542712431,0.00210147159002057,
18.651410108095));
#61736=CARTESIAN_POINT('Ctrl Pts',(-2.36912129924534,-0.0016254217087585,
17.848589891905));
#61737=CARTESIAN_POINT('Ctrl Pts',(-2.37091015942674,-0.284195516689885,
17.8675039666037));
#61738=CARTESIAN_POINT('Ctrl Pts',(-2.19351504650125,-1.35421254674421,
17.9392718561053));
#61739=CARTESIAN_POINT('Ctrl Pts',(-0.606031153241877,-2.7357359054823,
18.0638935604098));
#61740=CARTESIAN_POINT('Ctrl Pts',(1.96717496328582,-1.9954316242523,18.2224550048186));
#61741=CARTESIAN_POINT('Ctrl Pts',(2.7441002692833,0.566955390982473,18.3810164492273));
#61742=CARTESIAN_POINT('Ctrl Pts',(1.01531319693132,2.61164006237112,18.5395778936361));
#61743=CARTESIAN_POINT('Ctrl Pts',(-1.59529820733317,2.27736397432732,18.6954357078619));
#61744=CARTESIAN_POINT('Ctrl Pts',(-2.37233638595852,0.743458207631327,
18.7984397072849));
#61745=CARTESIAN_POINT('Ctrl Pts',(-2.37534353148036,-0.000727847436731129,
18.848589891905));
#61746=CARTESIAN_POINT('Origin',(0.,0.,-1.84858989190508));
#61747=CARTESIAN_POINT('',(-2.36883928475605,-0.0015223826853693,16.651410108095));
#61748=CARTESIAN_POINT('',(-2.36951653941713,0.0018022559201944,16.848589891905));
#61749=CARTESIAN_POINT('',(-2.37175,1.07555357745099E-12,-1.84858989190508));
#61750=CARTESIAN_POINT('Ctrl Pts',(-2.36883928475605,-0.00152238268536945,
16.651410108095));
#61751=CARTESIAN_POINT('Ctrl Pts',(-2.37056689977668,-0.296904640803646,
16.6711760158384));
#61752=CARTESIAN_POINT('Ctrl Pts',(-2.18214828101389,-1.38294063098053,
16.743991789713));
#61753=CARTESIAN_POINT('Ctrl Pts',(-0.552569484305025,-2.75060518602588,
16.8698574297189));
#61754=CARTESIAN_POINT('Ctrl Pts',(2.01593436473937,-1.95119721233924,17.0290070281124));
#61755=CARTESIAN_POINT('Ctrl Pts',(2.73111138732539,0.642022207091869,17.188156626506));
#61756=CARTESIAN_POINT('Ctrl Pts',(0.935471545677604,2.64500565436165,17.3473062248996));
#61757=CARTESIAN_POINT('Ctrl Pts',(-1.64122679092401,2.22907771841236,17.5017240520959));
#61758=CARTESIAN_POINT('Ctrl Pts',(-2.37035899611375,0.716125152553366,
17.603092013161));
#61759=CARTESIAN_POINT('Ctrl Pts',(-2.37489284321081,-0.00123559705226036,
17.651410108095));
#61760=CARTESIAN_POINT('Ctrl Pts',(-2.36951653941713,0.00180225592019443,
16.848589891905));
#61761=CARTESIAN_POINT('Ctrl Pts',(-2.36579276584773,-0.522726350568018,
16.8837144111195));
#61762=CARTESIAN_POINT('Ctrl Pts',(-1.93551536846003,-1.84209105910571,
16.9716927451369));
#61763=CARTESIAN_POINT('Ctrl Pts',(0.245024140396729,-2.79132367773206,
17.1125248939573));
#61764=CARTESIAN_POINT('Ctrl Pts',(2.47633259500592,-1.31122140851802,17.271086338366));
#61765=CARTESIAN_POINT('Ctrl Pts',(2.44643459674846,1.3661926903175,17.4296477827748));
#61766=CARTESIAN_POINT('Ctrl Pts',(0.182630818693805,2.79609919124984,17.5882092271835));
#61767=CARTESIAN_POINT('Ctrl Pts',(-1.9580065820238,1.80680355351091,17.7278565968936));
#61768=CARTESIAN_POINT('Ctrl Pts',(-2.36591133784849,0.505423204125703,
17.8146501518008));
#61769=CARTESIAN_POINT('Ctrl Pts',(-2.36912129924534,-0.0016254217087585,
17.848589891905));
#61770=CARTESIAN_POINT('Origin',(0.,0.,-1.84858989190508));
#61771=CARTESIAN_POINT('',(-2.36932045623978,0.00177252062842899,15.651410108095));
#61772=CARTESIAN_POINT('',(-2.37552790433159,0.000415529653166168,15.848589891905));
#61773=CARTESIAN_POINT('',(-2.37175,1.07555357745099E-12,-1.84858989190508));
#61774=CARTESIAN_POINT('Ctrl Pts',(-2.36932045623978,0.00177252062842921,
15.651410108095));
#61775=CARTESIAN_POINT('Ctrl Pts',(-2.3657336259535,-0.518015199574277,
15.6862101523846));
#61776=CARTESIAN_POINT('Ctrl Pts',(-1.94098877146081,-1.83550765140878,
15.7740600628054));
#61777=CARTESIAN_POINT('Ctrl Pts',(0.238564168873022,-2.7953978360347,15.9149598393574));
#61778=CARTESIAN_POINT('Ctrl Pts',(2.48109896001892,-1.30969839084066,16.074109437751));
#61779=CARTESIAN_POINT('Ctrl Pts',(2.4426630300295,1.38005769665789,16.2332590361446));
#61780=CARTESIAN_POINT('Ctrl Pts',(0.158592023455111,2.80107309695302,16.3924086345381));
#61781=CARTESIAN_POINT('Ctrl Pts',(-1.96949605169442,1.79029139008163,16.5317923251883));
#61782=CARTESIAN_POINT('Ctrl Pts',(-2.36593014103228,0.495873988647358,
16.6181261497072));
#61783=CARTESIAN_POINT('Ctrl Pts',(-2.36883928475605,-0.00152238268536945,
16.651410108095));
#61784=CARTESIAN_POINT('Ctrl Pts',(-2.37552790433159,0.000415529653166134,
15.848589891905));
#61785=CARTESIAN_POINT('Ctrl Pts',(-2.37368024029323,-0.761193483430817,
15.8999248556353));
#61786=CARTESIAN_POINT('Ctrl Pts',(-1.56394205346637,-2.31032295076223,
16.0041136341686));
#61787=CARTESIAN_POINT('Ctrl Pts',(1.07337977774581,-2.5883161622899,16.1611562275048));
#61788=CARTESIAN_POINT('Ctrl Pts',(2.75607650988087,-0.505536324043674,
16.3197176719135));
#61789=CARTESIAN_POINT('Ctrl Pts',(1.92212503357044,2.03886244228653,16.4782791163223));
#61790=CARTESIAN_POINT('Ctrl Pts',(-0.666970940652513,2.72152061678207,
16.636840560731));
#61791=CARTESIAN_POINT('Ctrl Pts',(-2.20841342965836,1.31836001741498,16.7602774859253));
#61792=CARTESIAN_POINT('Ctrl Pts',(-2.37139613474805,0.26656097481449,16.8308605963166));
#61793=CARTESIAN_POINT('Ctrl Pts',(-2.36951653941713,0.00180225592019443,
16.848589891905));
#61794=CARTESIAN_POINT('Origin',(0.,0.,-1.84858989190508));
#61795=CARTESIAN_POINT('',(-2.37529741037155,0.000871252838594932,14.651410108095));
#61796=CARTESIAN_POINT('',(-2.37070442127403,-0.00209855721355318,14.848589891905));
#61797=CARTESIAN_POINT('',(-2.37175,1.07555357745099E-12,-1.84858989190508));
#61798=CARTESIAN_POINT('Ctrl Pts',(-2.37529741037155,0.000871252838595101,
14.651410108095));
#61799=CARTESIAN_POINT('Ctrl Pts',(-2.37181600276552,-0.73866462242614,
14.7012442889308));
#61800=CARTESIAN_POINT('Ctrl Pts',(-1.60226833365963,-2.27170433151576,
14.8041283358978));
#61801=CARTESIAN_POINT('Ctrl Pts',(1.01066706572481,-2.61719582886661,14.960062248996));
#61802=CARTESIAN_POINT('Ctrl Pts',(2.74834116840978,-0.563722224505545,
15.1192118473896));
#61803=CARTESIAN_POINT('Ctrl Pts',(1.95935839934075,2.00800313428798,15.2783614457831));
#61804=CARTESIAN_POINT('Ctrl Pts',(-0.630938711931175,2.73369315508602,
15.4375110441767));
#61805=CARTESIAN_POINT('Ctrl Pts',(-2.20162297148963,1.3370520367252,15.5618605982807));
#61806=CARTESIAN_POINT('Ctrl Pts',(-2.37120145998666,0.274359337190549,
15.6331602862534));
#61807=CARTESIAN_POINT('Ctrl Pts',(-2.36932045623978,0.00177252062842921,
15.651410108095));
#61808=CARTESIAN_POINT('Ctrl Pts',(-2.37070442127403,-0.00209855721355335,
14.848589891905));
#61809=CARTESIAN_POINT('Ctrl Pts',(-2.37258491227423,-0.221216123050188,
14.8632814853483));
#61810=CARTESIAN_POINT('Ctrl Pts',(-2.2443457179653,-1.22646135653919,14.9308268935944));
#61811=CARTESIAN_POINT('Ctrl Pts',(-0.821625189105414,-2.678890955577,15.0512261166435));
#61812=CARTESIAN_POINT('Ctrl Pts',(1.80229479678065,-2.14552048900545,15.2097875610522));
#61813=CARTESIAN_POINT('Ctrl Pts',(2.78049052387073,0.346982924521951,15.368349005461));
#61814=CARTESIAN_POINT('Ctrl Pts',(1.21974494421116,2.52264681917943,15.5269104498698));
#61815=CARTESIAN_POINT('Ctrl Pts',(-1.45478282458735,2.394813486794,15.6854718942785));
#61816=CARTESIAN_POINT('Ctrl Pts',(-2.36509470132286,0.82957372331575,15.7926983749569));
#61817=CARTESIAN_POINT('Ctrl Pts',(-2.37558257129349,0.0229493074598575,
15.8470710408324));
#61818=CARTESIAN_POINT('Ctrl Pts',(-2.37552790433159,0.000415529653166134,
15.848589891905));
#61819=CARTESIAN_POINT('Origin',(0.,0.,-1.84858989190508));
#61820=CARTESIAN_POINT('',(-2.3719949540914,-0.00218192237732729,13.651410108095));
#61821=CARTESIAN_POINT('',(-2.36833556860473,0.00104783714029014,13.848589891905));
#61822=CARTESIAN_POINT('',(-2.37175,1.07555357745099E-12,-1.84858989190508));
#61823=CARTESIAN_POINT('Ctrl Pts',(-2.3719949540914,-0.00218192237732709,
13.651410108095));
#61824=CARTESIAN_POINT('Ctrl Pts',(-2.37363184364254,-0.178202818064253,
13.6632285593458));
#61825=CARTESIAN_POINT('Ctrl Pts',(-2.27525263091362,-1.14252130340604,
13.7280968767278));
#61826=CARTESIAN_POINT('Ctrl Pts',(-0.956898470366649,-2.63732956639619,
13.846015060241));
#61827=CARTESIAN_POINT('Ctrl Pts',(1.70214696396934,-2.23021470657591,14.0051646586345));
#61828=CARTESIAN_POINT('Ctrl Pts',(2.79634252716041,0.227223227623548,14.1643142570281));
#61829=CARTESIAN_POINT('Ctrl Pts',(1.31975170355224,2.47576601587237,14.3234638554217));
#61830=CARTESIAN_POINT('Ctrl Pts',(-1.37013816353632,2.4482408658461,14.4826134538153));
#61831=CARTESIAN_POINT('Ctrl Pts',(-2.35254974335426,0.883348319972068,
14.591928871373));
#61832=CARTESIAN_POINT('Ctrl Pts',(-2.37552205761282,0.0485918052708133,
14.6481944227996));
#61833=CARTESIAN_POINT('Ctrl Pts',(-2.37529741037155,0.000871252838595101,
14.651410108095));
#61834=CARTESIAN_POINT('Ctrl Pts',(-2.36833556860473,0.0010478371402901,
13.848589891905));
#61835=CARTESIAN_POINT('Ctrl Pts',(-2.36648927158143,-0.461002671016135,
13.8794919298641));
#61836=CARTESIAN_POINT('Ctrl Pts',(-2.01294080374263,-1.71593888244227,
13.9632477826261));
#61837=CARTESIAN_POINT('Ctrl Pts',(0.022316198533973,-2.80196836001547,
14.099857450191));
#61838=CARTESIAN_POINT('Ctrl Pts',(2.36424066594685,-1.50395836934669,14.2584188945997));
#61839=CARTESIAN_POINT('Ctrl Pts',(2.5473128609508,1.16735679707592,14.4169803390085));
#61840=CARTESIAN_POINT('Ctrl Pts',(0.404364597205185,2.77272681232246,14.5755417834172));
#61841=CARTESIAN_POINT('Ctrl Pts',(-1.87505217600518,1.93208845330377,14.7194116343828));
#61842=CARTESIAN_POINT('Ctrl Pts',(-2.36581974255682,0.567071361866622,
14.8104276705453));
#61843=CARTESIAN_POINT('Ctrl Pts',(-2.37070442127403,-0.00209855721355335,
14.848589891905));
#61844=CARTESIAN_POINT('Origin',(0.,0.,-1.84858989190508));
#61845=CARTESIAN_POINT('',(-2.36782090892634,8.12663433023876E-5,12.651410108095));
#61846=CARTESIAN_POINT('',(-2.3745092207065,0.00142872646625845,12.848589891905));
#61847=CARTESIAN_POINT('',(-2.37175,1.07555357745099E-12,-1.84858989190508));
#61848=CARTESIAN_POINT('Ctrl Pts',(-2.36782090892634,8.126634330273E-5,
12.651410108095));
#61849=CARTESIAN_POINT('Ctrl Pts',(-2.3676987046513,-0.401636019150047,
12.6782626958919));
#61850=CARTESIAN_POINT('Ctrl Pts',(-2.07971230686784,-1.59714884508751,
12.7581651498201));
#61851=CARTESIAN_POINT('Ctrl Pts',(-0.181310616086829,-2.79969433775756,
12.8911174698795));
#61852=CARTESIAN_POINT('Ctrl Pts',(2.25784308439087,-1.66532475230686,13.0502670682731));
#61853=CARTESIAN_POINT('Ctrl Pts',(2.62127386877248,1.00004261372609,13.2094166666667));
#61854=CARTESIAN_POINT('Ctrl Pts',(0.574865689414601,2.74603193053384,13.3685662650602));
#61855=CARTESIAN_POINT('Ctrl Pts',(-1.80882641908756,2.02530207859848,13.515897412203));
#61856=CARTESIAN_POINT('Ctrl Pts',(-2.366284284329,0.611907895625466,13.6101786932146));
#61857=CARTESIAN_POINT('Ctrl Pts',(-2.3719949540914,-0.00218192237732709,
13.651410108095));
#61858=CARTESIAN_POINT('Ctrl Pts',(-2.3745092207065,0.00142872646625845,
12.848589891905));
#61859=CARTESIAN_POINT('Ctrl Pts',(-2.36952764776996,-0.698330449908164,
12.8957023743799));
#61860=CARTESIAN_POINT('Ctrl Pts',(-1.67258769039563,-2.19175214238388,
12.9956686716578));
#61861=CARTESIAN_POINT('Ctrl Pts',(0.864190157080086,-2.66546432646371,
13.1484887837385));
#61862=CARTESIAN_POINT('Ctrl Pts',(2.70715729817405,-0.723065741262676,
13.3070502281472));
#61863=CARTESIAN_POINT('Ctrl Pts',(2.07814568976501,1.87958378247841,13.465611672556));
#61864=CARTESIAN_POINT('Ctrl Pts',(-0.448477109148286,2.76593437843611,
13.6241731169647));
#61865=CARTESIAN_POINT('Ctrl Pts',(-2.15298049765028,1.44611826026627,13.7518325234144));
#61866=CARTESIAN_POINT('Ctrl Pts',(-2.3696471164158,0.329273103676635,13.8266381150612));
#61867=CARTESIAN_POINT('Ctrl Pts',(-2.36833556860473,0.0010478371402901,
13.848589891905));
#61868=CARTESIAN_POINT('Origin',(0.,0.,-1.84858989190508));
#61869=CARTESIAN_POINT('',(-2.37229421808997,0.00215578506045859,11.651410108095));
#61870=CARTESIAN_POINT('',(-2.37257814772649,-0.00207573294591201,11.848589891905));
#61871=CARTESIAN_POINT('',(-2.37175,1.07555357745099E-12,-1.84858989190508));
#61872=CARTESIAN_POINT('Ctrl Pts',(-2.37229421808997,0.00215578506045873,
11.651410108095));
#61873=CARTESIAN_POINT('Ctrl Pts',(-2.36649070893558,-0.621492334890488,
11.6932968324381));
#61874=CARTESIAN_POINT('Ctrl Pts',(-1.79431307440946,-2.04441564917251,
11.7882334229125));
#61875=CARTESIAN_POINT('Ctrl Pts',(0.608740760399282,-2.7387217111284,11.9362198795181));
#61876=CARTESIAN_POINT('Ctrl Pts',(2.63342640009004,-0.967588404067735,
12.0953694779116));
#61877=CARTESIAN_POINT('Ctrl Pts',(2.23710078159852,1.69308653569416,12.2545190763052));
#61878=CARTESIAN_POINT('Ctrl Pts',(-0.21587854772131,2.79724120822844,12.4136686746988));
#61879=CARTESIAN_POINT('Ctrl Pts',(-2.08999848010885,1.57738079894681,12.5459656852954));
#61880=CARTESIAN_POINT('Ctrl Pts',(-2.36794013093322,0.391995059504984,
12.6252128297608));
#61881=CARTESIAN_POINT('Ctrl Pts',(-2.36782090892634,8.126634330273E-5,
12.651410108095));
#61882=CARTESIAN_POINT('Ctrl Pts',(-2.37257814772649,-0.00207573294591234,
11.848589891905));
#61883=CARTESIAN_POINT('Ctrl Pts',(-2.3740036192897,-0.157902106076437,
11.8590590040928));
#61884=CARTESIAN_POINT('Ctrl Pts',(-2.28906614944607,-1.0988790069114,11.9223819310836));
#61885=CARTESIAN_POINT('Ctrl Pts',(-1.03201708332093,-2.60508453662804,
12.0385586728772));
#61886=CARTESIAN_POINT('Ctrl Pts',(1.6260033530305,-2.28202493395194,12.197120117286));
#61887=CARTESIAN_POINT('Ctrl Pts',(2.7992760290567,0.124813526483961,12.3556815616948));
#61888=CARTESIAN_POINT('Ctrl Pts',(1.41645384406812,2.41768137083226,12.5142430061035));
#61889=CARTESIAN_POINT('Ctrl Pts',(-1.25977076144102,2.50289878578082,12.6728044505123));
#61890=CARTESIAN_POINT('Ctrl Pts',(-2.33228417027533,0.956398728600941,
12.7842534124461));
#61891=CARTESIAN_POINT('Ctrl Pts',(-2.37511629688339,0.0867044277261085,
12.842848559577));
#61892=CARTESIAN_POINT('Ctrl Pts',(-2.3745092207065,0.00142872646625845,
12.848589891905));
#61893=CARTESIAN_POINT('Origin',(0.,0.,-1.84858989190508));
#61894=CARTESIAN_POINT('',(-2.37513726959577,-0.00103386453644136,10.651410108095));
#61895=CARTESIAN_POINT('',(-2.36788450901277,6.16867972168256E-5,10.848589891905));
#61896=CARTESIAN_POINT('',(-2.37175,1.07555357745099E-12,-1.84858989190508));
#61897=CARTESIAN_POINT('Ctrl Pts',(-2.37513726959577,-0.00103386453644157,
10.651410108095));
#61898=CARTESIAN_POINT('Ctrl Pts',(-2.37545044739491,-0.0584894452066465,
10.6552811028531));
#61899=CARTESIAN_POINT('Ctrl Pts',(-2.34746382585173,-0.903032024338962,
10.7122019637425));
#61900=CARTESIAN_POINT('Ctrl Pts',(-1.33979301969774,-2.46497800978969,
10.8221726907631));
#61901=CARTESIAN_POINT('Ctrl Pts',(1.35023162953112,-2.4592755988281,10.9813222891566));
#61902=CARTESIAN_POINT('Ctrl Pts',(2.79893585448806,-0.192665531008406,
11.1404718875502));
#61903=CARTESIAN_POINT('Ctrl Pts',(1.67446954602361,2.25106944891023,11.2996214859438));
#61904=CARTESIAN_POINT('Ctrl Pts',(-0.989401707370339,2.62530877914012,
11.4587710843374));
#61905=CARTESIAN_POINT('Ctrl Pts',(-2.2819681016055,1.12272726704564,11.5760339583877));
#61906=CARTESIAN_POINT('Ctrl Pts',(-2.37384089896737,0.168362918657281,
11.6402469663069));
#61907=CARTESIAN_POINT('Ctrl Pts',(-2.37229421808997,0.00215578506045873,
11.651410108095));
#61908=CARTESIAN_POINT('Ctrl Pts',(-2.36788450901277,6.16867972165827E-5,
10.848589891905));
#61909=CARTESIAN_POINT('Ctrl Pts',(-2.367791686282,-0.399043730343822,10.8752694486087));
#61910=CARTESIAN_POINT('Ctrl Pts',(-2.08295912267226,-1.58892555039052,
10.9548028201152));
#61911=CARTESIAN_POINT('Ctrl Pts',(-0.200533038930914,-2.79487230540894,
11.0871900064247));
#61912=CARTESIAN_POINT('Ctrl Pts',(2.23717948448735,-1.68717297792302,11.2457514508335));
#61913=CARTESIAN_POINT('Ctrl Pts',(2.63206274630088,0.961129753352717,11.4043128952422));
#61914=CARTESIAN_POINT('Ctrl Pts',(0.623538130558561,2.73179884013891,11.562874339651));
#61915=CARTESIAN_POINT('Ctrl Pts',(-1.78414908989376,2.05577833064682,11.7109666718719));
#61916=CARTESIAN_POINT('Ctrl Pts',(-2.36680705776116,0.628794809487644,
11.8062051892899));
#61917=CARTESIAN_POINT('Ctrl Pts',(-2.37257814772649,-0.00207573294591234,
11.848589891905));
#61918=CARTESIAN_POINT('Origin',(0.,0.,-1.84858989190508));
#61919=CARTESIAN_POINT('',(-2.36910288125725,-0.0016703647433169,9.65141010809496));
#61920=CARTESIAN_POINT('',(-2.37280337475969,0.00203709636048592,9.84858989190502));
#61921=CARTESIAN_POINT('',(-2.37175,1.07555357745099E-12,-1.84858989190508));
#61922=CARTESIAN_POINT('Ctrl Pts',(-2.36910288125725,-0.0016703647433166,
9.65141010809496));
#61923=CARTESIAN_POINT('Ctrl Pts',(-2.37092842223778,-0.284110306409195,
9.67031523939932));
#61924=CARTESIAN_POINT('Ctrl Pts',(-2.19330740190733,-1.35688708086049,
9.74227023683487));
#61925=CARTESIAN_POINT('Ctrl Pts',(-0.597124060110883,-2.74127794672745,
9.86727510040159));
#61926=CARTESIAN_POINT('Ctrl Pts',(1.98401173368511,-1.98364799422109,10.0264246987952));
#61927=CARTESIAN_POINT('Ctrl Pts',(2.74116841667201,0.597626669265515,10.1855742971888));
#61928=CARTESIAN_POINT('Ctrl Pts',(0.978262417402176,2.6294799042921,10.3447238955823));
#61929=CARTESIAN_POINT('Ctrl Pts',(-1.6192440991928,2.25332728858875,10.5000024992177));
#61930=CARTESIAN_POINT('Ctrl Pts',(-2.37115851693319,0.728907865680533,
10.6022312367219));
#61931=CARTESIAN_POINT('Ctrl Pts',(-2.37513726959577,-0.00103386453644157,
10.651410108095));
#61932=CARTESIAN_POINT('Ctrl Pts',(-2.37280337475968,0.00203709636048583,
9.84858989190502));
#61933=CARTESIAN_POINT('Ctrl Pts',(-2.36701047519887,-0.636198310368005,
9.8914798931245));
#61934=CARTESIAN_POINT('Ctrl Pts',(-1.77272462907463,-2.07044996200305,
9.9872237091469));
#61935=CARTESIAN_POINT('Ctrl Pts',(0.649528893544149,-2.72573603265175,
10.1358213399722));
#61936=CARTESIAN_POINT('Ctrl Pts',(2.64109764832668,-0.936017048588331,
10.294382784381));
#61937=CARTESIAN_POINT('Ctrl Pts',(2.22100851147896,1.70840448816513,10.4529442287897));
#61938=CARTESIAN_POINT('Ctrl Pts',(-0.22714373294823,2.79283555330906,10.6115056731985));
#61939=CARTESIAN_POINT('Ctrl Pts',(-2.09085765599782,1.57368542285565,10.7433875609036));
#61940=CARTESIAN_POINT('Ctrl Pts',(-2.36797557372347,0.391608229833928,
10.8224156338057));
#61941=CARTESIAN_POINT('Ctrl Pts',(-2.36788450901277,6.16867972165827E-5,
10.848589891905));
#61942=CARTESIAN_POINT('Origin',(0.,0.,-1.84858989190508));
#61943=CARTESIAN_POINT('',(-2.36903760879731,0.00163642073173795,8.65141010809496));
#61944=CARTESIAN_POINT('',(-2.37433059532467,-0.00152653879847225,8.84858989190501));
#61945=CARTESIAN_POINT('',(-2.37175,1.07555357745099E-12,-1.84858989190508));
#61946=CARTESIAN_POINT('Ctrl Pts',(-2.36903760879731,0.00163642073173823,
8.65141010809496));
#61947=CARTESIAN_POINT('Ctrl Pts',(-2.36583245845381,-0.505446425674836,
8.6853493759455));
#61948=CARTESIAN_POINT('Ctrl Pts',(-1.95729525761598,-1.80985376099157,
8.77233850992723));
#61949=CARTESIAN_POINT('Ctrl Pts',(0.19317871866267,-2.79890048180234,8.91237751004016));
#61950=CARTESIAN_POINT('Ctrl Pts',(2.4595231253557,-1.34978069337877,9.07152710843373));
#61951=CARTESIAN_POINT('Ctrl Pts',(2.46473231443179,1.34024495618274,9.23067670682731));
#61952=CARTESIAN_POINT('Ctrl Pts',(0.204017275877662,2.79813131849115,9.38982630522089));
#61953=CARTESIAN_POINT('Ctrl Pts',(-1.95343190101933,1.81598178609972,9.53007077231009));
#61954=CARTESIAN_POINT('Ctrl Pts',(-2.36580575458343,0.50844706091372,9.61726537326812));
#61955=CARTESIAN_POINT('Ctrl Pts',(-2.36910288125725,-0.0016703647433166,
9.65141010809496));
#61956=CARTESIAN_POINT('Ctrl Pts',(-2.37433059532467,-0.00152653879847217,
8.84858989190501));
#61957=CARTESIAN_POINT('Ctrl Pts',(-2.37502560197468,-0.094325735057865,
8.85483652283741));
#61958=CARTESIAN_POINT('Ctrl Pts',(-2.32799838253791,-0.971604165542515,
8.91393696857272));
#61959=CARTESIAN_POINT('Ctrl Pts',(-1.23587473403734,-2.51478395593197,
9.02589122911094));
#61960=CARTESIAN_POINT('Ctrl Pts',(1.43941682598108,-2.40408067758287,9.1844526735197));
#61961=CARTESIAN_POINT('Ctrl Pts',(2.8003378439175,-0.0981461317030541,
9.34301411792845));
#61962=CARTESIAN_POINT('Ctrl Pts',(1.60419442889238,2.29740830884616,9.5015755623372));
#61963=CARTESIAN_POINT('Ctrl Pts',(-1.05678242634981,2.59513691480873,9.66013700674596));
#61964=CARTESIAN_POINT('Ctrl Pts',(-2.29402384393756,1.08362978939683,9.77580844993522));
#61965=CARTESIAN_POINT('Ctrl Pts',(-2.37414912830807,0.150306120239738,
9.83862607832158));
#61966=CARTESIAN_POINT('Ctrl Pts',(-2.37280337475968,0.00203709636048583,
9.84858989190502));
#61967=CARTESIAN_POINT('Origin',(0.,0.,-1.84858989190508));
#61968=CARTESIAN_POINT('',(-2.37508229419387,0.00108330972966132,7.65141010809496));
#61969=CARTESIAN_POINT('',(-2.36824036561998,-0.000937958850331377,7.84858989190501));
#61970=CARTESIAN_POINT('',(-2.37175,1.07555357745099E-12,-1.84858989190508));
#61971=CARTESIAN_POINT('Ctrl Pts',(-2.37508229419387,0.00108330972966112,
7.65141010809496));
#61972=CARTESIAN_POINT('Ctrl Pts',(-2.3709611151748,-0.725853319007325,
7.70038351249169));
#61973=CARTESIAN_POINT('Ctrl Pts',(-1.62452387639323,-2.24755017347193,
7.8024067830196));
#61974=CARTESIAN_POINT('Ctrl Pts',(0.968071232182813,-2.63324894641536,
7.95747991967872));
#61975=CARTESIAN_POINT('Ctrl Pts',(2.73883327901741,-0.608238599666532,
8.11662951807229));
#61976=CARTESIAN_POINT('Ctrl Pts',(1.99167942641439,1.9759491356751,8.27577911646587));
#61977=CARTESIAN_POINT('Ctrl Pts',(-0.586502744988177,2.74357001997377,
8.43492871485943));
#61978=CARTESIAN_POINT('Ctrl Pts',(-2.19066818915132,1.36310617154104,8.56013904540247));
#61979=CARTESIAN_POINT('Ctrl Pts',(-2.37084237196762,0.287165755523453,
8.63229950981431));
#61980=CARTESIAN_POINT('Ctrl Pts',(-2.36903760879731,0.00163642073173823,
8.65141010809496));
#61981=CARTESIAN_POINT('Ctrl Pts',(-2.36824036561998,-0.000937958850331759,
7.84858989190501));
#61982=CARTESIAN_POINT('Ctrl Pts',(-2.3694385945702,-0.336752264496505,
7.87104696735324));
#61983=CARTESIAN_POINT('Ctrl Pts',(-2.14590544977689,-1.46139918005804,
7.94635785760438));
#61984=CARTESIAN_POINT('Ctrl Pts',(-0.422112596148098,-2.77008044277018,
8.07452256265844));
#61985=CARTESIAN_POINT('Ctrl Pts',(2.09595354186346,-1.85970520609983,8.23308400706718));
#61986=CARTESIAN_POINT('Ctrl Pts',(2.70014765665469,0.748817291137776,8.39164545147595));
#61987=CARTESIAN_POINT('Ctrl Pts',(0.838763715722044,2.67357441123917,8.55020689588469));
#61988=CARTESIAN_POINT('Ctrl Pts',(-1.68501465022418,2.17736829258185,8.70252170936105));
#61989=CARTESIAN_POINT('Ctrl Pts',(-2.36914503160584,0.690864167473078,
8.80198270803449));
#61990=CARTESIAN_POINT('Ctrl Pts',(-2.37433059532467,-0.00152653879847217,
8.84858989190501));
#61991=CARTESIAN_POINT('Origin',(0.,0.,-1.84858989190508));
#61992=CARTESIAN_POINT('',(-2.37238791048953,-0.00214487927112815,6.65141010809495));
#61993=CARTESIAN_POINT('',(-2.37092048416906,0.00212358946080196,6.84858989190502));
#61994=CARTESIAN_POINT('',(-2.37175,1.07555357745099E-12,-1.84858989190508));
#61995=CARTESIAN_POINT('Ctrl Pts',(-2.37238791048953,-0.00214487927112778,
6.65141010809496));
#61996=CARTESIAN_POINT('Ctrl Pts',(-2.37390455983555,-0.165276290284716,
6.66236778290668));
#61997=CARTESIAN_POINT('Ctrl Pts',(-2.28404464566905,-1.11652245665044,
6.72637532384959));
#61998=CARTESIAN_POINT('Ctrl Pts',(-0.999561980729776,-2.62145718466985,
6.84343273092369));
#61999=CARTESIAN_POINT('Ctrl Pts',(1.66573870468711,-2.25753770557323,7.00258232931727));
#62000=CARTESIAN_POINT('Ctrl Pts',(2.79966104700711,0.181823943001463,7.16173192771085));
#62001=CARTESIAN_POINT('Ctrl Pts',(1.35974615823274,2.45402777277456,7.32088152610442));
#62002=CARTESIAN_POINT('Ctrl Pts',(-1.33023623090505,2.47014847617812,7.48003112449799));
#62003=CARTESIAN_POINT('Ctrl Pts',(-2.34584281991666,0.909205872162835,
7.59020731849484));
#62004=CARTESIAN_POINT('Ctrl Pts',(-2.37542533402904,0.0615922612091321,
7.6473336463605));
#62005=CARTESIAN_POINT('Ctrl Pts',(-2.37508229419387,0.00108330972966112,
7.65141010809496));
#62006=CARTESIAN_POINT('Ctrl Pts',(-2.37092048416906,0.00212358946080219,
6.84858989190502));
#62007=CARTESIAN_POINT('Ctrl Pts',(-2.36587563233299,-0.574449067114922,
6.88725741186907));
#62008=CARTESIAN_POINT('Ctrl Pts',(-1.86459843703705,-1.94698367018192,
6.97877874663604));
#62009=CARTESIAN_POINT('Ctrl Pts',(0.430755120614024,-2.76874966894979,
7.12315389620592));
#62010=CARTESIAN_POINT('Ctrl Pts',(2.55831581876159,-1.14304193917764,7.28171534061469));
#62011=CARTESIAN_POINT('Ctrl Pts',(2.34980895897243,1.52640838558285,7.44027678502343));
#62012=CARTESIAN_POINT('Ctrl Pts',(-0.00437219018642784,2.80205381589964,
7.59883822943218));
#62013=CARTESIAN_POINT('Ctrl Pts',(-2.02170346853928,1.70077735243487,7.73494259839271));
#62014=CARTESIAN_POINT('Ctrl Pts',(-2.36661850469818,0.453602969412513,
7.81819315255032));
#62015=CARTESIAN_POINT('Ctrl Pts',(-2.36824036561998,-0.000937958850331759,
7.84858989190501));
#62016=CARTESIAN_POINT('Origin',(0.,0.,-1.84858989190508));
#62017=CARTESIAN_POINT('',(-2.36782500652722,-0.000132179022545951,5.65141010809495));
#62018=CARTESIAN_POINT('',(-2.37546058182015,-0.000550553819199384,5.84858989190501));
#62019=CARTESIAN_POINT('',(-2.37175,1.07555357745099E-12,-1.84858989190508));
#62020=CARTESIAN_POINT('Ctrl Pts',(-2.36782500652722,-0.000132179022545899,
5.65141010809495));
#62021=CARTESIAN_POINT('Ctrl Pts',(-2.36801741756233,-0.388970489593967,
5.67740191945286));
#62022=CARTESIAN_POINT('Ctrl Pts',(-2.09318863810404,-1.57118029724025,
5.75644359694196));
#62023=CARTESIAN_POINT('Ctrl Pts',(-0.226710508403585,-2.79638414202316,
5.88853514056225));
#62024=CARTESIAN_POINT('Ctrl Pts',(2.23052676138529,-1.70173802070743,6.04768473895582));
#62025=CARTESIAN_POINT('Ctrl Pts',(2.63715407267815,0.957382014315266,6.2068343373494));
#62026=CARTESIAN_POINT('Ctrl Pts',(0.619343131473575,2.7363435474871,6.36598393574298));
#62027=CARTESIAN_POINT('Ctrl Pts',(-1.78972184470636,2.05039854636853,6.51417585932482));
#62028=CARTESIAN_POINT('Ctrl Pts',(-2.366561939603,0.624498882346401,6.60931791677548));
#62029=CARTESIAN_POINT('Ctrl Pts',(-2.37238791048953,-0.00214487927112778,
6.65141010809496));
#62030=CARTESIAN_POINT('Ctrl Pts',(-2.37546058182015,-0.000550553819199696,
5.84858989190501));
#62031=CARTESIAN_POINT('Ctrl Pts',(-2.37555500637229,-0.0305832574876921,
5.85061404158198));
#62032=CARTESIAN_POINT('Ctrl Pts',(-2.36144599049303,-0.84472755400906,
5.90549200606186));
#62033=CARTESIAN_POINT('Ctrl Pts',(-1.43190741113937,-2.40856095400742,
6.01322378534467));
#62034=CARTESIAN_POINT('Ctrl Pts',(1.24371659317073,-2.5109149207244,6.17178522975341));
#62035=CARTESIAN_POINT('Ctrl Pts',(2.78366924554423,-0.320484375057478,
6.33034667416217));
#62036=CARTESIAN_POINT('Ctrl Pts',(1.7817780141982,2.16258914529891,6.48890811857092));
#62037=CARTESIAN_POINT('Ctrl Pts',(-0.847103045334166,2.67094386572056,
6.64746956297967));
#62038=CARTESIAN_POINT('Ctrl Pts',(-2.25001273100393,1.21118166807022,6.76736348742437));
#62039=CARTESIAN_POINT('Ctrl Pts',(-2.37277133355458,0.213655896415416,
6.83440359706615));
#62040=CARTESIAN_POINT('Ctrl Pts',(-2.37092048416906,0.00212358946080219,
6.84858989190502));
#62041=CARTESIAN_POINT('Origin',(0.,0.,-1.84858989190508));
#62042=CARTESIAN_POINT('',(-2.37190116809107,0.00218740778883247,4.65141010809495));
#62043=CARTESIAN_POINT('',(-2.36934253286443,-0.00173065431709335,4.84858989190501));
#62044=CARTESIAN_POINT('',(-2.37175,1.07555357745099E-12,-1.84858989190508));
#62045=CARTESIAN_POINT('Ctrl Pts',(-2.37190116809107,0.00218740778883234,
4.65141010809495));
#62046=CARTESIAN_POINT('Ctrl Pts',(-2.36622595650251,-0.608904074897115,
4.69243605599904));
#62047=CARTESIAN_POINT('Ctrl Pts',(-1.81333638750516,-2.01929938386188,
4.78651187003434));
#62048=CARTESIAN_POINT('Ctrl Pts',(0.564226129275921,-2.74823776254792,
4.9336375502008));
#62049=CARTESIAN_POINT('Ctrl Pts',(2.61738109284993,-1.01018718025988,5.09278714859438));
#62050=CARTESIAN_POINT('Ctrl Pts',(2.26427587290829,1.65656774558932,5.25193674698795));
#62051=CARTESIAN_POINT('Ctrl Pts',(-0.170466175671311,2.80037554755443,
5.41108634538153));
#62052=CARTESIAN_POINT('Ctrl Pts',(-2.07645202982422,1.60334443212033,5.54424413241719));
#62053=CARTESIAN_POINT('Ctrl Pts',(-2.36762470235237,0.404657166379961,
5.62435205332167));
#62054=CARTESIAN_POINT('Ctrl Pts',(-2.36782500652722,-0.000132179022545899,
5.65141010809495));
#62055=CARTESIAN_POINT('Ctrl Pts',(-2.36934253286443,-0.00173065431709328,
4.84858989190501));
#62056=CARTESIAN_POINT('Ctrl Pts',(-2.37118989843079,-0.274085561974275,
4.86682448609781));
#62057=CARTESIAN_POINT('Ctrl Pts',(-2.20212096045125,-1.33365068797172,
4.93791289509353));
#62058=CARTESIAN_POINT('Ctrl Pts',(-0.641019536282537,-2.72774974243608,
5.06185511889216));
#62059=CARTESIAN_POINT('Ctrl Pts',(1.94145701387202,-2.02046266150336,5.2204165633009));
#62060=CARTESIAN_POINT('Ctrl Pts',(2.75113651059875,0.531763672408809,5.37897800770967));
#62061=CARTESIAN_POINT('Ctrl Pts',(1.04867864620236,2.59842217513736,5.5375394521184));
#62062=CARTESIAN_POINT('Ctrl Pts',(-1.57739889422249,2.29629762498076,5.69407674685021));
#62063=CARTESIAN_POINT('Ctrl Pts',(-2.37308942892567,0.753619104515225,
5.79776022677906));
#62064=CARTESIAN_POINT('Ctrl Pts',(-2.37546058182015,-0.000550553819199696,
5.84858989190501));
#62065=CARTESIAN_POINT('Origin',(0.,0.,-1.84858989190508));
#62066=CARTESIAN_POINT('',(-2.37534261640908,-0.000818844704635749,3.65141010809495));
#62067=CARTESIAN_POINT('',(-2.36928439194487,0.0017046354039639,3.84858989190501));
#62068=CARTESIAN_POINT('',(-2.37175,1.07555357745099E-12,-1.84858989190508));
#62069=CARTESIAN_POINT('Ctrl Pts',(-2.37534261640908,-0.000818844704635778,
3.65141010809495));
#62070=CARTESIAN_POINT('Ctrl Pts',(-2.37554183260228,-0.045488019799339,
3.65442032641404));
#62071=CARTESIAN_POINT('Ctrl Pts',(-2.35411815018044,-0.877178853768313,
3.71048041086432));
#62072=CARTESIAN_POINT('Ctrl Pts',(-1.37960980571773,-2.44291602421381,
3.81959036144579));
#62073=CARTESIAN_POINT('Ctrl Pts',(1.31015328351832,-2.48085878298404,3.97873995983935));
#62074=CARTESIAN_POINT('Ctrl Pts',(2.79544153036393,-0.238051622317477,
4.13788955823294));
#62075=CARTESIAN_POINT('Ctrl Pts',(1.71077171156123,2.22360564722096,4.2970391566265));
#62076=CARTESIAN_POINT('Ctrl Pts',(-0.946677043995799,2.64101580821315,
4.45618875502009));
#62077=CARTESIAN_POINT('Ctrl Pts',(-2.27311787854369,1.14872896002257,4.57431240550956));
#62078=CARTESIAN_POINT('Ctrl Pts',(-2.37356446372587,0.181286597264478,
4.63938618986785));
#62079=CARTESIAN_POINT('Ctrl Pts',(-2.37190116809107,0.00218740778883234,
4.65141010809495));
#62080=CARTESIAN_POINT('Ctrl Pts',(-2.36928439194487,0.00170463540396366,
3.84858989190501));
#62081=CARTESIAN_POINT('Ctrl Pts',(-2.36585269261901,-0.512803915466465,
3.88303493061364));
#62082=CARTESIAN_POINT('Ctrl Pts',(-1.94848825283823,-1.82186493092716,
3.97033378412518));
#62083=CARTESIAN_POINT('Ctrl Pts',(0.20925401019493,-2.79423289347191,4.11048645243965));
#62084=CARTESIAN_POINT('Ctrl Pts',(2.45933594484265,-1.34282962940415,4.2690478968484));
#62085=CARTESIAN_POINT('Ctrl Pts',(2.46373152879142,1.33474778785059,4.42760934125715));
#62086=CARTESIAN_POINT('Ctrl Pts',(0.218427035218096,2.79353080054729,4.58617078566591));
#62087=CARTESIAN_POINT('Ctrl Pts',(-1.94518171864127,1.82705282789237,4.72649763588185));
#62088=CARTESIAN_POINT('Ctrl Pts',(-2.36583522387729,0.515347737049405,
4.81397067129489));
#62089=CARTESIAN_POINT('Ctrl Pts',(-2.36934253286443,-0.00173065431709328,
4.84858989190501));
#62090=CARTESIAN_POINT('Origin',(0.,0.,-1.84858989190508));
#62091=CARTESIAN_POINT('',(-2.36939151225074,-0.00180255051221435,2.65141010809495));
#62092=CARTESIAN_POINT('',(-2.37543340018105,0.000596509793510114,2.84858989190501));
#62093=CARTESIAN_POINT('',(-2.37175,1.07555357745099E-12,-1.84858989190508));
#62094=CARTESIAN_POINT('Ctrl Pts',(-2.36939151225074,-0.00180255051221455,
2.65141010809495));
#62095=CARTESIAN_POINT('Ctrl Pts',(-2.37128654501027,-0.271300123974492,
2.66945446296022));
#62096=CARTESIAN_POINT('Ctrl Pts',(-2.2041984741782,-1.33083306058644,2.74054868395668));
#62097=CARTESIAN_POINT('Ctrl Pts',(-0.641521429760122,-2.73122899507208,
2.86469277108434));
#62098=CARTESIAN_POINT('Ctrl Pts',(1.95156679945169,-2.01557660741595,3.02384236947791));
#62099=CARTESIAN_POINT('Ctrl Pts',(2.75050382812508,0.553073821547345,3.18299196787149));
#62100=CARTESIAN_POINT('Ctrl Pts',(1.02079575688963,2.61326192654012,3.34214156626506));
#62101=CARTESIAN_POINT('Ctrl Pts',(-1.59690279772098,2.27745090552783,3.49828094633955));
#62102=CARTESIAN_POINT('Ctrl Pts',(-2.37203099343379,0.741728556467104,
3.60137046028285));
#62103=CARTESIAN_POINT('Ctrl Pts',(-2.37534261640908,-0.000818844704635778,
3.65141010809495));
#62104=CARTESIAN_POINT('Ctrl Pts',(-2.37543340018105,0.000596509793510109,
2.84858989190501));
#62105=CARTESIAN_POINT('Ctrl Pts',(-2.37289189110074,-0.75101179482527,
2.89924537512947));
#62106=CARTESIAN_POINT('Ctrl Pts',(-1.58200873350162,-2.29145202362107,
3.00275467315685));
#62107=CARTESIAN_POINT('Ctrl Pts',(1.04014173421655,-2.60185124395797,3.15911778598714));
#62108=CARTESIAN_POINT('Ctrl Pts',(2.74937577244265,-0.540793460784857,
3.31767923039589));
#62109=CARTESIAN_POINT('Ctrl Pts',(1.94808022437453,2.01407749008101,3.47624067480464));
#62110=CARTESIAN_POINT('Ctrl Pts',(-0.632060208719933,2.72983966543523,
3.6348021192134));
#62111=CARTESIAN_POINT('Ctrl Pts',(-2.19993069937822,1.33892162353352,3.75891852491352));
#62112=CARTESIAN_POINT('Ctrl Pts',(-2.37111842630456,0.276678131346021,
3.83018111581072));
#62113=CARTESIAN_POINT('Ctrl Pts',(-2.36928439194487,0.00170463540396366,
3.84858989190501));
#62114=CARTESIAN_POINT('Origin',(0.,0.,-1.84858989190508));
#62115=CARTESIAN_POINT('',(-2.36877975033525,0.00148782749813889,1.65141010809495));
#62116=CARTESIAN_POINT('',(-2.37099583443225,-0.00213048971222318,1.84858989190501));
#62117=CARTESIAN_POINT('',(-2.37175,1.07555357745099E-12,-1.84858989190508));
#62118=CARTESIAN_POINT('Ctrl Pts',(-2.36877975033525,0.00148782749813899,
1.65141010809495));
#62119=CARTESIAN_POINT('Ctrl Pts',(-2.36596424764654,-0.492870032272385,
1.68448859950641));
#62120=CARTESIAN_POINT('Ctrl Pts',(-1.97328459846742,-1.78415699276091,
1.77061695704905));
#62121=CARTESIAN_POINT('Ctrl Pts',(0.147742963738231,-2.80166329463351,
1.90979518072289));
#62122=CARTESIAN_POINT('Ctrl Pts',(2.43729952527864,-1.38950924165797,2.06894477911646));
#62123=CARTESIAN_POINT('Ctrl Pts',(2.48615290161395,1.30008022007748,2.22809437751004));
#62124=CARTESIAN_POINT('Ctrl Pts',(0.249388740897356,2.79445248935483,2.38724397590361));
#62125=CARTESIAN_POINT('Ctrl Pts',(-1.93704908267542,1.8416239542747,2.52834921943192));
#62126=CARTESIAN_POINT('Ctrl Pts',(-2.36571520511157,0.521014719177456,
2.61640459682903));
#62127=CARTESIAN_POINT('Ctrl Pts',(-2.36939151225074,-0.00180255051221455,
2.65141010809495));
#62128=CARTESIAN_POINT('Ctrl Pts',(-2.37099583443225,-0.00213048971222356,
1.84858989190501));
#62129=CARTESIAN_POINT('Ctrl Pts',(-2.37283470856056,-0.211048770807267,
1.86260200484238));
#62130=CARTESIAN_POINT('Ctrl Pts',(-2.25194621232616,-1.20591570523556,
1.92946793258267));
#62131=CARTESIAN_POINT('Ctrl Pts',(-0.855867697802383,-2.66814781527329,
2.04918767512588));
#62132=CARTESIAN_POINT('Ctrl Pts',(1.77466802262196,-2.16842771739956,2.20774911953463));
#62133=CARTESIAN_POINT('Ctrl Pts',(2.78470651107863,0.311343289720562,2.36631056394338));
#62134=CARTESIAN_POINT('Ctrl Pts',(1.25195381897505,2.50681790160282,2.52487200835213));
#62135=CARTESIAN_POINT('Ctrl Pts',(-1.42399178516171,2.41324930660116,2.68343345276089));
#62136=CARTESIAN_POINT('Ctrl Pts',(-2.36017099633076,0.849952732330805,
2.79133941394518));
#62137=CARTESIAN_POINT('Ctrl Pts',(-2.37554369583539,0.0332145832082634,
2.84639156032655));
#62138=CARTESIAN_POINT('Ctrl Pts',(-2.37543340018105,0.000596509793510109,
2.84858989190501));
#62139=CARTESIAN_POINT('Origin',(0.,0.,-1.84858989190508));
#62140=CARTESIAN_POINT('',(-2.37479956011642,0.00144393851757992,0.651410108094952));
#62141=CARTESIAN_POINT('',(-2.36820388529326,0.000916507492466495,0.848589891905012));
#62142=CARTESIAN_POINT('',(-2.37175,1.07555357745099E-12,-1.84858989190508));
#62143=CARTESIAN_POINT('Ctrl Pts',(-2.37479956011642,0.00144393851757997,
0.651410108094952));
#62144=CARTESIAN_POINT('Ctrl Pts',(-2.37014002571856,-0.712866861030972,
0.699522736052592));
#62145=CARTESIAN_POINT('Ctrl Pts',(-1.64646945403367,-2.22353554076285,
0.800685230141422));
#62146=CARTESIAN_POINT('Ctrl Pts',(0.92524708272242,-2.64846350983462,0.954897590361446));
#62147=CARTESIAN_POINT('Ctrl Pts',(2.72859047663099,-0.652671033011881,
1.11404718875502));
#62148=CARTESIAN_POINT('Ctrl Pts',(2.02348342694992,1.94341489122264,1.27319678714859));
#62149=CARTESIAN_POINT('Ctrl Pts',(-0.541916200030843,2.75270370291815,
1.43234638554217));
#62150=CARTESIAN_POINT('Ctrl Pts',(-2.17944386261456,1.38916365493018,1.55841749252429));
#62151=CARTESIAN_POINT('Ctrl Pts',(-2.37047963013088,0.299959905330106,
1.63143873337521));
#62152=CARTESIAN_POINT('Ctrl Pts',(-2.36877975033525,0.00148782749813899,
1.65141010809495));
#62153=CARTESIAN_POINT('Ctrl Pts',(-2.36820388529326,0.000916507492466252,
0.848589891905012));
#62154=CARTESIAN_POINT('Ctrl Pts',(-2.36666168705901,-0.451042231517807,
0.878812449358213));
#62155=CARTESIAN_POINT('Ctrl Pts',(-2.02471011777409,-1.69557760792411,
0.961888821614331));
#62156=CARTESIAN_POINT('Ctrl Pts',(-0.0135649315166644,-2.80200471609095,
1.09781900867337));
#62157=CARTESIAN_POINT('Ctrl Pts',(2.34478101694196,-1.53412545281777,1.25638045308212));
#62158=CARTESIAN_POINT('Ctrl Pts',(2.56205685808127,1.13464159452892,1.41494189749087));
#62159=CARTESIAN_POINT('Ctrl Pts',(0.439842266833678,2.76731764321101,1.57350334189962));
#62160=CARTESIAN_POINT('Ctrl Pts',(-1.86096804286685,1.95211388693732,1.718052673371));
#62161=CARTESIAN_POINT('Ctrl Pts',(-2.36589845897007,0.576992846277577,
1.80974819003947));
#62162=CARTESIAN_POINT('Ctrl Pts',(-2.37099583443225,-0.00213048971222356,
1.84858989190501));
#62163=CARTESIAN_POINT('Origin',(0.,0.,39.5));
#62164=CARTESIAN_POINT('',(-2.86973666310952,0.00133538653572275,39.1339652973708));
#62165=CARTESIAN_POINT('Ctrl Pts',(-0.439445221993938,2.33068358199192,
39.62825));
#62166=CARTESIAN_POINT('Ctrl Pts',(-0.35949827194111,2.34930793730339,39.6247609417367));
#62167=CARTESIAN_POINT('Ctrl Pts',(-0.278745636135806,2.3634061787771,39.6212861115939));
#62168=CARTESIAN_POINT('Ctrl Pts',(-0.197512062256915,2.37316448853009,
39.6178207830088));
#62169=CARTESIAN_POINT('Ctrl Pts',(-0.114123930084006,2.38318161795837,
39.6142635435044));
#62170=CARTESIAN_POINT('Ctrl Pts',(-0.0302282552652829,2.38862557677138,
39.6107163162615));
#62171=CARTESIAN_POINT('Ctrl Pts',(0.0538390324598612,2.38964547677812,
39.6071739885661));
#62172=CARTESIAN_POINT('Ctrl Pts',(0.0937642650950609,2.39012984764502,
39.6054916664508));
#62173=CARTESIAN_POINT('Ctrl Pts',(0.133728353022446,2.38961562430752,39.6038104494234));
#62174=CARTESIAN_POINT('Ctrl Pts',(0.173695695523468,2.3881147884205,39.6021297898218));
#62175=CARTESIAN_POINT('Ctrl Pts',(0.19786577786694,2.38720716422776,39.6011134179937));
#62176=CARTESIAN_POINT('Ctrl Pts',(0.222037051875367,2.38593866964451,39.6000972500259));
#62177=CARTESIAN_POINT('Ctrl Pts',(0.246201620501372,2.38431151277149,39.5990811647941));
#62178=CARTESIAN_POINT('Ctrl Pts',(0.262023069244234,2.38324615218255,39.598415895711));
#62179=CARTESIAN_POINT('Ctrl Pts',(0.27784241249069,2.38202687571003,39.5977506295992));
#62180=CARTESIAN_POINT('Ctrl Pts',(0.293641126549649,2.38065591301966,39.5970860183969));
#62181=CARTESIAN_POINT('Ctrl Pts',(0.379384271840456,2.37321539268935,39.5934790251521));
#62182=CARTESIAN_POINT('Ctrl Pts',(0.46463251786987,2.36130457094966,39.5898865577667));
#62183=CARTESIAN_POINT('Ctrl Pts',(0.549033644812378,2.34508734810305,39.5863033810857));
#62184=CARTESIAN_POINT('Ctrl Pts',(0.634178650960569,2.32872719286576,39.5826886236578));
#62185=CARTESIAN_POINT('Ctrl Pts',(0.718462490380905,2.30798424275509,39.5790833214255));
#62186=CARTESIAN_POINT('Ctrl Pts',(0.801522760414795,2.28297369408067,39.5754820995882));
#62187=CARTESIAN_POINT('Ctrl Pts',(0.853315250286197,2.26737828861944,39.5732365465042));
#62188=CARTESIAN_POINT('Ctrl Pts',(0.904631926849359,2.25012252017408,39.5709925799533));
#62189=CARTESIAN_POINT('Ctrl Pts',(0.955382243535092,2.23122440392206,39.5687488968205));
#62190=CARTESIAN_POINT('Ctrl Pts',(0.967602035670815,2.226674066753,39.5682086570094));
#62191=CARTESIAN_POINT('Ctrl Pts',(0.979786008270006,2.22202953927781,39.5676685642798));
#62192=CARTESIAN_POINT('Ctrl Pts',(0.991925279191415,2.21729426385562,39.5671289419076));
#62193=CARTESIAN_POINT('Ctrl Pts',(1.07366759536826,2.18540829778312,39.5634952819579));
#62194=CARTESIAN_POINT('Ctrl Pts',(1.15348638596816,2.14937373494847,39.5598783986484));
#62195=CARTESIAN_POINT('Ctrl Pts',(1.23102268640763,2.10933916676248,39.5562729770003));
#62196=CARTESIAN_POINT('Ctrl Pts',(1.30816316025863,2.06950897699608,39.5526859612052));
#62197=CARTESIAN_POINT('Ctrl Pts',(1.38304533569878,2.02571923323226,39.5491102903455));
#62198=CARTESIAN_POINT('Ctrl Pts',(1.45530281679409,1.97806672561256,39.545540730427));
#62199=CARTESIAN_POINT('Ctrl Pts',(1.51549908373607,1.938368371537,39.5425670012233));
#62200=CARTESIAN_POINT('Ctrl Pts',(1.57387380072491,1.89598823770892,39.5395975131496));
#62201=CARTESIAN_POINT('Ctrl Pts',(1.63020107000193,1.85095785631656,39.5366292400351));
#62202=CARTESIAN_POINT('Ctrl Pts',(1.65836470464044,1.82844266562037,39.5351451034778));
#62203=CARTESIAN_POINT('Ctrl Pts',(1.68601623605506,1.80526457576384,39.5336612706603));
#62204=CARTESIAN_POINT('Ctrl Pts',(1.71312572787294,1.78142555846922,39.5321773633112));
#62205=CARTESIAN_POINT('Ctrl Pts',(1.72751481855975,1.76877235994964,39.531389739642));
#62206=CARTESIAN_POINT('Ctrl Pts',(1.74175118247484,1.75593294056428,39.5306020949754));
#62207=CARTESIAN_POINT('Ctrl Pts',(1.75583018857345,1.74290745007241,39.5298143727475));
#62208=CARTESIAN_POINT('Ctrl Pts',(1.76643953526031,1.73309198842499,39.5292207784164));
#62209=CARTESIAN_POINT('Ctrl Pts',(1.77695982507892,1.72317043557429,39.528627119114));
#62210=CARTESIAN_POINT('Ctrl Pts',(1.7873768489527,1.71315495102162,39.5280340756501));
#62211=CARTESIAN_POINT('Ctrl Pts',(1.78918047975628,1.71142084378803,39.5279313945511));
#62212=CARTESIAN_POINT('Ctrl Pts',(1.79098110660068,1.70968383682676,39.5278287268096));
#62213=CARTESIAN_POINT('Ctrl Pts',(1.79277872129701,1.70794393308359,39.5277260723057));
#62214=CARTESIAN_POINT('Ctrl Pts',(1.85277206005579,1.64987663151762,39.5243000954034));
#62215=CARTESIAN_POINT('Ctrl Pts',(1.90941274940707,1.58858667736653,39.520888862746));
#62216=CARTESIAN_POINT('Ctrl Pts',(1.96268106277255,1.52446609117959,39.5174879201237));
#62217=CARTESIAN_POINT('Ctrl Pts',(2.01751082142157,1.45846594882589,39.5139872862313));
#62218=CARTESIAN_POINT('Ctrl Pts',(2.06876803124024,1.38946620854916,39.5104975544758));
#62219=CARTESIAN_POINT('Ctrl Pts',(2.11639781840586,1.31785082822935,39.5070138673568));
#62220=CARTESIAN_POINT('Ctrl Pts',(2.16250504721347,1.24852474211716,39.5036415415783));
#62221=CARTESIAN_POINT('Ctrl Pts',(2.20521314151012,1.17674668031166,39.5002748801611));
#62222=CARTESIAN_POINT('Ctrl Pts',(2.24443824676613,1.10283631226475,39.4969094767047));
#62223=CARTESIAN_POINT('Ctrl Pts',(2.26159923031564,1.07050052624423,39.4954371126925));
#62224=CARTESIAN_POINT('Ctrl Pts',(2.27809309201077,1.03775630392964,39.4939649894619));
#62225=CARTESIAN_POINT('Ctrl Pts',(2.29391059165361,1.00462924829656,39.4924927380198));
#62226=CARTESIAN_POINT('Ctrl Pts',(2.30309923797525,0.985385195521925,39.4916374828845));
#62227=CARTESIAN_POINT('Ctrl Pts',(2.31205961051446,0.966011939145637,39.4907821844824));
#62228=CARTESIAN_POINT('Ctrl Pts',(2.32078967559046,0.946514421244772,39.4899267704768));
#62229=CARTESIAN_POINT('Ctrl Pts',(2.32610779088639,0.934637070127862,39.4894056758151));
#62230=CARTESIAN_POINT('Ctrl Pts',(2.33133644269386,0.922722526711712,39.4888849296127));
#62231=CARTESIAN_POINT('Ctrl Pts',(2.33647546709348,0.91077224977599,39.4883645221385));
#62232=CARTESIAN_POINT('Ctrl Pts',(2.37171749020212,0.828820520581163,39.4847957100827));
#62233=CARTESIAN_POINT('Ctrl Pts',(2.40274873420275,0.745189063562941,39.4812427358572));
#62234=CARTESIAN_POINT('Ctrl Pts',(2.42951278311371,0.660283828018607,39.4777005656353));
#62235=CARTESIAN_POINT('Ctrl Pts',(2.45657092467005,0.574445624319474,39.4741194728193));
#62236=CARTESIAN_POINT('Ctrl Pts',(2.47926798471156,0.487304592098544,39.4705494227476));
#62237=CARTESIAN_POINT('Ctrl Pts',(2.4975005543187,0.399252281737089,39.466985213823));
#62238=CARTESIAN_POINT('Ctrl Pts',(2.51456467077104,0.316842895112961,39.4636494209282));
#62239=CARTESIAN_POINT('Ctrl Pts',(2.52771800895694,0.233634393127452,39.4603187444982));
#62240=CARTESIAN_POINT('Ctrl Pts',(2.53683582034357,0.149936742873024,39.456988920265));
#62241=CARTESIAN_POINT('Ctrl Pts',(2.54025499961356,0.118550124027614,39.4557402361776));
#62242=CARTESIAN_POINT('Ctrl Pts',(2.54310627315112,0.0870946671010823,
39.4544916719303));
#62243=CARTESIAN_POINT('Ctrl Pts',(2.54538154276705,0.0555866479532388,
39.4532430026497));
#62244=CARTESIAN_POINT('Ctrl Pts',(2.54664021905131,0.038156451466729,39.4525522403772));
#62245=CARTESIAN_POINT('Ctrl Pts',(2.54772260641032,0.0207101698921403,
39.4518614459615));
#62246=CARTESIAN_POINT('Ctrl Pts',(2.54862721938394,0.00325056775144827,
39.4511705813326));
#62247=CARTESIAN_POINT('Ctrl Pts',(2.54933098872424,-0.010332625325178,
39.4506331035844));
#62248=CARTESIAN_POINT('Ctrl Pts',(2.5499270655201,-0.0239235062956236,
39.4500955982875));
#62249=CARTESIAN_POINT('Ctrl Pts',(2.55041445808122,-0.0375069511551507,
39.4495585933208));
#62250=CARTESIAN_POINT('Ctrl Pts',(2.55382119554076,-0.132451425329508,
39.4458050790458));
#62251=CARTESIAN_POINT('Ctrl Pts',(2.55193263779309,-0.227203514255775,
39.4420691827466));
#62252=CARTESIAN_POINT('Ctrl Pts',(2.54463766231788,-0.321313299306112,
39.438345057077));
#62253=CARTESIAN_POINT('Ctrl Pts',(2.53776293446409,-0.410001624962419,
39.4348354701623));
#62254=CARTESIAN_POINT('Ctrl Pts',(2.52608656691972,-0.49812058693239,39.4313363367793));
#62255=CARTESIAN_POINT('Ctrl Pts',(2.50946448834332,-0.58530043370155,39.4278427630424));
#62256=CARTESIAN_POINT('Ctrl Pts',(2.50844839154163,-0.590629680766924,
39.4276292031627));
#62257=CARTESIAN_POINT('Ctrl Pts',(2.50741379735189,-0.595955417977466,
39.4274156640583));
#62258=CARTESIAN_POINT('Ctrl Pts',(2.50636066643785,-0.601277560448006,
39.4272021446113));
#62259=CARTESIAN_POINT('Ctrl Pts',(2.48918927936352,-0.688055535729271,
39.4237206922828));
#62260=CARTESIAN_POINT('Ctrl Pts',(2.46709408631404,-0.773878867566709,
39.4202444659784));
#62261=CARTESIAN_POINT('Ctrl Pts',(2.44034445210713,-0.858488994856188,
39.4167686198238));
#62262=CARTESIAN_POINT('Ctrl Pts',(2.42991429939784,-0.891479971164706,
39.4154133262932));
#62263=CARTESIAN_POINT('Ctrl Pts',(2.4187759588216,-0.924286351580536,39.414058090559));
#62264=CARTESIAN_POINT('Ctrl Pts',(2.40694340479929,-0.956892111550784,
39.4127026253509));
#62265=CARTESIAN_POINT('Ctrl Pts',(2.40229670837332,-0.969696538053649,
39.412170328154));
#62266=CARTESIAN_POINT('Ctrl Pts',(2.3975419341509,-0.982472644162397,39.4116378858603));
#62267=CARTESIAN_POINT('Ctrl Pts',(2.39268328644656,-0.995210568908195,
39.4111056518565));
#62268=CARTESIAN_POINT('Ctrl Pts',(2.35996373150917,-1.08099148036135,39.4075214323809));
#62269=CARTESIAN_POINT('Ctrl Pts',(2.322603485436,-1.16487755966247,39.403953527741));
#62270=CARTESIAN_POINT('Ctrl Pts',(2.28096449592765,-1.24660346235937,39.4003968590742));
#62271=CARTESIAN_POINT('Ctrl Pts',(2.23962237867528,-1.32774668633636,39.3968655482814));
#62272=CARTESIAN_POINT('Ctrl Pts',(2.19406163443676,-1.40676116498233,39.3933453138153));
#62273=CARTESIAN_POINT('Ctrl Pts',(2.14458115370232,-1.48337508521838,39.3898311846722));
#62274=CARTESIAN_POINT('Ctrl Pts',(2.09480630236801,-1.56044479903855,39.3862961491781));
#62275=CARTESIAN_POINT('Ctrl Pts',(2.0410643829371,-1.63508610297419,39.3827672918671));
#62276=CARTESIAN_POINT('Ctrl Pts',(1.98361248698335,-1.70699845916664,39.3792395524859));
#62277=CARTESIAN_POINT('Ctrl Pts',(1.9625644077349,-1.73334427329434,39.3779471297237));
#62278=CARTESIAN_POINT('Ctrl Pts',(1.9410179635923,-1.75932351900642,39.3766548570096));
#62279=CARTESIAN_POINT('Ctrl Pts',(1.91898445265148,-1.78492029350601,39.3753624855173));
#62280=CARTESIAN_POINT('Ctrl Pts',(1.90153877300993,-1.80518729176045,39.3743392124178));
#62281=CARTESIAN_POINT('Ctrl Pts',(1.88378772994283,-1.82521450164685,39.3733158773928));
#62282=CARTESIAN_POINT('Ctrl Pts',(1.86573664953228,-1.84499370935962,39.3722923569303));
#62283=CARTESIAN_POINT('Ctrl Pts',(1.8558141241398,-1.85586617163386,39.3717297364362));
#62284=CARTESIAN_POINT('Ctrl Pts',(1.84580621851311,-1.86665785434142,39.3711673608424));
#62285=CARTESIAN_POINT('Ctrl Pts',(1.83571834843321,-1.87736320670582,39.3706054437992));
#62286=CARTESIAN_POINT('Ctrl Pts',(1.76931159753876,-1.94783473955369,39.3669064384777));
#62287=CARTESIAN_POINT('Ctrl Pts',(1.69938786401867,-2.01462936439108,39.3632241072661));
#62288=CARTESIAN_POINT('Ctrl Pts',(1.62628672313842,-2.07743563507174,39.3595528525232));
#62289=CARTESIAN_POINT('Ctrl Pts',(1.5561772364533,-2.13767156771253,39.3560318433787));
#62290=CARTESIAN_POINT('Ctrl Pts',(1.48314412877673,-2.19423950466426,39.3525210226485));
#62291=CARTESIAN_POINT('Ctrl Pts',(1.4074450694785,-2.24683343290341,39.3490154521977));
#62292=CARTESIAN_POINT('Ctrl Pts',(1.33294635267627,-2.29859339137222,39.3455654687677));
#62293=CARTESIAN_POINT('Ctrl Pts',(1.25586490058951,-2.34650500808928,39.3421205704323));
#62294=CARTESIAN_POINT('Ctrl Pts',(1.1764163541384,-2.39023657739772,39.3386760502602));
#62295=CARTESIAN_POINT('Ctrl Pts',(1.14538583397869,-2.40731698230954,39.3373307109505));
#62296=CARTESIAN_POINT('Ctrl Pts',(1.11399394443605,-2.42375924272401,39.3359854293288));
#62297=CARTESIAN_POINT('Ctrl Pts',(1.08225259103083,-2.43954157402997,39.3346399249504));
#62298=CARTESIAN_POINT('Ctrl Pts',(1.06959621101295,-2.44583453766092,39.3341034256238));
#62299=CARTESIAN_POINT('Ctrl Pts',(1.05688426487745,-2.45202256581224,39.3335668908812));
#62300=CARTESIAN_POINT('Ctrl Pts',(1.04411748830536,-2.45810422120353,39.333030302944));
#62301=CARTESIAN_POINT('Ctrl Pts',(1.03064152771505,-2.46452370758792,39.3324639079849));
#62302=CARTESIAN_POINT('Ctrl Pts',(1.01711168853891,-2.47082119733044,39.331897757558));
#62303=CARTESIAN_POINT('Ctrl Pts',(1.00353479362675,-2.47699284501023,39.3313320696118));
#62304=CARTESIAN_POINT('Ctrl Pts',(0.966236089675615,-2.49394771290812,
39.329778000926));
#62305=CARTESIAN_POINT('Ctrl Pts',(0.928568841452935,-2.50995937495487,
39.3282268550137));
#62306=CARTESIAN_POINT('Ctrl Pts',(0.890556248926717,-2.52500318502184,
39.3266782169168));
#62307=CARTESIAN_POINT('Ctrl Pts',(0.807484702358906,-2.55787946326236,
39.3232938710138));
#62308=CARTESIAN_POINT('Ctrl Pts',(0.722765621710362,-2.58613669789995,
39.3199215020314));
#62309=CARTESIAN_POINT('Ctrl Pts',(0.636767319997115,-2.60991109724267,
39.3165567790635));
#62310=CARTESIAN_POINT('Ctrl Pts',(0.548522341733229,-2.63430659472855,
39.313104153846));
#62311=CARTESIAN_POINT('Ctrl Pts',(0.458929686032447,-2.65398210684791,
39.3096595793604));
#62312=CARTESIAN_POINT('Ctrl Pts',(0.368364879289187,-2.66903506839446,
39.3062183763255));
#62313=CARTESIAN_POINT('Ctrl Pts',(0.279383636592277,-2.68382482252575,
39.3028373441848));
#62314=CARTESIAN_POINT('Ctrl Pts',(0.189463090880913,-2.69415207285719,
39.2994595666231));
#62315=CARTESIAN_POINT('Ctrl Pts',(0.0989502335548338,-2.70006284797304,
39.2960806055499));
#62316=CARTESIAN_POINT('Ctrl Pts',(0.0775500298275637,-2.70146034878565,
39.2952817084927));
#62317=CARTESIAN_POINT('Ctrl Pts',(0.0561167062046726,-2.70261076645142,
39.2944827452768));
#62318=CARTESIAN_POINT('Ctrl Pts',(0.034654851265937,-2.70351433839264,
39.2936836572451));
#62319=CARTESIAN_POINT('Ctrl Pts',(0.0205332261909928,-2.70410887713211,
39.293157867577));
#62320=CARTESIAN_POINT('Ctrl Pts',(0.00640799301672085,-2.70459615835869,
39.2926323494521));
#62321=CARTESIAN_POINT('Ctrl Pts',(-0.00771643634287458,-2.70497657694664,
39.2921072000306));
#62322=CARTESIAN_POINT('Ctrl Pts',(-0.101719698230375,-2.70750840228552,
39.2886121378697));
#62323=CARTESIAN_POINT('Ctrl Pts',(-0.195729688081459,-2.70531291032107,
39.2851317795577));
#62324=CARTESIAN_POINT('Ctrl Pts',(-0.289352720535745,-2.698514854272,39.2816614070979));
#62325=CARTESIAN_POINT('Ctrl Pts',(-0.384132024040294,-2.69163284029931,
39.2781481745523));
#62326=CARTESIAN_POINT('Ctrl Pts',(-0.478515698146043,-2.68003388100711,
39.2746451760382));
#62327=CARTESIAN_POINT('Ctrl Pts',(-0.572104351374966,-2.66379465585476,
39.2711475165855));
#62328=CARTESIAN_POINT('Ctrl Pts',(-0.665368031458597,-2.64761181907741,
39.2676620022525));
#62329=CARTESIAN_POINT('Ctrl Pts',(-0.757843174723416,-2.62682077567727,
39.2641817899669));
#62330=CARTESIAN_POINT('Ctrl Pts',(-0.849129039468325,-2.60144632891952,
39.260702035573));
#62331=CARTESIAN_POINT('Ctrl Pts',(-0.887145207993385,-2.59087909327063,
39.2592528853696));
#62332=CARTESIAN_POINT('Ctrl Pts',(-0.924954967966171,-2.57951634574702,
39.2578038145793));
#62333=CARTESIAN_POINT('Ctrl Pts',(-0.962528474832794,-2.56735731546274,
39.2563544733274));
#62334=CARTESIAN_POINT('Ctrl Pts',(-0.978426001934737,-2.56221277268254,
39.2557412502415));
#62335=CARTESIAN_POINT('Ctrl Pts',(-0.994281227046726,-2.55692566296293,
39.2551279787381));
#62336=CARTESIAN_POINT('Ctrl Pts',(-1.01009184853142,-2.55149584746549,
39.2545146323168));
#62337=CARTESIAN_POINT('Ctrl Pts',(-1.02476184723976,-2.54645775415517,
39.2539455344343));
#62338=CARTESIAN_POINT('Ctrl Pts',(-1.03938588141779,-2.5412993580478,39.2533766649479));
#62339=CARTESIAN_POINT('Ctrl Pts',(-1.0539555861852,-2.5360234172864,39.2528082630797));
#62340=CARTESIAN_POINT('Ctrl Pts',(-1.14426394783588,-2.50332120581856,
39.2492851003049));
#62341=CARTESIAN_POINT('Ctrl Pts',(-1.23256614389459,-2.46607951371862,
39.2457767692827));
#62342=CARTESIAN_POINT('Ctrl Pts',(-1.31846265596223,-2.42437923432781,
39.242278438605));
#62343=CARTESIAN_POINT('Ctrl Pts',(-1.40300647890962,-2.38333564649392,
39.2388351992661));
#62344=CARTESIAN_POINT('Ctrl Pts',(-1.48522069962827,-2.33797256204044,
39.235401647783));
#62345=CARTESIAN_POINT('Ctrl Pts',(-1.56471216223979,-2.28831887886664,
39.2319731774254));
#62346=CARTESIAN_POINT('Ctrl Pts',(-1.60971511361838,-2.26020815834111,
39.2300321981083));
#62347=CARTESIAN_POINT('Ctrl Pts',(-1.653845098157,-2.23072140038903,39.2280928473407));
#62348=CARTESIAN_POINT('Ctrl Pts',(-1.69702733238731,-2.19985722057624,
39.2261542892225));
#62349=CARTESIAN_POINT('Ctrl Pts',(-1.73923615147419,-2.16968878197637,
39.2242594301361));
#62350=CARTESIAN_POINT('Ctrl Pts',(-1.78053947778623,-2.13820426438569,
39.2223653283661));
#62351=CARTESIAN_POINT('Ctrl Pts',(-1.82091439461048,-2.1054636261719,39.2204712032763));
#62352=CARTESIAN_POINT('Ctrl Pts',(-1.8498018668194,-2.08203833267543,39.2191159934036));
#62353=CARTESIAN_POINT('Ctrl Pts',(-1.87821401254732,-2.05796992890122,
39.2177607715932));
#62354=CARTESIAN_POINT('Ctrl Pts',(-1.90614139306952,-2.0332792648442,39.2164052519267));
#62355=CARTESIAN_POINT('Ctrl Pts',(-1.91596398111765,-2.02459509120772,
39.2159284900168));
#62356=CARTESIAN_POINT('Ctrl Pts',(-1.92572742236068,-2.01583317561599,
39.2154516504522));
#62357=CARTESIAN_POINT('Ctrl Pts',(-1.93542869344419,-2.00699675843135,
39.2149748479154));
#62358=CARTESIAN_POINT('Ctrl Pts',(-2.00468455990689,-1.94391494953425,
39.2115710287112));
#62359=CARTESIAN_POINT('Ctrl Pts',(-2.07052139305739,-1.87727179191439,
39.2081815447992));
#62360=CARTESIAN_POINT('Ctrl Pts',(-2.13285384149172,-1.80747796902504,
39.2048020558727));
#62361=CARTESIAN_POINT('Ctrl Pts',(-2.19655932242106,-1.73614675767774,
39.2013481250105));
#62362=CARTESIAN_POINT('Ctrl Pts',(-2.25660484514008,-1.66152391967282,
39.197904634314));
#62363=CARTESIAN_POINT('Ctrl Pts',(-2.31286801647662,-1.58400136238957,
39.1944669502929));
#62364=CARTESIAN_POINT('Ctrl Pts',(-2.36972346584143,-1.50566273117583,
39.1909930780395));
#62365=CARTESIAN_POINT('Ctrl Pts',(-2.42271702573988,-1.42436223090701,
39.1875251353579));
#62366=CARTESIAN_POINT('Ctrl Pts',(-2.47168306438995,-1.34046815016254,
39.1840583408827));
#62367=CARTESIAN_POINT('Ctrl Pts',(-2.49987230981729,-1.29217118971394,
39.1820625429173));
#62368=CARTESIAN_POINT('Ctrl Pts',(-2.52672599489418,-1.24301406482777,
39.180067125489));
#62369=CARTESIAN_POINT('Ctrl Pts',(-2.5522056678096,-1.19306325792156,39.1780711763405));
#62370=CARTESIAN_POINT('Ctrl Pts',(-2.56042357732412,-1.17695272099689,
39.1774274267306));
#62371=CARTESIAN_POINT('Ctrl Pts',(-2.56849851456185,-1.16075960512442,
39.176783621809));
#62372=CARTESIAN_POINT('Ctrl Pts',(-2.57642906806209,-1.14448609784345,
39.1761397309685));
#62373=CARTESIAN_POINT('Ctrl Pts',(-2.58202630645732,-1.13300055654104,
39.1756852846887));
#62374=CARTESIAN_POINT('Ctrl Pts',(-2.58755084539627,-1.12147647157377,
39.1752308557641));
#62375=CARTESIAN_POINT('Ctrl Pts',(-2.59299833616596,-1.10992317430216,
39.174776766792));
#62376=CARTESIAN_POINT('Ctrl Pts',(-2.63494544068166,-1.02095976185379,
39.1712801628739));
#62377=CARTESIAN_POINT('Ctrl Pts',(-2.67239555551184,-0.930128022481478,
39.1677982025641));
#62378=CARTESIAN_POINT('Ctrl Pts',(-2.70522126537772,-0.837829477144926,
39.1643261716253));
#62379=CARTESIAN_POINT('Ctrl Pts',(-2.73808241364883,-0.745431286948738,
39.1608503923063));
#62380=CARTESIAN_POINT('Ctrl Pts',(-2.76630961610753,-0.651562246339273,
39.1573845638093));
#62381=CARTESIAN_POINT('Ctrl Pts',(-2.78973122846687,-0.556596849324899,
39.153923956612));
#62382=CARTESIAN_POINT('Ctrl Pts',(-2.81265859587411,-0.463635420584731,
39.1505363754563));
#62383=CARTESIAN_POINT('Ctrl Pts',(-2.83098131139472,-0.369622551783345,
39.1471537975648));
#62384=CARTESIAN_POINT('Ctrl Pts',(-2.84449142099832,-0.274895379555267,
39.14377178655));
#62385=CARTESIAN_POINT('Ctrl Pts',(-2.85412274004531,-0.207364645540725,
39.1413607604326));
#62386=CARTESIAN_POINT('Ctrl Pts',(-2.86130723538155,-0.139470568128866,
39.1389500224146));
#62387=CARTESIAN_POINT('Ctrl Pts',(-2.86595331455768,-0.0713343506542745,
39.1365379651471));
#62388=CARTESIAN_POINT('Ctrl Pts',(-2.86760682598113,-0.0470850837618877,
39.1356795285827));
#62389=CARTESIAN_POINT('Ctrl Pts',(-2.86893661989062,-0.02283541425464,
39.1348219958471));
#62390=CARTESIAN_POINT('Ctrl Pts',(-2.86994055756815,0.00140893619034663,
39.1339652973708));
#62391=CARTESIAN_POINT('',(0.260859905888426,2.92566825966708,39.058));
#62392=CARTESIAN_POINT('Ctrl Pts',(0.260722923797069,2.92490787419814,39.058));
#62393=CARTESIAN_POINT('Ctrl Pts',(0.162848360265034,2.92110708545298,39.0703773556647));
#62394=CARTESIAN_POINT('Ctrl Pts',(0.0654427185948832,2.91266301593948,
39.0827988569344));
#62395=CARTESIAN_POINT('Ctrl Pts',(-0.0311162990840133,2.89958345814013,
39.0952840450831));
#62396=CARTESIAN_POINT('Ctrl Pts',(-0.129313155017022,2.88628204431298,
39.1079810075358));
#62397=CARTESIAN_POINT('Ctrl Pts',(-0.226635485341331,2.86818645239439,
39.1207438357102));
#62398=CARTESIAN_POINT('Ctrl Pts',(-0.32266288795503,2.84525380804573,39.133593082222));
#62399=CARTESIAN_POINT('Ctrl Pts',(-0.412969691932927,2.82368732013164,
39.1456768661673));
#62400=CARTESIAN_POINT('Ctrl Pts',(-0.502131726890962,2.79784231531796,
39.1578370788154));
#62401=CARTESIAN_POINT('Ctrl Pts',(-0.589768635260519,2.76764452465773,
39.1700908141378));
#62402=CARTESIAN_POINT('Ctrl Pts',(-0.617754478167129,2.75800120609176,
39.1740039041604));
#62403=CARTESIAN_POINT('Ctrl Pts',(-0.6455845199527,2.7479137292182,39.1779265313547));
#62404=CARTESIAN_POINT('Ctrl Pts',(-0.67324554731687,2.73737892024034,39.1818592523898));
#62405=CARTESIAN_POINT('Ctrl Pts',(-0.693406364060657,2.72970059541034,
39.1847256270565));
#62406=CARTESIAN_POINT('Ctrl Pts',(-0.713477387242329,2.7217846284664,39.1875973638378));
#62407=CARTESIAN_POINT('Ctrl Pts',(-0.733453348713622,2.71362967314459,
39.1904746782677));
#62408=CARTESIAN_POINT('Ctrl Pts',(-0.749161208632885,2.70721712093644,
39.1927372202773));
#62409=CARTESIAN_POINT('Ctrl Pts',(-0.764811862045415,2.70065600518691,
39.1950034483465));
#62410=CARTESIAN_POINT('Ctrl Pts',(-0.780383183738797,2.69395435536418,
39.1972706037194));
#62411=CARTESIAN_POINT('Ctrl Pts',(-0.863899019700987,2.65801046451841,
39.2094303535436));
#62412=CARTESIAN_POINT('Ctrl Pts',(-0.945263791906173,2.61797609039484,
39.2216352057428));
#62413=CARTESIAN_POINT('Ctrl Pts',(-1.02414462749053,2.57382342820898,39.2339041184484));
#62414=CARTESIAN_POINT('Ctrl Pts',(-1.06217855473277,2.55253436441183,39.2398198130493));
#62415=CARTESIAN_POINT('Ctrl Pts',(-1.09963454861993,2.53028724262747,39.245750400908));
#62416=CARTESIAN_POINT('Ctrl Pts',(-1.13647239878871,2.50707567377056,39.2516980071986));
#62417=CARTESIAN_POINT('Ctrl Pts',(-1.21477794615272,2.45773526448529,39.2643407255971));
#62418=CARTESIAN_POINT('Ctrl Pts',(-1.29029332358275,2.40403849832711,39.2770603421731));
#62419=CARTESIAN_POINT('Ctrl Pts',(-1.36280597910661,2.34631276383115,39.289877269102));
#62420=CARTESIAN_POINT('Ctrl Pts',(-1.43780473366327,2.28660790042783,39.3031336248369));
#62421=CARTESIAN_POINT('Ctrl Pts',(-1.50959208190557,2.22259204721685,39.3164940778875));
#62422=CARTESIAN_POINT('Ctrl Pts',(-1.57787834130925,2.15460693677166,39.3299812127298));
#62423=CARTESIAN_POINT('Ctrl Pts',(-1.59002758401102,2.14251127339636,39.3323807946659));
#62424=CARTESIAN_POINT('Ctrl Pts',(-1.60206585076167,2.13028993909883,39.3347843866167));
#62425=CARTESIAN_POINT('Ctrl Pts',(-1.61399130943753,2.11794483308677,39.3371921157736));
#62426=CARTESIAN_POINT('Ctrl Pts',(-1.62247302820951,2.10916464942671,39.3389045598937));
#62427=CARTESIAN_POINT('Ctrl Pts',(-1.63089629603585,2.10032323235738,39.3406188236418));
#62428=CARTESIAN_POINT('Ctrl Pts',(-1.63925448160622,2.09142789834082,39.3423336976597));
#62429=CARTESIAN_POINT('Ctrl Pts',(-1.70075807351381,2.02597170708621,39.3549525741946));
#62430=CARTESIAN_POINT('Ctrl Pts',(-1.75883748111895,1.95749928194615,39.3676238420838));
#62431=CARTESIAN_POINT('Ctrl Pts',(-1.81332493160888,1.88633203750824,39.380369171064));
#62432=CARTESIAN_POINT('Ctrl Pts',(-1.86759709574965,1.81544598325444,39.3930641417448));
#62433=CARTESIAN_POINT('Ctrl Pts',(-1.918305926586,1.74188536506989,39.4058325894245));
#62434=CARTESIAN_POINT('Ctrl Pts',(-1.96523749898236,1.66594995450098,39.4186959279941));
#62435=CARTESIAN_POINT('Ctrl Pts',(-2.01136571686395,1.59131437370118,39.4313390774547));
#62436=CARTESIAN_POINT('Ctrl Pts',(-2.05384502137649,1.51438370651053,39.4440738970063));
#62437=CARTESIAN_POINT('Ctrl Pts',(-2.09242267521999,1.43543935198141,39.4569207195948));
#62438=CARTESIAN_POINT('Ctrl Pts',(-2.11318763556892,1.39294645186315,39.4638357010694));
#62439=CARTESIAN_POINT('Ctrl Pts',(-2.13282130912474,1.34987015428585,39.4707831329688));
#62440=CARTESIAN_POINT('Ctrl Pts',(-2.15127797244486,1.30625529672902,39.4777661862196));
#62441=CARTESIAN_POINT('Ctrl Pts',(-2.15677341232959,1.29326904760979,39.4798453783621));
#62442=CARTESIAN_POINT('Ctrl Pts',(-2.16216519449366,1.28023327496112,39.4819280131221));
#62443=CARTESIAN_POINT('Ctrl Pts',(-2.16744975458983,1.26715483776717,39.4840132729464));
#62444=CARTESIAN_POINT('Ctrl Pts',(-2.19936788078035,1.18816260357277,39.4966079989029));
#62445=CARTESIAN_POINT('Ctrl Pts',(-2.22727542829756,1.10787312475877,39.5092572977189));
#62446=CARTESIAN_POINT('Ctrl Pts',(-2.25099555335962,1.02655503037711,39.5219833174302));
#62447=CARTESIAN_POINT('Ctrl Pts',(-2.27436406309063,0.946442354963575,
39.5345206929575));
#62448=CARTESIAN_POINT('Ctrl Pts',(-2.29366844569015,0.865330512105231,
39.5471325316936));
#62449=CARTESIAN_POINT('Ctrl Pts',(-2.30868993862032,0.783477908782109,
39.5598400112676));
#62450=CARTESIAN_POINT('Ctrl Pts',(-2.32326996787289,0.704030855390139,
39.5721740332437));
#62451=CARTESIAN_POINT('Ctrl Pts',(-2.33381505358564,0.623885304742978,
39.5845981571237));
#62452=CARTESIAN_POINT('Ctrl Pts',(-2.34007838345357,0.543289558251172,
39.5971317477171));
#62453=CARTESIAN_POINT('Ctrl Pts',(-2.345223193426,0.477086786078833,39.6074270607909));
#62454=CARTESIAN_POINT('Ctrl Pts',(-2.34747816613177,0.410580313554983,
39.6177962340149));
#62455=CARTESIAN_POINT('Ctrl Pts',(-2.34668236863851,0.343918483395665,
39.62825));
#62456=CARTESIAN_POINT('',(-2.14344942214843,2.01149700971877,39.058));
#62457=CARTESIAN_POINT('Origin',(0.,0.,39.058));
#62458=CARTESIAN_POINT('Ctrl Pts',(-2.86994055756815,0.00140893619034663,
39.1339652973708));
#62459=CARTESIAN_POINT('Ctrl Pts',(-2.87320577914358,0.0802616159190132,
39.1311789587253));
#62460=CARTESIAN_POINT('Ctrl Pts',(-2.87302560073353,0.159057577103706,
39.1284014445519));
#62461=CARTESIAN_POINT('Ctrl Pts',(-2.86931315923603,0.237604716866276,
39.125630361528));
#62462=CARTESIAN_POINT('Ctrl Pts',(-2.86480590834164,0.33296828453044,39.1222660077877));
#62463=CARTESIAN_POINT('Ctrl Pts',(-2.85509398930959,0.427965500006218,
39.1189111337089));
#62464=CARTESIAN_POINT('Ctrl Pts',(-2.8404520930183,0.522299278433487,39.1155614561975));
#62465=CARTESIAN_POINT('Ctrl Pts',(-2.82552036226947,0.618500381895329,
39.1121454722498));
#62466=CARTESIAN_POINT('Ctrl Pts',(-2.80546129783727,0.71401229537241,39.1087348926365));
#62467=CARTESIAN_POINT('Ctrl Pts',(-2.78051144060668,0.808516432443364,
39.1053251748457));
#62468=CARTESIAN_POINT('Ctrl Pts',(-2.76597047184241,0.863594170666203,
39.1033379650819));
#62469=CARTESIAN_POINT('Ctrl Pts',(-2.74976727234159,0.918329478376449,
39.1013510480489));
#62470=CARTESIAN_POINT('Ctrl Pts',(-2.73194088190628,0.972657121596614,
39.0993635245144));
#62471=CARTESIAN_POINT('Ctrl Pts',(-2.72568217604983,0.991731130999871,
39.098665720591));
#62472=CARTESIAN_POINT('Ctrl Pts',(-2.71922333763423,1.01075486961467,39.0979678419068));
#62473=CARTESIAN_POINT('Ctrl Pts',(-2.71256590131154,1.02972544345301,39.0972698495451));
#62474=CARTESIAN_POINT('Ctrl Pts',(-2.70786090595029,1.04313247546704,39.0967765589351));
#62475=CARTESIAN_POINT('Ctrl Pts',(-2.70306010139198,1.05650330826665,39.0962835663674));
#62476=CARTESIAN_POINT('Ctrl Pts',(-2.69816441448398,1.06983707108187,39.0957908567459));
#62477=CARTESIAN_POINT('Ctrl Pts',(-2.66407853481969,1.16267246748952,39.0923604002682));
#62478=CARTESIAN_POINT('Ctrl Pts',(-2.6253979559053,1.25371035778419,39.0889436904178));
#62479=CARTESIAN_POINT('Ctrl Pts',(-2.58240965705905,1.34263826608692,39.0855362733872));
#62480=CARTESIAN_POINT('Ctrl Pts',(-2.53890424253589,1.4326359077062,39.0820878677897));
#62481=CARTESIAN_POINT('Ctrl Pts',(-2.49098647195779,1.5204733357728,39.0786489799275));
#62482=CARTESIAN_POINT('Ctrl Pts',(-2.43890099522592,1.60581543086489,39.0752149933246));
#62483=CARTESIAN_POINT('Ctrl Pts',(-2.38699542910386,1.6908627422796,39.0717928681975));
#62484=CARTESIAN_POINT('Ctrl Pts',(-2.33095040623944,1.77343274680066,39.0683756105289));
#62485=CARTESIAN_POINT('Ctrl Pts',(-2.27096264380004,1.85317031961247,39.0649586515155));
#62486=CARTESIAN_POINT('Ctrl Pts',(-2.23024681086646,1.90729105292729,39.0626394396184));
#62487=CARTESIAN_POINT('Ctrl Pts',(-2.18771369495367,1.96010644704108,39.0603203653064));
#62488=CARTESIAN_POINT('Ctrl Pts',(-2.14341454569435,2.01149633185867,39.058));
#62489=CARTESIAN_POINT('',(-2.,-2.44929359829471E-16,40.));
#62490=CARTESIAN_POINT('',(-2.5,-3.06161699786838E-16,39.5));
#62491=CARTESIAN_POINT('Origin',(0.,0.,40.));
#62492=CARTESIAN_POINT('Ctrl Pts',(1.70810875200399,-2.39535560853235,-0.329233991005384));
#62493=CARTESIAN_POINT('Ctrl Pts',(2.5065338081197,-1.82600514494664,-0.276184124874192));
#62494=CARTESIAN_POINT('Ctrl Pts',(3.47517087235694,0.164164634797699,-0.170084392611809));
#62495=CARTESIAN_POINT('Ctrl Pts',(1.73627755672406,3.01873330702807,-0.0109347942182355));
#62496=CARTESIAN_POINT('Ctrl Pts',(-1.60036897517342,3.08916744448106,0.148214804175339));
#62497=CARTESIAN_POINT('Ctrl Pts',(-3.46493207619462,0.324065259852807,
0.307364402568913));
#62498=CARTESIAN_POINT('Ctrl Pts',(-2.14446912907937,-2.7412743082718,0.466514000962488));
#62499=CARTESIAN_POINT('Ctrl Pts',(1.14770819747867,-3.28524492291903,0.625663599356061));
#62500=CARTESIAN_POINT('Ctrl Pts',(3.38463715916455,-0.809595521922738,
0.784813197749637));
#62501=CARTESIAN_POINT('Ctrl Pts',(2.5099982047375,2.41067844839361,0.943962796143209));
#62502=CARTESIAN_POINT('Ctrl Pts',(-0.672211430585623,3.41454803161592,
1.10311239453679));
#62503=CARTESIAN_POINT('Ctrl Pts',(-3.23641431966485,1.27938206751248,1.26226199293036));
#62504=CARTESIAN_POINT('Ctrl Pts',(-2.82526444201928,-2.03201736216267,
1.42141159132393));
#62505=CARTESIAN_POINT('Ctrl Pts',(0.183265436626373,-3.47527918744039,
1.58056118971751));
#62506=CARTESIAN_POINT('Ctrl Pts',(3.02330987809428,-1.72359489362586,1.73971078811108));
#62507=CARTESIAN_POINT('Ctrl Pts',(3.0839092807201,1.61266406976645,1.89886038650466));
#62508=CARTESIAN_POINT('Ctrl Pts',(0.309350342877327,3.46633465739727,2.05800998489823));
#62509=CARTESIAN_POINT('Ctrl Pts',(-2.74960604526907,2.1332709394318,2.2171595832918));
#62510=CARTESIAN_POINT('Ctrl Pts',(-3.2807428921365,-1.16099267046222,2.37630918168538));
#62511=CARTESIAN_POINT('Ctrl Pts',(-0.795765171857732,-3.3879100678833,
2.53545878007895));
#62512=CARTESIAN_POINT('Ctrl Pts',(2.42079035479599,-2.50019031475376,2.69460837847253));
#62513=CARTESIAN_POINT('Ctrl Pts',(3.41181923151422,0.686051726781072,2.8537579768661));
#62514=CARTESIAN_POINT('Ctrl Pts',(1.26623004817903,3.24157967234375,3.01290757525968));
#62515=CARTESIAN_POINT('Ctrl Pts',(-2.04345363315851,2.81699745515115,3.17205717365325));
#62516=CARTESIAN_POINT('Ctrl Pts',(-3.47451095858186,-0.197360047609994,
3.33120677204682));
#62517=CARTESIAN_POINT('Ctrl Pts',(-1.7113152939479,-3.03027677589855,3.4903563704404));
#62518=CARTESIAN_POINT('Ctrl Pts',(1.62515904294783,-3.07734227449719,3.64950596883397));
#62519=CARTESIAN_POINT('Ctrl Pts',(3.46756149776779,-0.295287392371581,
3.80865556722755));
#62520=CARTESIAN_POINT('Ctrl Pts',(2.12209987368507,2.75823666664889,3.96780516562112));
#62521=CARTESIAN_POINT('Ctrl Pts',(-1.1742906560288,3.27600653853182,4.1269547640147));
#62522=CARTESIAN_POINT('Ctrl Pts',(-3.39111013780228,0.782016251666639,
4.28610436240827));
#62523=CARTESIAN_POINT('Ctrl Pts',(-2.49035024800795,-2.4309119742704,4.44525396080185));
#62524=CARTESIAN_POINT('Ctrl Pts',(0.69988543157182,-3.40900832609501,4.60440355919542));
#62525=CARTESIAN_POINT('Ctrl Pts',(3.24668922743323,-1.25307080608154,4.763553157589));
#62526=CARTESIAN_POINT('Ctrl Pts',(2.80868540870487,2.0548634162641,4.92270275598256));
#62527=CARTESIAN_POINT('Ctrl Pts',(-0.211452087625477,3.47368182182148,
5.08185235437615));
#62528=CARTESIAN_POINT('Ctrl Pts',(-3.03719346007492,1.69900949693403,5.24100195276971));
#62529=CARTESIAN_POINT('Ctrl Pts',(-3.07072482055295,-1.63762830368612,
5.4001515511633));
#62530=CARTESIAN_POINT('Ctrl Pts',(-0.281219485916566,-3.46873074558119,
5.55930114955686));
#62531=CARTESIAN_POINT('Ctrl Pts',(2.76682185390363,-2.11089417388877,5.71845074795045));
#62532=CARTESIAN_POINT('Ctrl Pts',(3.27121630939976,1.18756946816326,5.87760034634401));
#62533=CARTESIAN_POINT('Ctrl Pts',(0.768254450424601,3.394254334018,6.03674994473758));
#62534=CARTESIAN_POINT('Ctrl Pts',(-2.44099358900468,2.48046924654082,6.19589954313117));
#62535=CARTESIAN_POINT('Ctrl Pts',(-3.40614133387891,-0.713707641992457,
6.35504914152473));
#62536=CARTESIAN_POINT('Ctrl Pts',(-1.23989094436864,-3.25174535144891,
6.51419873991831));
#62537=CARTESIAN_POINT('Ctrl Pts',(2.06623938829558,-2.80032715496828,6.67334833831189));
#62538=CARTESIAN_POINT('Ctrl Pts',(3.47279553085058,0.225540651548871,6.83249793670546));
#62539=CARTESIAN_POINT('Ctrl Pts',(1.68667574471175,3.04406016970723,6.99164753509903));
#62540=CARTESIAN_POINT('Ctrl Pts',(-1.65007061929938,3.06405684280202,7.15079713349261));
#62541=CARTESIAN_POINT('Ctrl Pts',(-3.46984292017243,0.267146951931126,
7.30994673188618));
#62542=CARTESIAN_POINT('Ctrl Pts',(-2.09965374212423,-2.77536151659212,
7.46909633027976));
#62543=CARTESIAN_POINT('Ctrl Pts',(1.20082874041637,-3.26637225692158,7.62824592867333));
#62544=CARTESIAN_POINT('Ctrl Pts',(3.39734268235243,-0.754480008524603,
7.78739552706691));
#62545=CARTESIAN_POINT('Ctrl Pts',(2.47054743228023,2.45103504043708,7.94654512546048));
#62546=CARTESIAN_POINT('Ctrl Pts',(-0.727518109309972,3.40321829820288,
8.10569472385404));
#62547=CARTESIAN_POINT('Ctrl Pts',(-3.2567479723672,1.22669068190765,8.26484432224764));
#62548=CARTESIAN_POINT('Ctrl Pts',(-2.79192282561145,-2.07758136313038,
8.42399392064119));
#62549=CARTESIAN_POINT('Ctrl Pts',(0.239625504503551,-3.47185209969956,
8.58314351903478));
#62550=CARTESIAN_POINT('Ctrl Pts',(3.05087679342124,-1.67431424050583,8.74229311742835));
#62551=CARTESIAN_POINT('Ctrl Pts',(3.05733845011404,1.66248578521777,8.90144271582193));
#62552=CARTESIAN_POINT('Ctrl Pts',(0.253070022401753,3.47089800316265,9.06059231421549));
#62553=CARTESIAN_POINT('Ctrl Pts',(-2.78385551443731,2.08837876337934,9.21974191260909));
#62554=CARTESIAN_POINT('Ctrl Pts',(-3.26147446067824,-1.21406825464651,
9.37889151100263));
#62555=CARTESIAN_POINT('Ctrl Pts',(-0.740693152670185,-3.40037513197947,
9.53804110939624));
#62556=CARTESIAN_POINT('Ctrl Pts',(2.46103616338236,-2.46058496848232,9.69719070778978));
#62557=CARTESIAN_POINT('Ctrl Pts',(3.40023926714405,0.741316606294871,9.85634030618338));
#62558=CARTESIAN_POINT('Ctrl Pts',(1.21347023590029,3.26169700787503,10.0154899045769));
#62559=CARTESIAN_POINT('Ctrl Pts',(-2.08888915415634,2.78347255891718,10.1746395029705));
#62560=CARTESIAN_POINT('Ctrl Pts',(-3.47085154388881,-0.253706414742628,
10.3337891013641));
#62561=CARTESIAN_POINT('Ctrl Pts',(-1.66192518770954,-3.05764321905834,
10.4929386997577));
#62562=CARTESIAN_POINT('Ctrl Pts',(1.67487359716716,-3.05056975303127,10.6520882981512));
#62563=CARTESIAN_POINT('Ctrl Pts',(3.47189597719149,-0.238988928945294,
10.8112378965448));
#62564=CARTESIAN_POINT('Ctrl Pts',(2.07706942316891,2.79230370768181,10.9703874949384));
#62565=CARTESIAN_POINT('Ctrl Pts',(-1.22728779301538,3.25652300125645,11.129537093332));
#62566=CARTESIAN_POINT('Ctrl Pts',(-3.40335163300419,0.7268941097055,11.2886866917255));
#62567=CARTESIAN_POINT('Ctrl Pts',(-2.45058201906605,-2.47099679328547,
11.4478362901191));
#62568=CARTESIAN_POINT('Ctrl Pts',(0.75510290591141,-3.39720428971839,11.6069858885127));
#62569=CARTESIAN_POINT('Ctrl Pts',(3.2665923765427,-1.20022982387123,11.7661354869063));
#62570=CARTESIAN_POINT('Ctrl Pts',(2.77497649392323,2.10016257531898,11.9252850852998));
#62571=CARTESIAN_POINT('Ctrl Pts',(-0.267783150583668,3.46979387988111,
12.0844346836934));
#62572=CARTESIAN_POINT('Ctrl Pts',(-3.06435933528609,1.6495087901681,12.243584282087));
#62573=CARTESIAN_POINT('Ctrl Pts',(-3.04375086292351,-1.6872338513227,12.4027338804806));
#62574=CARTESIAN_POINT('Ctrl Pts',(-0.224903903247275,-3.47283682583864,
12.5618834788741));
#62575=CARTESIAN_POINT('Ctrl Pts',(2.80070595732196,-2.06572590757297,12.7210330772677));
#62576=CARTESIAN_POINT('Ctrl Pts',(3.25151796012581,1.24048713801321,12.8801826756613));
#62577=CARTESIAN_POINT('Ctrl Pts',(0.71308310667526,3.40627213645228,13.0393322740549));
#62578=CARTESIAN_POINT('Ctrl Pts',(-2.48091676625765,2.4405387486165,13.1984818724484));
#62579=CARTESIAN_POINT('Ctrl Pts',(-3.39411341586236,-0.768876781324591,
13.357631470842));
#62580=CARTESIAN_POINT('Ctrl Pts',(-1.18696966367366,-3.27143399782347,
13.5167810692356));
#62581=CARTESIAN_POINT('Ctrl Pts',(2.11140144112928,-2.76643477042095,13.6759306676291));
#62582=CARTESIAN_POINT('Ctrl Pts',(3.46867912507889,0.281855480412862,13.8350802660227));
#62583=CARTESIAN_POINT('Ctrl Pts',(1.63706525217668,3.07102503159981,13.9942298644163));
#62584=CARTESIAN_POINT('Ctrl Pts',(-1.69956634431306,3.03688189198646,14.1533794628099));
#62585=CARTESIAN_POINT('Ctrl Pts',(-3.4737205336237,0.210815177057792,14.3125290612034));
#62586=CARTESIAN_POINT('Ctrl Pts',(-2.05434840323376,-2.80906212511005,
14.471678659597));
#62587=CARTESIAN_POINT('Ctrl Pts',(1.25366607246256,-3.24645941963753,14.6308282579906));
#62588=CARTESIAN_POINT('Ctrl Pts',(3.40913659427078,-0.699260370820959,
14.7899778563842));
#62589=CARTESIAN_POINT('Ctrl Pts',(2.4304553223822,2.49079591907906,14.9491274547778));
#62590=CARTESIAN_POINT('Ctrl Pts',(-0.782638005903754,3.39096669643213,
15.1082770531713));
#62591=CARTESIAN_POINT('Ctrl Pts',(-3.27622179205498,1.17368997348573,15.2674266515649));
#62592=CARTESIAN_POINT('Ctrl Pts',(-2.75784752895294,-2.12260556666684,
15.4265762499585));
#62593=CARTESIAN_POINT('Ctrl Pts',(0.295923172689008,-3.46750729782397,
15.585725848352));
#62594=CARTESIAN_POINT('Ctrl Pts',(3.07764019832444,-1.6245947784769,15.7448754467456));
#62595=CARTESIAN_POINT('Ctrl Pts',(3.02996295323977,1.71187087322363,15.9040250451392));
#62596=CARTESIAN_POINT('Ctrl Pts',(0.196722982187926,3.47454708600645,16.0631746435328));
#62597=CARTESIAN_POINT('Ctrl Pts',(-2.81737207355656,2.04293709735284,16.2223242419263));
#62598=CARTESIAN_POINT('Ctrl Pts',(-3.2413474630231,-1.26682437952171,16.3814738403199));
#62599=CARTESIAN_POINT('Ctrl Pts',(-0.68542612957718,-3.41194495932888,
16.5406234387135));
#62600=CARTESIAN_POINT('Ctrl Pts',(2.50063408920154,-2.42033190627238,16.6997730371071));
#62601=CARTESIAN_POINT('Ctrl Pts',(3.38776418320275,0.796386353226517,16.8589226355006));
#62602=CARTESIAN_POINT('Ctrl Pts',(1.16039097180682,3.28095568046051,17.0180722338942));
#62603=CARTESIAN_POINT('Ctrl Pts',(-2.13377476758282,2.74921491081068,17.1772218322878));
#62604=CARTESIAN_POINT('Ctrl Pts',(-3.46627841739718,-0.309985995947102,
17.3363714306813));
#62605=CARTESIAN_POINT('Ctrl Pts',(-1.61209757425368,-3.08420472661629,
17.495521029075));
#62606=CARTESIAN_POINT('Ctrl Pts',(1.7241472355999,-3.0229941605253,17.6546706274685));
#62607=CARTESIAN_POINT('Ctrl Pts',(3.47531646938709,-0.182627550505842,
17.8138202258621));
#62608=CARTESIAN_POINT('Ctrl Pts',(2.03149217768794,2.82563566593247,17.9729698242556));
#62609=CARTESIAN_POINT('Ctrl Pts',(-1.27996184268848,3.2361821743929,18.1321194226493));
#62610=CARTESIAN_POINT('Ctrl Pts',(-3.4146971854187,0.671580610567688,18.2912690210428));
#62611=CARTESIAN_POINT('Ctrl Pts',(-2.41016866685424,-2.5104311147512,18.4504186194364));
#62612=CARTESIAN_POINT('Ctrl Pts',(0.810121597082249,-3.38450592886727,
18.6095682178299));
#62613=CARTESIAN_POINT('Ctrl Pts',(3.28563558515027,-1.1470728774542,18.7687178162235));
#62614=CARTESIAN_POINT('Ctrl Pts',(2.74053705803234,2.14490886010299,18.9278674146171));
#62615=CARTESIAN_POINT('Ctrl Pts',(-0.324043718802237,3.46499250401812,
19.0870170130107));
#62616=CARTESIAN_POINT('Ctrl Pts',(-3.09071850846487,1.59957384513173,19.2461666114042));
#62617=CARTESIAN_POINT('Ctrl Pts',(-3.01597562850516,-1.73639522945087,
19.4053162097978));
#62618=CARTESIAN_POINT('Ctrl Pts',(-0.168529113932866,-3.47602867110644,
19.5644658081914));
#62619=CARTESIAN_POINT('Ctrl Pts',(2.83385276627145,-2.02001383254979,19.723615406585));
#62620=CARTESIAN_POINT('Ctrl Pts',(3.23096363873481,1.29307824580353,19.8827650049785));
#62621=CARTESIAN_POINT('Ctrl Pts',(0.657724041601946,3.41739322725609,20.0419146033721));
#62622=CARTESIAN_POINT('Ctrl Pts',(-2.52018683453118,2.3999657713502,20.2010642017657));
#62623=CARTESIAN_POINT('Ctrl Pts',(-3.38119198703589,-0.823843511476016,
20.3602138001593));
#62624=CARTESIAN_POINT('Ctrl Pts',(-1.13373590955914,-3.29026142912276,
20.5193633985529));
#62625=CARTESIAN_POINT('Ctrl Pts',(2.1560076610309,-2.73181411340027,20.6785129969464));
#62626=CARTESIAN_POINT('Ctrl Pts',(3.46364957884472,0.338096109953581,20.83766259534));
#62627=CARTESIAN_POINT('Ctrl Pts',(1.58702379717214,3.09718143669468,20.9968121937336));
#62628=CARTESIAN_POINT('Ctrl Pts',(-1.74861465325227,3.00890747265985,21.1559617921271));
#62629=CARTESIAN_POINT('Ctrl Pts',(-3.47668367944616,0.154427904439827,
21.3151113905207));
#62630=CARTESIAN_POINT('Ctrl Pts',(-2.00850225079915,-2.84202323937219,
21.4742609889143));
#62631=CARTESIAN_POINT('Ctrl Pts',(1.3061733730541,-3.22569194191282,21.6334105873079));
#62632=CARTESIAN_POINT('Ctrl Pts',(3.42003304048126,-0.643856650671137,
21.7925601857014));
#62633=CARTESIAN_POINT('Ctrl Pts',(2.38972338763523,2.52990108802421,21.951709784095));
#62634=CARTESIAN_POINT('Ctrl Pts',(-0.837551870632141,3.37782241223505,
22.1108593824886));
#62635=CARTESIAN_POINT('Ctrl Pts',(-3.29483313626591,1.12038028756356,22.2700089808822));
#62636=CARTESIAN_POINT('Ctrl Pts',(-2.72304622043883,-2.16707098775067,
22.4291585792757));
#62637=CARTESIAN_POINT('Ctrl Pts',(0.352142938187871,-3.46224966397303,
22.5883081776693));
#62638=CARTESIAN_POINT('Ctrl Pts',(3.10359340496692,-1.57444763686911,22.7474577760629));
#62639=CARTESIAN_POINT('Ctrl Pts',(3.00178980928638,1.76080530594988,22.9066073744565));
#62640=CARTESIAN_POINT('Ctrl Pts',(0.140324154043218,3.47728148362897,23.06575697285));
#62641=CARTESIAN_POINT('Ctrl Pts',(-2.8501469508005,1.99695762184366,23.2249065712436));
#62642=CARTESIAN_POINT('Ctrl Pts',(-3.22036717066564,-1.31924700897744,
23.3840561696372));
#62643=CARTESIAN_POINT('Ctrl Pts',(-0.629978665944583,-3.42261658165964,
23.5432057680308));
#62644=CARTESIAN_POINT('Ctrl Pts',(2.53957371539527,-2.37944168423399,23.7023553664243));
#62645=CARTESIAN_POINT('Ctrl Pts',(3.37439725990662,0.851246448997968,23.8615049648179));
#62646=CARTESIAN_POINT('Ctrl Pts',(1.10700623121625,3.29935063135843,24.0206545632115));
#62647=CARTESIAN_POINT('Ctrl Pts',(-2.17809865823012,2.7142335234119,24.179804161605));
#62648=CARTESIAN_POINT('Ctrl Pts',(-3.46079278243677,-0.366183972383433,
24.3389537599987));
#62649=CARTESIAN_POINT('Ctrl Pts',(-1.56184557114644,-3.10995430778124,
24.4981033583922));
#62650=CARTESIAN_POINT('Ctrl Pts',(1.77296698696289,-2.99462275549635,24.6572529567858));
#62651=CARTESIAN_POINT('Ctrl Pts',(3.47782207381884,-0.126218094801235,
24.8164025551794));
#62652=CARTESIAN_POINT('Ctrl Pts',(1.98538013563459,2.85822376689167,24.9755521535729));
#62653=CARTESIAN_POINT('Ctrl Pts',(-1.33229893846449,3.21498941260517,25.1347017519665));
#62654=CARTESIAN_POINT('Ctrl Pts',(-3.42514380828257,0.616090315765816,
25.2938513503601));
#62655=CARTESIAN_POINT('Ctrl Pts',(-2.36912083031805,-2.54920455749435,
25.4530009487536));
#62656=CARTESIAN_POINT('Ctrl Pts',(0.864927021247645,-3.37091658640681,
25.6121505471473));
#62657=CARTESIAN_POINT('Ctrl Pts',(3.30381384007098,-1.0936139605694,25.7713001455407));
#62658=CARTESIAN_POINT('Ctrl Pts',(2.70537616732062,2.18909049102374,25.9304497439344));
#62659=CARTESIAN_POINT('Ctrl Pts',(-0.380218981513895,3.45927895820695,
26.0895993423279));
#62660=CARTESIAN_POINT('Ctrl Pts',(-3.11626404047753,1.54921780735424,26.2487489407215));
#62661=CARTESIAN_POINT('Ctrl Pts',(-2.98740642921401,-1.78509949618719,
26.4078985391151));
#62662=CARTESIAN_POINT('Ctrl Pts',(-0.112109958810153,-3.47830544112107,
26.5670481375086));
#62663=CARTESIAN_POINT('Ctrl Pts',(2.86625355475253,-1.97376998266397,26.7261977359023));
#62664=CARTESIAN_POINT('Ctrl Pts',(3.20955875621522,1.34532894676326,26.8853473342958));
#62665=CARTESIAN_POINT('Ctrl Pts',(0.602191828648999,3.42761467876791,27.0444969326894));
#62666=CARTESIAN_POINT('Ctrl Pts',(-2.55879345585885,2.3587609957032,27.203646531083));
#62667=CARTESIAN_POINT('Ctrl Pts',(-3.36738044900546,-0.878593362285773,
27.3627961294765));
#62668=CARTESIAN_POINT('Ctrl Pts',(-1.08020369597472,-3.30822268896751,
27.5219457278701));
#62669=CARTESIAN_POINT('Ctrl Pts',(2.20004630527573,-2.69647429790079,27.6810953262637));
#62670=CARTESIAN_POINT('Ctrl Pts',(3.45770821619155,0.394247734652099,27.8402449246573));
#62671=CARTESIAN_POINT('Ctrl Pts',(1.53656455326529,3.12252249923767,27.9993945230509));
#62672=CARTESIAN_POINT('Ctrl Pts',(-1.79720263399863,2.98014094917425,28.1585441214444));
#62673=CARTESIAN_POINT('Ctrl Pts',(-3.47873157758249,0.0979999782004309,
28.317693719838));
#62674=CARTESIAN_POINT('Ctrl Pts',(-1.96212735396128,-2.87423618226371,
28.4768433182315));
#62675=CARTESIAN_POINT('Ctrl Pts',(1.35833681948244,-3.20407529084994,28.6359929166252));
#62676=CARTESIAN_POINT('Ctrl Pts',(3.43002915246079,-0.588283433275092,
28.7951425150187));
#62677=CARTESIAN_POINT('Ctrl Pts',(2.34836235084664,2.56834025271633,28.9542921134123));
#62678=CARTESIAN_POINT('Ctrl Pts',(-0.892245247251056,3.36378890588496,
29.1134417118058));
#62679=CARTESIAN_POINT('Ctrl Pts',(-3.31257710550631,1.06677565808014,29.2725913101995));
#62680=CARTESIAN_POINT('Ctrl Pts',(-2.68752806162076,-2.21096592072287,
29.431740908593));
#62681=CARTESIAN_POINT('Ctrl Pts',(0.408270000973746,-3.45608058223499,
29.5908905069866));
#62682=CARTESIAN_POINT('Ctrl Pts',(3.1287295810871,-1.52388601707194,29.7500401053801));
#62683=CARTESIAN_POINT('Ctrl Pts',(2.97282643492082,1.80927620125641,29.9091897037738));
#62684=CARTESIAN_POINT('Ctrl Pts',(0.0838883851327475,3.47910047619161,
30.0683393021673));
#62685=CARTESIAN_POINT('Ctrl Pts',(-2.8821715180818,1.95045244109027,30.2274889005609));
#62686=CARTESIAN_POINT('Ctrl Pts',(-3.19853910673239,-1.37132234259506,
30.3866384989544));
#62687=CARTESIAN_POINT('Ctrl Pts',(-0.57436535848797,-3.43238718963432,
30.5457880973481));
#62688=CARTESIAN_POINT('Ctrl Pts',(2.57784479098707,-2.33792506684404,30.7049376957416));
#62689=CARTESIAN_POINT('Ctrl Pts',(3.36014201613933,0.905882451520032,30.8640872941352));
#62690=CARTESIAN_POINT('Ctrl Pts',(1.053330067826,3.31687701804131,31.0232368925287));
#62691=CARTESIAN_POINT('Ctrl Pts',(-2.22184915769754,2.67853760567881,31.1823864909223));
#62692=CARTESIAN_POINT('Ctrl Pts',(-3.45439608311781,-0.422285549761243,
31.3415360893159));
#62693=CARTESIAN_POINT('Ctrl Pts',(-1.51118240738248,-3.13488518389664,
31.5006856877095));
#62694=CARTESIAN_POINT('Ctrl Pts',(1.82131999930616,-2.9654630068042,31.659835286103));
#62695=CARTESIAN_POINT('Ctrl Pts',(3.47941213087869,-0.0697754117944455,
31.8189848844967));
#62696=CARTESIAN_POINT('Ctrl Pts',(1.93874543614596,2.89005943164153,31.9781344828902));
#62697=CARTESIAN_POINT('Ctrl Pts',(-1.38428530244174,3.19295029495303,32.1372840812838));
#62698=CARTESIAN_POINT('Ctrl Pts',(-3.43468875149016,0.560437833290886,
32.2964336796773));
#62699=CARTESIAN_POINT('Ctrl Pts',(-2.32744931542688,-2.58730691428671,
32.4555832780709));
#62700=CARTESIAN_POINT('Ctrl Pts',(0.919504750710926,-3.35643983977321,
32.6147328764645));
#62701=CARTESIAN_POINT('Ctrl Pts',(3.32112235582321,-1.03986714644137,32.7738824748581));
#62702=CARTESIAN_POINT('Ctrl Pts',(2.66950307800085,2.2326958371308,32.9330320732517));
#62703=CARTESIAN_POINT('Ctrl Pts',(-0.436294150407741,3.45265474655611,
33.0921816716452));
#62704=CARTESIAN_POINT('Ctrl Pts',(-3.14098920638393,1.49845393321781,33.2513312700388));
#62705=CARTESIAN_POINT('Ctrl Pts',(-2.95805078598005,-1.83333382998357,
33.4104808684324));
#62706=CARTESIAN_POINT('Ctrl Pts',(-0.0556612903949957,-3.47966653651546,
33.569630466826));
#62707=CARTESIAN_POINT('Ctrl Pts',(2.89789979315677,-1.92700653175223,33.7287800652195));
#62708=CARTESIAN_POINT('Ctrl Pts',(3.18730894747029,1.39722548573591,33.8879296636131));
#62709=CARTESIAN_POINT('Ctrl Pts',(0.546501086838704,3.43693380015624,34.0470792620067));
#62710=CARTESIAN_POINT('Ctrl Pts',(-2.59672646692132,2.31693526896525,34.2062288604002));
#62711=CARTESIAN_POINT('Ctrl Pts',(-3.35268243771507,-0.93311192069785,
34.3653784587938));
#62712=CARTESIAN_POINT('Ctrl Pts',(-1.02638711541363,-3.32531304898012,
34.5245280571874));
#62713=CARTESIAN_POINT('Ctrl Pts',(2.2435057805037,-2.66042462727713,34.683677655581));
#62714=CARTESIAN_POINT('Ctrl Pts',(3.45085660129929,0.450295572495346,34.8428272539745));
#62715=CARTESIAN_POINT('Ctrl Pts',(1.48570080382082,3.14704154797274,35.0019768523681));
#62716=CARTESIAN_POINT('Ctrl Pts',(-1.84531749526043,2.95058989467884,35.1611264507617));
#62717=CARTESIAN_POINT('Ctrl Pts',(-3.47986368959678,0.0415462526435041,
35.3202760491553));
#62718=CARTESIAN_POINT('Ctrl Pts',(-1.91523591975808,-2.90569247263341,
35.4794256475488));
#62719=CARTESIAN_POINT('Ctrl Pts',(1.41014267708635,-3.18161515899672,35.6385752459424));
#62720=CARTESIAN_POINT('Ctrl Pts',(3.43912230342089,-0.532555344832574,
35.797724844336));
#62721=CARTESIAN_POINT('Ctrl Pts',(2.30638309143408,2.60610328701889,35.9568744427296));
#62722=CARTESIAN_POINT('Ctrl Pts',(-0.946703720385058,3.34886988492517,
36.1160240411231));
#62723=CARTESIAN_POINT('Ctrl Pts',(-3.32944906139014,1.01289017147471,36.2751736395167));
#62724=CARTESIAN_POINT('Ctrl Pts',(-2.65130234024599,-2.25427876213499,
36.4343232379102));
#62725=CARTESIAN_POINT('Ctrl Pts',(0.464289466150589,-3.44900176816319,
36.5934728363039));
#62726=CARTESIAN_POINT('Ctrl Pts',(3.15304233706577,-1.47292305497444,36.7526224346974));
#62727=CARTESIAN_POINT('Ctrl Pts',(2.94308002069685,1.85727046589526,36.911772033091));
#62728=CARTESIAN_POINT('Ctrl Pts',(0.0274313606274201,3.48000422041144,
37.0709216314846));
#62729=CARTESIAN_POINT('Ctrl Pts',(-2.91343892506985,1.90343258514806,37.2300712298781));
#62730=CARTESIAN_POINT('Ctrl Pts',(-3.17586600267692,-1.4230343579686,37.3892208282717));
#62731=CARTESIAN_POINT('Ctrl Pts',(-0.518606599465324,-3.44125862475635,
37.5483704266653));
#62732=CARTESIAN_POINT('Ctrl Pts',(2.61544821472821,-2.29578456290637,37.7075200250589));
#62733=CARTESIAN_POINT('Ctrl Pts',(3.34498126840255,0.960263912504391,37.8666696234524));
#62734=CARTESIAN_POINT('Ctrl Pts',(0.999416555317858,3.33356087664399,38.025819221846));
#62735=CARTESIAN_POINT('Ctrl Pts',(-2.26509095496236,2.64207807872185,38.1849688202396));
#62736=CARTESIAN_POINT('Ctrl Pts',(-3.44694460696967,-0.478164392868984,
38.3441184186332));
#62737=CARTESIAN_POINT('Ctrl Pts',(-1.46039886746108,-3.15920366970597,
38.5032680170267));
#62738=CARTESIAN_POINT('Ctrl Pts',(1.86972333428146,-2.93511622232055,38.6624176154203));
#62739=CARTESIAN_POINT('Ctrl Pts',(3.47907139646688,-0.0140916651033557,
38.8215672138139));
#62740=CARTESIAN_POINT('Ctrl Pts',(1.89357215294747,2.92263494718828,38.9807168122074));
#62741=CARTESIAN_POINT('Ctrl Pts',(-1.43998038369654,3.16705211734282,39.1398664106011));
#62742=CARTESIAN_POINT('Ctrl Pts',(-2.7687072675905,1.39687744165701,39.2459661428634));
#62743=CARTESIAN_POINT('Ctrl Pts',(-2.91090525077878,0.426608275808765,
39.2990160089946));
#62744=CARTESIAN_POINT('Ctrl Pts',(1.59774743137961,-2.24059110187415,-0.219489327336922));
#62745=CARTESIAN_POINT('Ctrl Pts',(2.34458605102921,-1.70802650978855,-0.166439461205731));
#62746=CARTESIAN_POINT('Ctrl Pts',(3.25063923968512,0.153557917939087,-0.0603397289433482));
#62747=CARTESIAN_POINT('Ctrl Pts',(1.62409624279688,2.82369221612243,0.0988098694502261));
#62748=CARTESIAN_POINT('Ctrl Pts',(-1.49696874765322,2.88957558687682,0.2579594678438));
#62749=CARTESIAN_POINT('Ctrl Pts',(-3.2410619746254,0.30312732483917,0.417109066237375));
#62750=CARTESIAN_POINT('Ctrl Pts',(-2.00591445868996,-2.56415991055002,
0.576258664630948));
#62751=CARTESIAN_POINT('Ctrl Pts',(1.07355449255992,-3.0729844518909,0.735408263024524));
#62752=CARTESIAN_POINT('Ctrl Pts',(3.16595493165337,-0.757287358952449,
0.894557861418096));
#62753=CARTESIAN_POINT('Ctrl Pts',(2.34782661214163,2.25492392933661,1.05370745981167));
#62754=CARTESIAN_POINT('Ctrl Pts',(-0.628779687067362,3.19393325538333,
1.21285705820524));
#62755=CARTESIAN_POINT('Ctrl Pts',(-3.02730880575264,1.19672088192463,1.37200665659882));
#62756=CARTESIAN_POINT('Ctrl Pts',(-2.64272342139147,-1.90072822769928,
1.53115625499239));
#62757=CARTESIAN_POINT('Ctrl Pts',(0.171424612330327,-3.25074055650477,
1.69030585338597));
#62758=CARTESIAN_POINT('Ctrl Pts',(2.8279730938224,-1.61223300963656,1.84945545177954));
#62759=CARTESIAN_POINT('Ctrl Pts',(2.88465715435138,1.50846945320346,2.00860505017312));
#62760=CARTESIAN_POINT('Ctrl Pts',(0.289363142217337,3.24237393471646,2.16775464856669));
#62761=CARTESIAN_POINT('Ctrl Pts',(-2.57195333199973,1.99543978679069,2.32690424696027));
#62762=CARTESIAN_POINT('Ctrl Pts',(-3.06877329840881,-1.08598065252297,
2.48605384535384));
#62763=CARTESIAN_POINT('Ctrl Pts',(-0.74435059115853,-3.16901637694623,
2.64520344374742));
#62764=CARTESIAN_POINT('Ctrl Pts',(2.26438250301455,-2.33865241230782,2.80435304214099));
#62765=CARTESIAN_POINT('Ctrl Pts',(3.19138076371783,0.641725758369828,2.96350264053456));
#62766=CARTESIAN_POINT('Ctrl Pts',(1.18441861774923,3.03214042374254,3.12265223892814));
#62767=CARTESIAN_POINT('Ctrl Pts',(-1.91142559845319,2.63499056654934,3.28180183732171));
#62768=CARTESIAN_POINT('Ctrl Pts',(-3.25002196309905,-0.184608567080839,
3.44095143571529));
#62769=CARTESIAN_POINT('Ctrl Pts',(-1.60074679787117,-2.8344898586703,3.60010103410886));
#62770=CARTESIAN_POINT('Ctrl Pts',(1.52015712313799,-2.87851444399281,3.75925063250244));
#62771=CARTESIAN_POINT('Ctrl Pts',(3.24352150863317,-0.276208802353544,
3.91840023089601));
#62772=CARTESIAN_POINT('Ctrl Pts',(1.98499048631045,2.58002632683958,4.07754982928958));
#62773=CARTESIAN_POINT('Ctrl Pts',(-1.0984194520178,3.06434296175893,4.23669942768315));
#62774=CARTESIAN_POINT('Ctrl Pts',(-3.17200968957183,0.731489992034621,
4.39584902607674));
#62775=CARTESIAN_POINT('Ctrl Pts',(-2.32944811466034,-2.27385016220058,
4.5549986244703));
#62776=CARTESIAN_POINT('Ctrl Pts',(0.654665664139852,-3.18875147157931,
4.71414822286388));
#62777=CARTESIAN_POINT('Ctrl Pts',(3.03691984923879,-1.17210959747432,4.87329782125745));
#62778=CARTESIAN_POINT('Ctrl Pts',(2.62721556343934,1.92209819270584,5.03244741965103));
#62779=CARTESIAN_POINT('Ctrl Pts',(-0.197790116974089,3.2492463970658,5.19159701804461));
#62780=CARTESIAN_POINT('Ctrl Pts',(-2.84095965420498,1.58923608138611,5.35074661643817));
#62781=CARTESIAN_POINT('Ctrl Pts',(-2.8723245453524,-1.53182074191662,5.50989621483176));
#62782=CARTESIAN_POINT('Ctrl Pts',(-0.263049826745572,-3.24461521106184,
5.66904581322532));
#62783=CARTESIAN_POINT('Ctrl Pts',(2.58805682306418,-1.97450878949499,5.82819541161891));
#62784=CARTESIAN_POINT('Ctrl Pts',(3.05986223049256,1.11084031688059,5.98734501001246));
#62785=CARTESIAN_POINT('Ctrl Pts',(0.718617344107592,3.1749507385077,6.14649460840606));
#62786=CARTESIAN_POINT('Ctrl Pts',(-2.28328040136243,2.3202055270938,6.30564420679962));
#62787=CARTESIAN_POINT('Ctrl Pts',(-3.18606971642545,-0.667594818193805,
6.4647938051932));
#62788=CARTESIAN_POINT('Ctrl Pts',(-1.15978128982235,-3.04164929585589,
6.62394340358677));
#62789=CARTESIAN_POINT('Ctrl Pts',(1.93273916042609,-2.61939733850326,6.78309300198035));
#62790=CARTESIAN_POINT('Ctrl Pts',(3.24841736956942,0.210968415366401,6.94224260037392));
#62791=CARTESIAN_POINT('Ctrl Pts',(1.57769921588541,2.84738270406301,7.1013921987675));
#62792=CARTESIAN_POINT('Ctrl Pts',(-1.54345915650127,2.86608738726072,7.26054179716106));
#62793=CARTESIAN_POINT('Ctrl Pts',(-3.24565552778308,0.249886522593035,
7.41969139555465));
#62794=CARTESIAN_POINT('Ctrl Pts',(-1.96399460475218,-2.5960447360758,7.57884099394821));
#62795=CARTESIAN_POINT('Ctrl Pts',(1.12324290433852,-3.0553311534195,7.7379905923418));
#62796=CARTESIAN_POINT('Ctrl Pts',(3.17783954790743,-0.705732872238579,
7.89714019073536));
#62797=CARTESIAN_POINT('Ctrl Pts',(2.31092476365828,2.29267307218309,8.05628978912895));
#62798=CARTESIAN_POINT('Ctrl Pts',(-0.680512987869373,3.18333553879317,
8.21543938752251));
#62799=CARTESIAN_POINT('Ctrl Pts',(-3.04632869622369,1.14743389951957,8.3745889859161));
#62800=CARTESIAN_POINT('Ctrl Pts',(-2.61153601490394,-1.94334832751677,
8.53373858430965));
#62801=CARTESIAN_POINT('Ctrl Pts',(0.22414324255659,-3.24753489373382,8.69288818270324));
#62802=CARTESIAN_POINT('Ctrl Pts',(2.85375890406606,-1.56613639146347,8.8520377810968));
#62803=CARTESIAN_POINT('Ctrl Pts',(2.85980307155329,1.55507217553943,9.0111873794904));
#62804=CARTESIAN_POINT('Ctrl Pts',(0.236719106893722,3.24664244160548,9.17033697788396));
#62805=CARTESIAN_POINT('Ctrl Pts',(-2.60398993466071,1.95344810511779,9.32948657627754));
#62806=CARTESIAN_POINT('Ctrl Pts',(-3.050749804979,-1.13562701034412,9.48863617467111));
#62807=CARTESIAN_POINT('Ctrl Pts',(-0.69283678848375,-3.1806760702288,9.64778577306469));
#62808=CARTESIAN_POINT('Ctrl Pts',(2.30202802014995,-2.30160597706191,9.80693537145825));
#62809=CARTESIAN_POINT('Ctrl Pts',(3.18054898365337,0.693419960618418,9.96608496985184));
#62810=CARTESIAN_POINT('Ctrl Pts',(1.13506762973426,3.05095797334739,10.1252345682454));
#62811=CARTESIAN_POINT('Ctrl Pts',(-1.9539255194228,2.60363172198968,10.284384166639));
#62812=CARTESIAN_POINT('Ctrl Pts',(-3.2465989840766,-0.237314381770985,
10.4435337650326));
#62813=CARTESIAN_POINT('Ctrl Pts',(-1.55454779837227,-2.86008814930212,
10.6026833634261));
#62814=CARTESIAN_POINT('Ctrl Pts',(1.56665960795514,-2.85347170163021,10.7618329618197));
#62815=CARTESIAN_POINT('Ctrl Pts',(3.24757593629035,-0.223547796299663,
10.9209825602133));
#62816=CARTESIAN_POINT('Ctrl Pts',(1.94286946412048,2.61189228809128,11.0801321586069));
#62817=CARTESIAN_POINT('Ctrl Pts',(-1.1479924311337,3.04611826055101,11.2392817570004));
#62818=CARTESIAN_POINT('Ctrl Pts',(-3.18346025880061,0.679929305030804,
11.398431355394));
#62819=CARTESIAN_POINT('Ctrl Pts',(-2.2922493206328,-2.3113450913399,11.5575809537876));
#62820=CARTESIAN_POINT('Ctrl Pts',(0.706315524074037,-3.17771009685506,
11.7167305521812));
#62821=CARTESIAN_POINT('Ctrl Pts',(3.05553705105848,-1.12268268393673,11.8758801505747));
#62822=CARTESIAN_POINT('Ctrl Pts',(2.59568458981499,1.9644705621107,12.0350297489683));
#62823=CARTESIAN_POINT('Ctrl Pts',(-0.250481616296216,3.24560965599688,
12.1941793473619));
#62824=CARTESIAN_POINT('Ctrl Pts',(-2.86637033563197,1.54293362728653,12.3533289457555));
#62825=CARTESIAN_POINT('Ctrl Pts',(-2.84709338166566,-1.57822126309276,
12.512478544149));
#62826=CARTESIAN_POINT('Ctrl Pts',(-0.210372807527127,-3.24845599647828,
12.6716281425426));
#62827=CARTESIAN_POINT('Ctrl Pts',(2.61975166634493,-1.9322588558176,12.8307777409362));
#62828=CARTESIAN_POINT('Ctrl Pts',(3.04143659634136,1.16033896325084,12.9899273393297));
#62829=CARTESIAN_POINT('Ctrl Pts',(0.66701063425504,3.1861920678128,13.1490769377233));
#62830=CARTESIAN_POINT('Ctrl Pts',(-2.3206241324531,2.28285494832214,13.3082265361169));
#62831=CARTESIAN_POINT('Ctrl Pts',(-3.1748189251083,-0.719199466057081,
13.4673761345105));
#62832=CARTESIAN_POINT('Ctrl Pts',(-1.11027926590465,-3.06006585401438,
13.626525732904));
#62833=CARTESIAN_POINT('Ctrl Pts',(1.97498328207596,-2.58769474913928,13.7856753312976));
#62834=CARTESIAN_POINT('Ctrl Pts',(3.24456692577273,0.263644729483094,13.9448249296912));
#62835=CARTESIAN_POINT('Ctrl Pts',(1.53129406930187,2.87260535969066,14.1039745280848));
#62836=CARTESIAN_POINT('Ctrl Pts',(-1.58975695072081,2.84066821660634,14.2631241264783));
#62837=CARTESIAN_POINT('Ctrl Pts',(-3.24928260768908,0.197194357352772,
14.4222737248719));
#62838=CARTESIAN_POINT('Ctrl Pts',(-1.9216164547924,-2.62756794010615,14.5814233232655));
#62839=CARTESIAN_POINT('Ctrl Pts',(1.17266640354997,-3.03670488938056,14.7405729216591));
#62840=CARTESIAN_POINT('Ctrl Pts',(3.18887145231711,-0.654080988715819,
14.8997225200526));
#62841=CARTESIAN_POINT('Ctrl Pts',(2.27342301470172,2.32986499081536,15.0588721184462));
#62842=CARTESIAN_POINT('Ctrl Pts',(-0.732071574579563,3.17187551598343,
15.2180217168398));
#62843=CARTESIAN_POINT('Ctrl Pts',(-3.06454430769971,1.09785757971964,15.3771713152334));
#62844=CARTESIAN_POINT('Ctrl Pts',(-2.57966233142462,-1.98546350634593,
15.5363209136269));
#62845=CARTESIAN_POINT('Ctrl Pts',(0.276803504750348,-3.24347081056088,
15.6954705120205));
#62846=CARTESIAN_POINT('Ctrl Pts',(2.87879311888926,-1.51962931593148,15.8546201104141));
#62847=CARTESIAN_POINT('Ctrl Pts',(2.83419631216968,1.60126648103505,16.0137697088077));
#62848=CARTESIAN_POINT('Ctrl Pts',(0.18401266261032,3.25005575632197,16.1729193072012));
#62849=CARTESIAN_POINT('Ctrl Pts',(-2.63534098076865,1.91094243615129,16.3320689055948));
#62850=CARTESIAN_POINT('Ctrl Pts',(-3.03192321752246,-1.1849745491996,16.4912185039884));
#62851=CARTESIAN_POINT('Ctrl Pts',(-0.64114058115313,-3.19149836822788,
16.650368102382));
#62852=CARTESIAN_POINT('Ctrl Pts',(2.33906751438082,-2.26395367496133,16.8095177007755));
#62853=CARTESIAN_POINT('Ctrl Pts',(3.1688799179103,0.744931637848302,16.9686672991691));
#62854=CARTESIAN_POINT('Ctrl Pts',(1.08541782976375,3.06897233842756,17.1278168975627));
#62855=CARTESIAN_POINT('Ctrl Pts',(-1.99591106248259,2.57158746883364,17.2869664959562));
#62856=CARTESIAN_POINT('Ctrl Pts',(-3.24232132839643,-0.289957725587986,
17.4461160943498));
#62857=CARTESIAN_POINT('Ctrl Pts',(-1.50793955910327,-2.8849335114165,17.6052656927434));
#62858=CARTESIAN_POINT('Ctrl Pts',(1.6127496646616,-2.82767777484218,17.764415291137));
#62859=CARTESIAN_POINT('Ctrl Pts',(3.25077542965584,-0.17082794018687,17.9235648895305));
#62860=CARTESIAN_POINT('Ctrl Pts',(1.90023697552094,2.64307066043752,18.0827144879241));
#62861=CARTESIAN_POINT('Ctrl Pts',(-1.19726319768579,3.02709165944306,18.2418640863177));
#62862=CARTESIAN_POINT('Ctrl Pts',(-3.19407277232272,0.628189624483898,
18.4010136847113));
#62863=CARTESIAN_POINT('Ctrl Pts',(-2.25444708490623,-2.34823155173427,
18.5601632831048));
#62864=CARTESIAN_POINT('Ctrl Pts',(0.757779444268192,-3.16583218017745,
18.7193128814984));
#62865=CARTESIAN_POINT('Ctrl Pts',(3.0733498733406,-1.07296022071643,18.878462479892));
#62866=CARTESIAN_POINT('Ctrl Pts',(2.56347029422739,2.00632577858539,19.0376120782856));
#62867=CARTESIAN_POINT('Ctrl Pts',(-0.303107175560938,3.24111849819258,
19.1967616766791));
#62868=CARTESIAN_POINT('Ctrl Pts',(-2.89102643624049,1.49622499115646,19.3559112750727));
#62869=CARTESIAN_POINT('Ctrl Pts',(-2.82111271187761,-1.62420631266014,
19.5150608734663));
#62870=CARTESIAN_POINT('Ctrl Pts',(-0.15764040701926,-3.25144161584941,
19.6742104718599));
#62871=CARTESIAN_POINT('Ctrl Pts',(2.65075685193123,-1.88950024904527,19.8333600702534));
#62872=CARTESIAN_POINT('Ctrl Pts',(3.02221029463916,1.20953214681529,19.992509668647));
#62873=CARTESIAN_POINT('Ctrl Pts',(0.615228331798773,3.19659462224329,20.1516592670406));
#62874=CARTESIAN_POINT('Ctrl Pts',(-2.35735695209384,2.24490340095456,20.3108088654341));
#62875=CARTESIAN_POINT('Ctrl Pts',(-3.16273235293131,-0.770614782445889,
20.4699584638278));
#62876=CARTESIAN_POINT('Ctrl Pts',(-1.06048495755082,-3.07767684041242,
20.6291080622213));
#62877=CARTESIAN_POINT('Ctrl Pts',(2.01670748329427,-2.55531094116301,20.7882576606149));
#62878=CARTESIAN_POINT('Ctrl Pts',(3.23986233974024,0.316251638312774,20.9474072590085));
#62879=CARTESIAN_POINT('Ctrl Pts',(1.4844858048385,2.89707179311033,21.106556857402));
#62880=CARTESIAN_POINT('Ctrl Pts',(-1.63563623652694,2.81450123129526,21.2657064557956));
#62881=CARTESIAN_POINT('Ctrl Pts',(-3.25205430394149,0.14445028009062,21.4248560541892));
#62882=CARTESIAN_POINT('Ctrl Pts',(-1.8787324333827,-2.65839942878388,21.5840056525828));
#62883=CARTESIAN_POINT('Ctrl Pts',(1.2217811947191,-3.01727920342704,21.7431552509763));
#62884=CARTESIAN_POINT('Ctrl Pts',(3.19906387649592,-0.602256916358366,
21.9023048493699));
#62885=CARTESIAN_POINT('Ctrl Pts',(2.23532278013483,2.36644356531332,22.0614544477634));
#62886=CARTESIAN_POINT('Ctrl Pts',(-0.783437441193132,3.15958048717536,
22.2206040461571));
#62887=CARTESIAN_POINT('Ctrl Pts',(-3.08195316844857,1.04799224553065,22.3797536445506));
#62888=CARTESIAN_POINT('Ctrl Pts',(-2.54710954389172,-2.02705600579221,
22.5389032429442));
#62889=CARTESIAN_POINT('Ctrl Pts',(0.329390897568978,-3.23855287370784,
22.6980528413378));
#62890=CARTESIAN_POINT('Ctrl Pts',(2.90306948255782,-1.47272219330192,22.8572024397313));
#62891=CARTESIAN_POINT('Ctrl Pts',(2.80784344187814,1.64703924819794,23.0163520381249));
#62892=CARTESIAN_POINT('Ctrl Pts',(0.131257776426808,3.2526134838511,23.1755016365185));
#62893=CARTESIAN_POINT('Ctrl Pts',(-2.66599826524709,1.86793370570319,23.3346512349121));
#62894=CARTESIAN_POINT('Ctrl Pts',(-3.01229846694121,-1.23401013985552,
23.4938008333056));
#62895=CARTESIAN_POINT('Ctrl Pts',(-0.589275591589926,-3.20148049445235,
23.6529504316992));
#62896=CARTESIAN_POINT('Ctrl Pts',(2.37549124188466,-2.22570538008331,23.8121000300928));
#62897=CARTESIAN_POINT('Ctrl Pts',(3.15637663476935,0.796247209530284,23.9712496284864));
#62898=CARTESIAN_POINT('Ctrl Pts',(1.03548229020669,3.08617878708782,24.1303992268799));
#62899=CARTESIAN_POINT('Ctrl Pts',(-2.03737117580815,2.53886623735648,24.2895488252735));
#62900=CARTESIAN_POINT('Ctrl Pts',(-3.23719012164088,-0.3425247371407,24.4486984236671));
#62901=CARTESIAN_POINT('Ctrl Pts',(-1.46093435010116,-2.90901940589901,
24.6078480220607));
#62902=CARTESIAN_POINT('Ctrl Pts',(1.65841516005192,-2.80113945317124,24.7669976204542));
#62903=CARTESIAN_POINT('Ctrl Pts',(3.25311914637773,-0.118063113092684,
24.9261472188478));
#62904=CARTESIAN_POINT('Ctrl Pts',(1.85710424368523,2.67355323629226,25.0852968172414));
#62905=CARTESIAN_POINT('Ctrl Pts',(-1.24621878101377,3.00726816713295,25.244446415635));
#62906=CARTESIAN_POINT('Ctrl Pts',(-3.20384443635041,0.576284571083659,
25.4035960140285));
#62907=CARTESIAN_POINT('Ctrl Pts',(-2.21605135904132,-2.38449983294058,
25.5627456124222));
#62908=CARTESIAN_POINT('Ctrl Pts',(0.80904387668984,-3.1531208484283,25.7218952108157));
#62909=CARTESIAN_POINT('Ctrl Pts',(3.09035362680328,-1.02295529741349,25.8810448092093));
#62910=CARTESIAN_POINT('Ctrl Pts',(2.53058115718985,2.04765282361984,26.0401944076028));
#62911=CARTESIAN_POINT('Ctrl Pts',(-0.355652940928235,3.2357741059616,26.1993440059964));
#62912=CARTESIAN_POINT('Ctrl Pts',(-2.9149214652359,1.44912246918937,26.3584936043899));
#62913=CARTESIAN_POINT('Ctrl Pts',(-2.79438937547971,-1.66976378491353,
26.5176432027836));
#62914=CARTESIAN_POINT('Ctrl Pts',(-0.104866507188719,-3.25357128320136,
26.6767928011771));
#62915=CARTESIAN_POINT('Ctrl Pts',(2.68106421761248,-1.84624422551311,26.8359423995708));
#62916=CARTESIAN_POINT('Ctrl Pts',(3.00218838676911,1.25840691731703,26.9950919979642));
#62917=CARTESIAN_POINT('Ctrl Pts',(0.563284068589358,3.20615566329458,27.1542415963579));
#62918=CARTESIAN_POINT('Ctrl Pts',(-2.39346919025677,2.20636087585285,27.3133911947514));
#62919=CARTESIAN_POINT('Ctrl Pts',(-3.14981318172185,-0.821827232119886,
27.472540793145));
#62920=CARTESIAN_POINT('Ctrl Pts',(-1.0104114732658,-3.09447761890361,27.6316903915386));
#62921=CARTESIAN_POINT('Ctrl Pts',(2.0579007800566,-2.52225443971164,27.7908399899321));
#62922=CARTESIAN_POINT('Ctrl Pts',(3.23430484996867,0.368775292924697,27.9499895883257));
#62923=CARTESIAN_POINT('Ctrl Pts',(1.43728674491509,2.92077556345809,28.1091391867193));
#62924=CARTESIAN_POINT('Ctrl Pts',(-1.68108493605638,2.78759331986695,28.2682887851129));
#62925=CARTESIAN_POINT('Ctrl Pts',(-3.25396988688269,0.0916681758473751,
28.4274383835065));
#62926=CARTESIAN_POINT('Ctrl Pts',(-1.83535382987383,-2.68853108562466,
28.5865879819));
#62927=CARTESIAN_POINT('Ctrl Pts',(1.27057434822587,-2.99705920943062,28.7457375802936));
#62928=CARTESIAN_POINT('Ctrl Pts',(3.20841413725675,-0.550274298012868,
28.9048871786872));
#62929=CARTESIAN_POINT('Ctrl Pts',(2.19663408996178,2.40239916625452,29.0640367770808));
#62930=CARTESIAN_POINT('Ctrl Pts',(-0.83459706548745,3.14645368907319,29.2231863754743));
#62931=CARTESIAN_POINT('Ctrl Pts',(-3.09855069553404,0.997851024155426,
29.3823359738679));
#62932=CARTESIAN_POINT('Ctrl Pts',(-2.51388622192681,-2.06811487650207,
29.5414855722615));
#62933=CARTESIAN_POINT('Ctrl Pts',(0.381891577219384,-3.23278237783669,
29.700635170655));
#62934=CARTESIAN_POINT('Ctrl Pts',(2.92658160424422,-1.42542737201929,29.8597847690487));
#62935=CARTESIAN_POINT('Ctrl Pts',(2.78075139815295,1.6923784272062,30.0189343674421));
#62936=CARTESIAN_POINT('Ctrl Pts',(0.078468336229367,3.25431495086323,30.1780839658358));
#62937=CARTESIAN_POINT('Ctrl Pts',(-2.6959537174715,1.82443323595418,30.3372335642293));
#62938=CARTESIAN_POINT('Ctrl Pts',(-2.99188071951124,-1.28272087354164,
30.4963831626229));
#62939=CARTESIAN_POINT('Ctrl Pts',(-0.53725547341239,-3.21061982107676,
30.6555327610165));
#62940=CARTESIAN_POINT('Ctrl Pts',(2.41128961400306,-2.18687116140927,30.81468235941));
#62941=CARTESIAN_POINT('Ctrl Pts',(3.14304242575827,0.847353166682053,30.9738319578037));
#62942=CARTESIAN_POINT('Ctrl Pts',(0.985274156747698,3.10257278967758,31.1329815561972));
#62943=CARTESIAN_POINT('Ctrl Pts',(-2.078294944897,2.50547664152315,31.2921311545908));
#62944=CARTESIAN_POINT('Ctrl Pts',(-3.2312067146159,-0.395001578001435,
31.4512807529843));
#62945=CARTESIAN_POINT('Ctrl Pts',(-1.41354454563206,-2.93233949206372,
31.610430351378));
#62946=CARTESIAN_POINT('Ctrl Pts',(1.70364407254376,-2.77386372291233,31.7695799497715));
#62947=CARTESIAN_POINT('Ctrl Pts',(3.25460646946541,-0.065267205520362,
31.9287295481651));
#62948=CARTESIAN_POINT('Ctrl Pts',(1.81348262343787,2.70333199102358,32.0878791465587));
#62949=CARTESIAN_POINT('Ctrl Pts',(-1.29484629340955,2.98665300221604,32.2470287449522));
#62950=CARTESIAN_POINT('Ctrl Pts',(-3.21277267846304,0.524227808995236,
32.4061783433458));
#62951=CARTESIAN_POINT('Ctrl Pts',(-2.17707225083119,-2.42014038722208,
32.5653279417394));
#62952=CARTESIAN_POINT('Ctrl Pts',(0.860095325819289,-3.13957944790481,
32.724477540133));
#62953=CARTESIAN_POINT('Ctrl Pts',(3.10654383515604,-0.972681077978029,
32.8836271385265));
#62954=CARTESIAN_POINT('Ctrl Pts',(2.49702583686903,2.08844081774213,33.0427767369201));
#62955=CARTESIAN_POINT('Ctrl Pts',(-0.408105079563564,3.22957788623167,
33.2019263353136));
#62956=CARTESIAN_POINT('Ctrl Pts',(-2.93804913217808,1.40163846126938,33.3610759337073));
#62957=CARTESIAN_POINT('Ctrl Pts',(-2.76693040747283,-1.71488168670816,
33.5202255321008));
#62958=CARTESIAN_POINT('Ctrl Pts',(-0.0520650009267163,-3.25484443789231,
33.6793751304944));
#62959=CARTESIAN_POINT('Ctrl Pts',(2.71066578488031,-1.80250217250329,33.838524728888));
#62960=CARTESIAN_POINT('Ctrl Pts',(2.98137614356199,1.30695040832354,33.9976743272815));
#62961=CARTESIAN_POINT('Ctrl Pts',(0.511191519110511,3.21487267399046,34.1568239256752));
#62962=CARTESIAN_POINT('Ctrl Pts',(-2.42895134027704,2.16723751946073,34.3159735240686));
#62963=CARTESIAN_POINT('Ctrl Pts',(-3.13606481250469,-0.872823333254088,
34.4751231224623));
#62964=CARTESIAN_POINT('Ctrl Pts',(-0.960071995023433,-3.11046376661199,
34.6342727208558));
#62965=CARTESIAN_POINT('Ctrl Pts',(2.09855232805267,-2.48853394704777,34.7934223192495));
#62966=CARTESIAN_POINT('Ctrl Pts',(3.22789591957588,0.421201866375226,34.9525719176429));
#62967=CARTESIAN_POINT('Ctrl Pts',(1.38970931465493,2.94371043050936,35.1117215160366));
#62968=CARTESIAN_POINT('Ctrl Pts',(-1.72609108446586,2.7599515661676,35.2708711144301));
#62969=CARTESIAN_POINT('Ctrl Pts',(-3.25502885286523,0.0388619391867563,
35.4300207128238));
#62970=CARTESIAN_POINT('Ctrl Pts',(-1.79149206260406,-2.7179549774465,35.5891703112173));
#62971=CARTESIAN_POINT('Ctrl Pts',(1.31903301680886,-2.97605023214225,35.7483199096108));
#62972=CARTESIAN_POINT('Ctrl Pts',(3.21691977752854,-0.498146814876754,
35.9074695080045));
#62973=CARTESIAN_POINT('Ctrl Pts',(2.15736712067839,2.43772232175455,36.066619106398));
#62974=CARTESIAN_POINT('Ctrl Pts',(-0.885536963467963,3.13249858967495,
36.2257687047916));
#62975=CARTESIAN_POINT('Ctrl Pts',(-3.11433255025735,0.947447091904948,
36.3849183031851));
#62976=CARTESIAN_POINT('Ctrl Pts',(-2.48000105319356,-2.10862926472869,
36.5440679015787));
#62977=CARTESIAN_POINT('Ctrl Pts',(0.434291611168368,-3.22616092765844,
36.7032174999723));
#62978=CARTESIAN_POINT('Ctrl Pts',(2.94932350716411,-1.37775713925967,36.8623670983659));
#62979=CARTESIAN_POINT('Ctrl Pts',(2.75292690696447,1.73727177076979,37.0215166967595));
#62980=CARTESIAN_POINT('Ctrl Pts',(0.0256590137662085,3.25516030394989,
37.180666295153));
#62981=CARTESIAN_POINT('Ctrl Pts',(-2.72520092971278,1.78045134430509,37.3398158935466));
#62982=CARTESIAN_POINT('Ctrl Pts',(-2.97067253020624,-1.33109176306352,
37.4989654919402));
#62983=CARTESIAN_POINT('Ctrl Pts',(-0.485099301329773,-3.21891807062454,
37.6581150903338));
#62984=CARTESIAN_POINT('Ctrl Pts',(2.44646347141876,-2.14745336564863,37.8172646887273));
#62985=CARTESIAN_POINT('Ctrl Pts',(3.12886121760872,0.898221028286588,37.9764142871209));
#62986=CARTESIAN_POINT('Ctrl Pts',(0.934844009354873,3.11817870013068,38.1355638855145));
#62987=CARTESIAN_POINT('Ctrl Pts',(-2.1187428791559,2.47137277344305,38.2947134839081));
#62988=CARTESIAN_POINT('Ctrl Pts',(-3.22423668014841,-0.447270075507296,
38.4538630823016));
#62989=CARTESIAN_POINT('Ctrl Pts',(-1.36604214253824,-2.95508675460852,
38.6130126806952));
#62990=CARTESIAN_POINT('Ctrl Pts',(1.74892005631017,-2.74547765153221,38.7721622790888));
#62991=CARTESIAN_POINT('Ctrl Pts',(3.25428774998656,-0.0131811992043684,
38.9313118774823));
#62992=CARTESIAN_POINT('Ctrl Pts',(1.77122799701979,2.73380279461243,39.0904614758759));
#62993=CARTESIAN_POINT('Ctrl Pts',(-1.34694290196035,2.96242811214064,39.2496110742695));
#62994=CARTESIAN_POINT('Ctrl Pts',(-2.58982041971561,1.30662485145711,39.3557108065319));
#62995=CARTESIAN_POINT('Ctrl Pts',(-2.72283095673202,0.399045011671065,
39.4087606726631));
#62996=CARTESIAN_POINT('Ctrl Pts',(1.48738611075523,-2.08582659521596,-0.109744663668461));
#62997=CARTESIAN_POINT('Ctrl Pts',(2.18263829393873,-1.59004787463046,-0.0566947975372698));
#62998=CARTESIAN_POINT('Ctrl Pts',(3.0261076070133,0.142951201080473,0.0494049347251129));
#62999=CARTESIAN_POINT('Ctrl Pts',(1.5119149288697,2.6286511252168,0.208554533118687));
#63000=CARTESIAN_POINT('Ctrl Pts',(-1.39356852013302,2.68998372927258,0.367704131512261));
#63001=CARTESIAN_POINT('Ctrl Pts',(-3.01719187305616,0.282189389825537,
0.526853729905836));
#63002=CARTESIAN_POINT('Ctrl Pts',(-1.86735978830055,-2.38704551282824,
0.68600332829941));
#63003=CARTESIAN_POINT('Ctrl Pts',(0.999400787641171,-2.86072398086276,
0.845152926692984));
#63004=CARTESIAN_POINT('Ctrl Pts',(2.94727270414218,-0.704979195982167,
1.00430252508656));
#63005=CARTESIAN_POINT('Ctrl Pts',(2.18565501954578,2.09916941027963,1.16345212348013));
#63006=CARTESIAN_POINT('Ctrl Pts',(-0.585347943549101,2.97331847915074,
1.32260172187371));
#63007=CARTESIAN_POINT('Ctrl Pts',(-2.81820329184044,1.11405969633679,1.48175132026728));
#63008=CARTESIAN_POINT('Ctrl Pts',(-2.46018240076365,-1.7694390932359,1.64090091866086));
#63009=CARTESIAN_POINT('Ctrl Pts',(0.159583788034279,-3.02620192556914,
1.80005051705443));
#63010=CARTESIAN_POINT('Ctrl Pts',(2.63263630955052,-1.50087112564727,1.95920011544801));
#63011=CARTESIAN_POINT('Ctrl Pts',(2.68540502798266,1.40427483664047,2.11834971384158));
#63012=CARTESIAN_POINT('Ctrl Pts',(0.269375941557349,3.01841321203564,2.27749931223515));
#63013=CARTESIAN_POINT('Ctrl Pts',(-2.39430061873041,1.85760863414959,2.43664891062873));
#63014=CARTESIAN_POINT('Ctrl Pts',(-2.85680370468111,-1.01096863458373,
2.5957985090223));
#63015=CARTESIAN_POINT('Ctrl Pts',(-0.69293601045933,-2.95012268600915,
2.75494810741588));
#63016=CARTESIAN_POINT('Ctrl Pts',(2.10797465123312,-2.17711450986188,2.91409770580944));
#63017=CARTESIAN_POINT('Ctrl Pts',(2.97094229592146,0.597399789958587,3.07324730420303));
#63018=CARTESIAN_POINT('Ctrl Pts',(1.10260718731943,2.82270117514133,3.23239690259659));
#63019=CARTESIAN_POINT('Ctrl Pts',(-1.77939756374786,2.45298367794754,3.39154650099018));
#63020=CARTESIAN_POINT('Ctrl Pts',(-3.02553296761625,-0.171857086551683,
3.55069609938375));
#63021=CARTESIAN_POINT('Ctrl Pts',(-1.49017830179445,-2.63870294144206,
3.70984569777733));
#63022=CARTESIAN_POINT('Ctrl Pts',(1.41515520332815,-2.67968661348843,3.86899529617089));
#63023=CARTESIAN_POINT('Ctrl Pts',(3.01948151949855,-0.25713021233551,4.02814489456448));
#63024=CARTESIAN_POINT('Ctrl Pts',(1.84788109893584,2.40181598703027,4.18729449295804));
#63025=CARTESIAN_POINT('Ctrl Pts',(-1.0225482480068,2.85267938498604,4.34644409135163));
#63026=CARTESIAN_POINT('Ctrl Pts',(-2.95290924134139,0.680963732402603,
4.50559368974519));
#63027=CARTESIAN_POINT('Ctrl Pts',(-2.16854598131273,-2.11678835013076,
4.66474328813878));
#63028=CARTESIAN_POINT('Ctrl Pts',(0.60944589670789,-2.96849461706362,4.82389288653233));
#63029=CARTESIAN_POINT('Ctrl Pts',(2.82715047104436,-1.0911483888671,4.98304248492593));
#63030=CARTESIAN_POINT('Ctrl Pts',(2.44574571817382,1.78933296914758,5.14219208331948));
#63031=CARTESIAN_POINT('Ctrl Pts',(-0.184128146322703,3.02481097231012,
5.30134168171307));
#63032=CARTESIAN_POINT('Ctrl Pts',(-2.64472584833504,1.47946266583818,5.46049128010663));
#63033=CARTESIAN_POINT('Ctrl Pts',(-2.67392427015187,-1.42601318014711,
5.61964087850022));
#63034=CARTESIAN_POINT('Ctrl Pts',(-0.244880167574575,-3.0204996765425,
5.77879047689378));
#63035=CARTESIAN_POINT('Ctrl Pts',(2.40929179222473,-1.83812340510121,5.93794007528737));
#63036=CARTESIAN_POINT('Ctrl Pts',(2.84850815158536,1.03411116559793,6.09708967368094));
#63037=CARTESIAN_POINT('Ctrl Pts',(0.668980237790581,2.9556471429974,6.25623927207451));
#63038=CARTESIAN_POINT('Ctrl Pts',(-2.12556721372019,2.15994180764678,6.41538887046809));
#63039=CARTESIAN_POINT('Ctrl Pts',(-2.96599809897198,-0.621481994395149,
6.57453846886165));
#63040=CARTESIAN_POINT('Ctrl Pts',(-1.07967163527606,-2.83155324026287,
6.73368806725523));
#63041=CARTESIAN_POINT('Ctrl Pts',(1.7992389325566,-2.43846752203824,6.89283766564881));
#63042=CARTESIAN_POINT('Ctrl Pts',(3.02403920828826,0.196396179183931,7.05198726404238));
#63043=CARTESIAN_POINT('Ctrl Pts',(1.46872268705907,2.65070523841879,7.21113686243596));
#63044=CARTESIAN_POINT('Ctrl Pts',(-1.43684769370316,2.66811793171942,7.37028646082953));
#63045=CARTESIAN_POINT('Ctrl Pts',(-3.02146813539374,0.232626093254943,
7.52943605922311));
#63046=CARTESIAN_POINT('Ctrl Pts',(-1.82833546738012,-2.41672795555947,
7.68858565761668));
#63047=CARTESIAN_POINT('Ctrl Pts',(1.04565706826066,-2.84429004991743,7.84773525601024));
#63048=CARTESIAN_POINT('Ctrl Pts',(2.95833641346242,-0.656985735952557,
8.00688485440384));
#63049=CARTESIAN_POINT('Ctrl Pts',(2.15130209503633,2.13431110392909,8.16603445279739));
#63050=CARTESIAN_POINT('Ctrl Pts',(-0.633507866428774,2.96345277938347,
8.32518405119099));
#63051=CARTESIAN_POINT('Ctrl Pts',(-2.83590942008017,1.0681771171315,8.48433364958454));
#63052=CARTESIAN_POINT('Ctrl Pts',(-2.43114920419642,-1.80911529190317,
8.64348324797814));
#63053=CARTESIAN_POINT('Ctrl Pts',(0.20866098060963,-3.02321768776808,8.80263284637168));
#63054=CARTESIAN_POINT('Ctrl Pts',(2.65664101471088,-1.45795854242112,8.96178244476528));
#63055=CARTESIAN_POINT('Ctrl Pts',(2.66226769299254,1.44765856586108,9.12093204315885));
#63056=CARTESIAN_POINT('Ctrl Pts',(0.220368191385691,3.02238688004832,9.28008164155242));
#63057=CARTESIAN_POINT('Ctrl Pts',(-2.4241243548841,1.81851744685623,9.439231239946));
#63058=CARTESIAN_POINT('Ctrl Pts',(-2.84002514927976,-1.05718576604174,
9.59838083833957));
#63059=CARTESIAN_POINT('Ctrl Pts',(-0.644980424297316,-2.96097700847812,
9.75753043673315));
#63060=CARTESIAN_POINT('Ctrl Pts',(2.14301987691753,-2.1426269856415,9.91668003512672));
#63061=CARTESIAN_POINT('Ctrl Pts',(2.96085870016269,0.645523314941969,10.0758296335203));
#63062=CARTESIAN_POINT('Ctrl Pts',(1.05666502356821,2.84021893881974,10.2349792319139));
#63063=CARTESIAN_POINT('Ctrl Pts',(-1.81896188468925,2.42379088506218,10.3941288303075));
#63064=CARTESIAN_POINT('Ctrl Pts',(-3.0223464242644,-0.220922348799343,
10.553278428701));
#63065=CARTESIAN_POINT('Ctrl Pts',(-1.447170409035,-2.66253307954591,10.7124280270946));
#63066=CARTESIAN_POINT('Ctrl Pts',(1.45844561874313,-2.65637365022915,10.8715776254882));
#63067=CARTESIAN_POINT('Ctrl Pts',(3.02325589538921,-0.208106663654035,
11.0307272238817));
#63068=CARTESIAN_POINT('Ctrl Pts',(1.80866950507204,2.43148086850076,11.1898768222753));
#63069=CARTESIAN_POINT('Ctrl Pts',(-1.06869706925202,2.83571351984556,11.3490264206689));
#63070=CARTESIAN_POINT('Ctrl Pts',(-2.96356888459703,0.632964500356112,
11.5081760190625));
#63071=CARTESIAN_POINT('Ctrl Pts',(-2.13391662219954,-2.15169338939434,
11.667325617456));
#63072=CARTESIAN_POINT('Ctrl Pts',(0.657528142236659,-2.95821590399173,
11.8264752158496));
#63073=CARTESIAN_POINT('Ctrl Pts',(2.84448172557426,-1.04513554400223,11.9856248142432));
#63074=CARTESIAN_POINT('Ctrl Pts',(2.41639268570676,1.82877854890243,12.1447744126368));
#63075=CARTESIAN_POINT('Ctrl Pts',(-0.233180082008765,3.02142543211266,
12.3039240110303));
#63076=CARTESIAN_POINT('Ctrl Pts',(-2.66838133597785,1.43635846440497,12.4630736094239));
#63077=CARTESIAN_POINT('Ctrl Pts',(-2.65043590040781,-1.46920867486283,
12.6222232078175));
#63078=CARTESIAN_POINT('Ctrl Pts',(-0.195841711806975,-3.02407516711792,
12.7813728062111));
#63079=CARTESIAN_POINT('Ctrl Pts',(2.43879737536789,-1.79879180406223,12.9405224046046));
#63080=CARTESIAN_POINT('Ctrl Pts',(2.83135523255693,1.08019078848846,13.0996720029982));
#63081=CARTESIAN_POINT('Ctrl Pts',(0.620938161834819,2.96611199917332,13.2588216013918));
#63082=CARTESIAN_POINT('Ctrl Pts',(-2.16033149864856,2.12517114802777,13.4179711997854));
#63083=CARTESIAN_POINT('Ctrl Pts',(-2.95552443435423,-0.669522150789567,
13.5771207981789));
#63084=CARTESIAN_POINT('Ctrl Pts',(-1.03358886813565,-2.84869771020528,
13.7362703965725));
#63085=CARTESIAN_POINT('Ctrl Pts',(1.83856512302265,-2.4089547278576,13.8954199949661));
#63086=CARTESIAN_POINT('Ctrl Pts',(3.02045472646657,0.245433978553323,14.0545695933596));
#63087=CARTESIAN_POINT('Ctrl Pts',(1.42552288642705,2.67418568778151,14.2137191917532));
#63088=CARTESIAN_POINT('Ctrl Pts',(-1.47994755712857,2.64445454122622,14.3728687901468));
#63089=CARTESIAN_POINT('Ctrl Pts',(-3.02484468175446,0.183573537647755,
14.5320183885404));
#63090=CARTESIAN_POINT('Ctrl Pts',(-1.78888450635103,-2.44607375510225,
14.6911679869339));
#63091=CARTESIAN_POINT('Ctrl Pts',(1.09166673463739,-2.82695035912358,14.8503175853276));
#63092=CARTESIAN_POINT('Ctrl Pts',(2.96860631036345,-0.608901606610685,
15.0094671837211));
#63093=CARTESIAN_POINT('Ctrl Pts',(2.11639070702123,2.16893406255168,15.1686167821147));
#63094=CARTESIAN_POINT('Ctrl Pts',(-0.681505143255366,2.95278433553472,
15.3277663805082));
#63095=CARTESIAN_POINT('Ctrl Pts',(-2.85286682334445,1.02202518595354,15.4869159789018));
#63096=CARTESIAN_POINT('Ctrl Pts',(-2.4014771338963,-1.84832144602502,15.6460655772954));
#63097=CARTESIAN_POINT('Ctrl Pts',(0.257683836811684,-3.01943432329778,
15.805215175689));
#63098=CARTESIAN_POINT('Ctrl Pts',(2.67994603945409,-1.41466385338607,15.9643647740825));
#63099=CARTESIAN_POINT('Ctrl Pts',(2.63842967109959,1.49066208884647,16.1235143724761));
#63100=CARTESIAN_POINT('Ctrl Pts',(0.171302343032715,3.02556442663749,16.2826639708697));
#63101=CARTESIAN_POINT('Ctrl Pts',(-2.45330988798075,1.77894777494975,16.4418135692633));
#63102=CARTESIAN_POINT('Ctrl Pts',(-2.82249897202182,-1.10312471887749,
16.6009631676568));
#63103=CARTESIAN_POINT('Ctrl Pts',(-0.596855032729077,-2.97105177712688,
16.7601127660504));
#63104=CARTESIAN_POINT('Ctrl Pts',(2.1775009395601,-2.10757544365029,16.919262364444));
#63105=CARTESIAN_POINT('Ctrl Pts',(2.94999565261784,0.693476922470085,17.0784119628376));
#63106=CARTESIAN_POINT('Ctrl Pts',(1.01044468772068,2.85698899639461,17.2375615612311));
#63107=CARTESIAN_POINT('Ctrl Pts',(-1.85804735738235,2.3939600268566,17.3967111596247));
#63108=CARTESIAN_POINT('Ctrl Pts',(-3.01836423939567,-0.269929455228868,
17.5558607580183));
#63109=CARTESIAN_POINT('Ctrl Pts',(-1.40378154395286,-2.68566229621672,
17.7150103564118));
#63110=CARTESIAN_POINT('Ctrl Pts',(1.50135209372329,-2.63236138915906,17.8741599548054));
#63111=CARTESIAN_POINT('Ctrl Pts',(3.02623438992458,-0.159028329867903,
18.033309553199));
#63112=CARTESIAN_POINT('Ctrl Pts',(1.76898177335394,2.46050565494257,18.1924591515926));
#63113=CARTESIAN_POINT('Ctrl Pts',(-1.1145645526831,2.81800114449322,18.3516087499861));
#63114=CARTESIAN_POINT('Ctrl Pts',(-2.97344835922673,0.584798638400112,
18.5107583483797));
#63115=CARTESIAN_POINT('Ctrl Pts',(-2.09872550295822,-2.18603198871735,
18.6699079467733));
#63116=CARTESIAN_POINT('Ctrl Pts',(0.705437291454138,-2.94715843148763,
18.8290575451669));
#63117=CARTESIAN_POINT('Ctrl Pts',(2.86106416153093,-0.99884756397866,18.9882071435604));
#63118=CARTESIAN_POINT('Ctrl Pts',(2.38640353042244,1.86774269706779,19.147356741954));
#63119=CARTESIAN_POINT('Ctrl Pts',(-0.282170632319641,3.01724449236703,
19.3065063403476));
#63120=CARTESIAN_POINT('Ctrl Pts',(-2.6913343640161,1.39287613718119,19.4656559387412));
#63121=CARTESIAN_POINT('Ctrl Pts',(-2.62624979525007,-1.51201739586941,
19.6248055371347));
#63122=CARTESIAN_POINT('Ctrl Pts',(-0.146751700105655,-3.02685456059239,
19.7839551355284));
#63123=CARTESIAN_POINT('Ctrl Pts',(2.46766093759102,-1.75898666554075,19.9431047339219));
#63124=CARTESIAN_POINT('Ctrl Pts',(2.8134569505435,1.12598604782707,20.1022543323155));
#63125=CARTESIAN_POINT('Ctrl Pts',(0.572732621995603,2.9757960172305,20.261403930709));
#63126=CARTESIAN_POINT('Ctrl Pts',(-2.19452706965651,2.08984103055892,20.4205535291026));
#63127=CARTESIAN_POINT('Ctrl Pts',(-2.94427271882673,-0.717386053415761,
20.5797031274962));
#63128=CARTESIAN_POINT('Ctrl Pts',(-0.987234005542506,-2.86509225170207,
20.7388527258898));
#63129=CARTESIAN_POINT('Ctrl Pts',(1.87740730555765,-2.37880776892575,20.8980023242833));
#63130=CARTESIAN_POINT('Ctrl Pts',(3.01607510063576,0.294407166671968,21.057151922677));
#63131=CARTESIAN_POINT('Ctrl Pts',(1.38194781250485,2.69696214952598,21.2163015210705));
#63132=CARTESIAN_POINT('Ctrl Pts',(-1.52265781980161,2.62009498993066,21.3754511194641));
#63133=CARTESIAN_POINT('Ctrl Pts',(-3.02742492843683,0.134472655741415,
21.5346007178576));
#63134=CARTESIAN_POINT('Ctrl Pts',(-1.74896261596624,-2.47477561819557,
21.6937503162512));
#63135=CARTESIAN_POINT('Ctrl Pts',(1.13738901638409,-2.80886646494126,21.8528999146448));
#63136=CARTESIAN_POINT('Ctrl Pts',(2.97809471251059,-0.560657182045595,
22.0120495130384));
#63137=CARTESIAN_POINT('Ctrl Pts',(2.08092217263444,2.20298604260242,22.1711991114319));
#63138=CARTESIAN_POINT('Ctrl Pts',(-0.729323011754126,2.94133856211567,
22.3303487098256));
#63139=CARTESIAN_POINT('Ctrl Pts',(-2.86907320063122,0.975604203497742,
22.489498308219));
#63140=CARTESIAN_POINT('Ctrl Pts',(-2.37117286734461,-1.88704102383374,
22.6486479066127));
#63141=CARTESIAN_POINT('Ctrl Pts',(0.306638856950085,-3.01485608344266,
22.8077975050062));
#63142=CARTESIAN_POINT('Ctrl Pts',(2.70254556014871,-1.37099674973474,22.9669471033998));
#63143=CARTESIAN_POINT('Ctrl Pts',(2.61389707446989,1.53327319044601,23.1260967017934));
#63144=CARTESIAN_POINT('Ctrl Pts',(0.1221913988104,3.02794548407324,23.2852463001869));
#63145=CARTESIAN_POINT('Ctrl Pts',(-2.48184957969368,1.73890978956272,23.4443958985805));
#63146=CARTESIAN_POINT('Ctrl Pts',(-2.80422976321679,-1.1487732707336,23.6035454969741));
#63147=CARTESIAN_POINT('Ctrl Pts',(-0.548572517235271,-2.98034440724506,
23.7626950953677));
#63148=CARTESIAN_POINT('Ctrl Pts',(2.21140876837405,-2.07196907593263,23.9218446937612));
#63149=CARTESIAN_POINT('Ctrl Pts',(2.93835600963208,0.741247970062597,24.0809942921549));
#63150=CARTESIAN_POINT('Ctrl Pts',(0.963958349197132,2.87300694281721,24.2401438905484));
#63151=CARTESIAN_POINT('Ctrl Pts',(-1.89664369338618,2.36349895130105,24.399293488942));
#63152=CARTESIAN_POINT('Ctrl Pts',(-3.013587460845,-0.318865501897966,24.5584430873356));
#63153=CARTESIAN_POINT('Ctrl Pts',(-1.36002312905589,-2.70808450401678,
24.7175926857291));
#63154=CARTESIAN_POINT('Ctrl Pts',(1.54386333314095,-2.60765615084613,24.8767422841227));
#63155=CARTESIAN_POINT('Ctrl Pts',(3.02841621893663,-0.109908131384133,
25.0358918825163));
#63156=CARTESIAN_POINT('Ctrl Pts',(1.72882835173588,2.48888270569285,25.1950414809098));
#63157=CARTESIAN_POINT('Ctrl Pts',(-1.16013862356305,2.79954692166073,25.3541910793034));
#63158=CARTESIAN_POINT('Ctrl Pts',(-2.98254506441825,0.536478826401498,
25.513340677697));
#63159=CARTESIAN_POINT('Ctrl Pts',(-2.0629818877646,-2.2197951083868,25.6724902760906));
#63160=CARTESIAN_POINT('Ctrl Pts',(0.753160732132038,-2.93532511044979,
25.8316398744841));
#63161=CARTESIAN_POINT('Ctrl Pts',(2.87689341353558,-0.952296634257589,
25.9907894728777));
#63162=CARTESIAN_POINT('Ctrl Pts',(2.35578614705909,1.90621515621594,26.1499390712713));
#63163=CARTESIAN_POINT('Ctrl Pts',(-0.331086900342577,3.01226925371626,
26.3090886696649));
#63164=CARTESIAN_POINT('Ctrl Pts',(-2.71357888999427,1.3490271310245,26.4682382680584));
#63165=CARTESIAN_POINT('Ctrl Pts',(-2.60137232174541,-1.55442807363986,
26.6273878664521));
#63166=CARTESIAN_POINT('Ctrl Pts',(-0.0976230555672867,-3.02883712528166,
26.7865374648456));
#63167=CARTESIAN_POINT('Ctrl Pts',(2.49587488047244,-1.71871846836224,26.9456870632392));
#63168=CARTESIAN_POINT('Ctrl Pts',(2.79481801732299,1.1714848878708,27.1048366616327));
#63169=CARTESIAN_POINT('Ctrl Pts',(0.524376308529718,2.98469664782127,27.2639862600263));
#63170=CARTESIAN_POINT('Ctrl Pts',(-2.22814492465468,2.05396075600249,27.4231358584199));
#63171=CARTESIAN_POINT('Ctrl Pts',(-2.93224591443823,-0.76506110195399,
27.5822854568135));
#63172=CARTESIAN_POINT('Ctrl Pts',(-0.940619250556885,-2.88073254883971,
27.741435055207));
#63173=CARTESIAN_POINT('Ctrl Pts',(1.91575525483747,-2.34803458152248,27.9005846536006));
#63174=CARTESIAN_POINT('Ctrl Pts',(3.01090148374579,0.343302851197289,28.0597342519942));
#63175=CARTESIAN_POINT('Ctrl Pts',(1.33800893656488,2.7190286276785,28.2188838503878));
#63176=CARTESIAN_POINT('Ctrl Pts',(-1.56496723811412,2.59504569055965,28.3780334487813));
#63177=CARTESIAN_POINT('Ctrl Pts',(-3.02920819618289,0.0853363734943193,
28.5371830471749));
#63178=CARTESIAN_POINT('Ctrl Pts',(-1.70858030578638,-2.5028259889856,28.6963326455685));
#63179=CARTESIAN_POINT('Ctrl Pts',(1.1828118769693,-2.79004312801131,28.8554822439621));
#63180=CARTESIAN_POINT('Ctrl Pts',(2.98679912205271,-0.51226516275064,29.0146318423556));
#63181=CARTESIAN_POINT('Ctrl Pts',(2.04490582907692,2.23645807979271,29.1737814407492));
#63182=CARTESIAN_POINT('Ctrl Pts',(-0.776948883723837,2.92911847226141,
29.3329310391428));
#63183=CARTESIAN_POINT('Ctrl Pts',(-2.88452428556178,0.928926390230714,
29.4920806375363));
#63184=CARTESIAN_POINT('Ctrl Pts',(-2.34024438223286,-1.92526383228128,
29.65123023593));
#63185=CARTESIAN_POINT('Ctrl Pts',(0.355513153465022,-3.00948417343838,
29.8103798343235));
#63186=CARTESIAN_POINT('Ctrl Pts',(2.72443362740134,-1.32696872696665,29.9695294327171));
#63187=CARTESIAN_POINT('Ctrl Pts',(2.58867636138508,1.575480653156,30.1286790311106));
#63188=CARTESIAN_POINT('Ctrl Pts',(0.0730482873259879,3.02952942553484,
30.2878286295043));
#63189=CARTESIAN_POINT('Ctrl Pts',(-2.50973591686119,1.69841403081809,30.4469782278978));
#63190=CARTESIAN_POINT('Ctrl Pts',(-2.78522233229009,-1.19411940448822,
30.6061278262914));
#63191=CARTESIAN_POINT('Ctrl Pts',(-0.500145588336814,-2.98885245251919,
30.7652774246849));
#63192=CARTESIAN_POINT('Ctrl Pts',(2.24473443701905,-2.0358172559745,30.9244270230786));
#63193=CARTESIAN_POINT('Ctrl Pts',(2.92594283537721,0.788823881844076,31.0835766214721));
#63194=CARTESIAN_POINT('Ctrl Pts',(0.917218245669399,2.88826856131385,31.2427262198657));
#63195=CARTESIAN_POINT('Ctrl Pts',(-1.93474073209646,2.33241567736749,31.4018758182592));
#63196=CARTESIAN_POINT('Ctrl Pts',(-3.00801734611399,-0.367717606241629,
31.5610254166528));
#63197=CARTESIAN_POINT('Ctrl Pts',(-1.31590668388164,-2.72979380023079,
31.7201750150464));
#63198=CARTESIAN_POINT('Ctrl Pts',(1.58596814578136,-2.58226443902045,31.8793246134399));
#63199=CARTESIAN_POINT('Ctrl Pts',(3.02980080805213,-0.0607589992462767,
32.0384742118336));
#63200=CARTESIAN_POINT('Ctrl Pts',(1.68821981072978,2.51660455040564,32.1976238102271));
#63201=CARTESIAN_POINT('Ctrl Pts',(-1.20540728437737,2.78035570947905,32.3567734086207));
#63202=CARTESIAN_POINT('Ctrl Pts',(-2.99085660543591,0.488017784699585,
32.5159230070143));
#63203=CARTESIAN_POINT('Ctrl Pts',(-2.02669518623548,-2.25297386015744,
32.6750726054078));
#63204=CARTESIAN_POINT('Ctrl Pts',(0.800685900927647,-2.92271905603642,
32.8342222038014));
#63205=CARTESIAN_POINT('Ctrl Pts',(2.89196531448888,-0.905495009514679,
32.993371802195));
#63206=CARTESIAN_POINT('Ctrl Pts',(2.32454859573719,1.94418579835346,33.1525214005885));
#63207=CARTESIAN_POINT('Ctrl Pts',(-0.379916008719381,3.00650102590723,
33.3116709989822));
#63208=CARTESIAN_POINT('Ctrl Pts',(-2.73510905797225,1.30482298932096,33.4708205973757));
#63209=CARTESIAN_POINT('Ctrl Pts',(-2.5758100289656,-1.59642954343275,33.6299701957693));
#63210=CARTESIAN_POINT('Ctrl Pts',(-0.0484687114584423,-3.03002233926915,
33.7891197941628));
#63211=CARTESIAN_POINT('Ctrl Pts',(2.52343177660385,-1.67799781325436,33.9482693925565));
#63212=CARTESIAN_POINT('Ctrl Pts',(2.77544333965369,1.21667533091117,34.10741899095));
#63213=CARTESIAN_POINT('Ctrl Pts',(0.475881951382315,2.99281154782468,34.2665685893436));
#63214=CARTESIAN_POINT('Ctrl Pts',(-2.26117621363277,2.01753976995621,34.4257181877372));
#63215=CARTESIAN_POINT('Ctrl Pts',(-2.91944718729431,-0.812534745810323,
34.5848677861307));
#63216=CARTESIAN_POINT('Ctrl Pts',(-0.893756874633229,-2.89561448424386,
34.7440173845244));
#63217=CARTESIAN_POINT('Ctrl Pts',(1.95359887560164,-2.31664326681841,34.9031669829178));
#63218=CARTESIAN_POINT('Ctrl Pts',(3.00493523785246,0.392108160255101,35.0623165813115));
#63219=CARTESIAN_POINT('Ctrl Pts',(1.29371782548904,2.74037931304599,35.221466179705));
#63220=CARTESIAN_POINT('Ctrl Pts',(-1.60686467367129,2.56931323765636,35.3806157780986));
#63221=CARTESIAN_POINT('Ctrl Pts',(-3.03019401613369,0.0361776257300149,
35.5397653764922));
#63222=CARTESIAN_POINT('Ctrl Pts',(-1.66774820545003,-2.5302174822596,35.6989149748858));
#63223=CARTESIAN_POINT('Ctrl Pts',(1.22792335653137,-2.77048530528777,35.8580645732793));
#63224=CARTESIAN_POINT('Ctrl Pts',(2.99471725163619,-0.463738284920935,
36.0172141716729));
#63225=CARTESIAN_POINT('Ctrl Pts',(2.00835114992269,2.26934135649022,36.1763637700665));
#63226=CARTESIAN_POINT('Ctrl Pts',(-0.824370206550868,2.91612729442474,
36.3355133684601));
#63227=CARTESIAN_POINT('Ctrl Pts',(-2.89921603912457,0.882004012335179,
36.4946629668536));
#63228=CARTESIAN_POINT('Ctrl Pts',(-2.30869976614112,-1.96297976732238,
36.6538125652472));
#63229=CARTESIAN_POINT('Ctrl Pts',(0.404293756186146,-3.00332008715369,
36.8129621636408));
#63230=CARTESIAN_POINT('Ctrl Pts',(2.74560467726245,-1.28259122354491,36.9721117620343));
#63231=CARTESIAN_POINT('Ctrl Pts',(2.56277379323208,1.61727307564432,37.1312613604279));
#63232=CARTESIAN_POINT('Ctrl Pts',(0.0238866669049971,3.03031638748835,
37.2904109588215));
#63233=CARTESIAN_POINT('Ctrl Pts',(-2.53696293435572,1.65747010346212,37.4495605572151));
#63234=CARTESIAN_POINT('Ctrl Pts',(-2.76547905773556,-1.23914916815844,
37.6087101556087));
#63235=CARTESIAN_POINT('Ctrl Pts',(-0.451592003194222,-2.99657751649272,
37.7678597540022));
#63236=CARTESIAN_POINT('Ctrl Pts',(2.27747872810931,-1.99912216839089,37.9270093523958));
#63237=CARTESIAN_POINT('Ctrl Pts',(2.91274116681489,0.836178144068786,38.0861589507893));
#63238=CARTESIAN_POINT('Ctrl Pts',(0.870271463391887,2.90279652361737,38.245308549183));
#63239=CARTESIAN_POINT('Ctrl Pts',(-1.97239480334944,2.30066746816425,38.4044581475765));
#63240=CARTESIAN_POINT('Ctrl Pts',(-3.00152875332717,-0.416375758145608,
38.5636077459701));
#63241=CARTESIAN_POINT('Ctrl Pts',(-1.27168541761539,-2.75096983951106,
38.7227573443637));
#63242=CARTESIAN_POINT('Ctrl Pts',(1.62811677833888,-2.55583908074386,38.8819069427572));
#63243=CARTESIAN_POINT('Ctrl Pts',(3.02950410350625,-0.0122707333053821,
39.0410565411509));
#63244=CARTESIAN_POINT('Ctrl Pts',(1.64888384109211,2.54497064203657,39.2002061395443));
#63245=CARTESIAN_POINT('Ctrl Pts',(-1.25390542022416,2.75780410693846,39.359355737938));
#63246=CARTESIAN_POINT('Ctrl Pts',(-2.41093357184072,1.21637226125721,39.4654554702004));
#63247=CARTESIAN_POINT('Ctrl Pts',(-2.53475666268526,0.371481747533365,
39.5185053363315));
#63248=CARTESIAN_POINT('Ctrl Pts',(1.37702479013085,-1.93106208855777,0.));
#63249=CARTESIAN_POINT('Ctrl Pts',(2.02069053684824,-1.47206923947237,0.0530498661311914));
#63250=CARTESIAN_POINT('Ctrl Pts',(2.80157597434148,0.132344484221863,0.159149598393574));
#63251=CARTESIAN_POINT('Ctrl Pts',(1.39973361494253,2.43361003431117,0.318299196787148));
#63252=CARTESIAN_POINT('Ctrl Pts',(-1.29016829261282,2.49039187166835,0.477448795180722));
#63253=CARTESIAN_POINT('Ctrl Pts',(-2.79332177148693,0.2612514548119,0.636598393574298));
#63254=CARTESIAN_POINT('Ctrl Pts',(-1.72880511791114,-2.20993111510645,
0.79574799196787));
#63255=CARTESIAN_POINT('Ctrl Pts',(0.92524708272242,-2.64846350983462,0.954897590361446));
#63256=CARTESIAN_POINT('Ctrl Pts',(2.72859047663099,-0.652671033011881,
1.11404718875502));
#63257=CARTESIAN_POINT('Ctrl Pts',(2.02348342694992,1.94341489122264,1.27319678714859));
#63258=CARTESIAN_POINT('Ctrl Pts',(-0.541916200030843,2.75270370291815,
1.43234638554217));
#63259=CARTESIAN_POINT('Ctrl Pts',(-2.60909777792823,1.03139851074894,1.59149598393574));
#63260=CARTESIAN_POINT('Ctrl Pts',(-2.27764138013584,-1.63814995877251,
1.75064558232932));
#63261=CARTESIAN_POINT('Ctrl Pts',(0.147742963738231,-2.80166329463351,
1.90979518072289));
#63262=CARTESIAN_POINT('Ctrl Pts',(2.43729952527864,-1.38950924165797,2.06894477911646));
#63263=CARTESIAN_POINT('Ctrl Pts',(2.48615290161395,1.30008022007748,2.22809437751004));
#63264=CARTESIAN_POINT('Ctrl Pts',(0.249388740897356,2.79445248935483,2.38724397590361));
#63265=CARTESIAN_POINT('Ctrl Pts',(-2.21664790546107,1.71977748150848,2.54639357429719));
#63266=CARTESIAN_POINT('Ctrl Pts',(-2.64483411095343,-0.935956616644485,
2.70554317269076));
#63267=CARTESIAN_POINT('Ctrl Pts',(-0.641521429760122,-2.73122899507208,
2.86469277108434));
#63268=CARTESIAN_POINT('Ctrl Pts',(1.95156679945169,-2.01557660741595,3.02384236947791));
#63269=CARTESIAN_POINT('Ctrl Pts',(2.75050382812508,0.553073821547345,3.18299196787149));
#63270=CARTESIAN_POINT('Ctrl Pts',(1.02079575688963,2.61326192654012,3.34214156626506));
#63271=CARTESIAN_POINT('Ctrl Pts',(-1.64736952904253,2.27097678934574,3.50129116465863));
#63272=CARTESIAN_POINT('Ctrl Pts',(-2.80104397213344,-0.15910560602253,
3.66044076305221));
#63273=CARTESIAN_POINT('Ctrl Pts',(-1.37960980571773,-2.44291602421381,
3.81959036144579));
#63274=CARTESIAN_POINT('Ctrl Pts',(1.31015328351832,-2.48085878298404,3.97873995983935));
#63275=CARTESIAN_POINT('Ctrl Pts',(2.79544153036393,-0.238051622317477,
4.13788955823294));
#63276=CARTESIAN_POINT('Ctrl Pts',(1.71077171156123,2.22360564722096,4.2970391566265));
#63277=CARTESIAN_POINT('Ctrl Pts',(-0.946677043995799,2.64101580821315,
4.45618875502009));
#63278=CARTESIAN_POINT('Ctrl Pts',(-2.73380879311094,0.630437472770587,
4.61533835341365));
#63279=CARTESIAN_POINT('Ctrl Pts',(-2.00764384796512,-1.95972653806095,
4.77448795180724));
#63280=CARTESIAN_POINT('Ctrl Pts',(0.564226129275921,-2.74823776254792,
4.9336375502008));
#63281=CARTESIAN_POINT('Ctrl Pts',(2.61738109284993,-1.01018718025988,5.09278714859438));
#63282=CARTESIAN_POINT('Ctrl Pts',(2.26427587290829,1.65656774558932,5.25193674698795));
#63283=CARTESIAN_POINT('Ctrl Pts',(-0.170466175671311,2.80037554755443,
5.41108634538153));
#63284=CARTESIAN_POINT('Ctrl Pts',(-2.4484920424651,1.36968925029025,5.5702359437751));
#63285=CARTESIAN_POINT('Ctrl Pts',(-2.47552399495132,-1.3202056183776,5.72938554216868));
#63286=CARTESIAN_POINT('Ctrl Pts',(-0.226710508403585,-2.79638414202316,
5.88853514056225));
#63287=CARTESIAN_POINT('Ctrl Pts',(2.23052676138529,-1.70173802070743,6.04768473895582));
#63288=CARTESIAN_POINT('Ctrl Pts',(2.63715407267815,0.957382014315266,6.2068343373494));
#63289=CARTESIAN_POINT('Ctrl Pts',(0.619343131473575,2.7363435474871,6.36598393574298));
#63290=CARTESIAN_POINT('Ctrl Pts',(-1.96785402607795,1.99967808819976,6.52513353413654));
#63291=CARTESIAN_POINT('Ctrl Pts',(-2.74592648151851,-0.575369170596496,
6.68428313253012));
#63292=CARTESIAN_POINT('Ctrl Pts',(-0.999561980729776,-2.62145718466985,
6.84343273092369));
#63293=CARTESIAN_POINT('Ctrl Pts',(1.66573870468711,-2.25753770557323,7.00258232931727));
#63294=CARTESIAN_POINT('Ctrl Pts',(2.79966104700711,0.181823943001463,7.16173192771085));
#63295=CARTESIAN_POINT('Ctrl Pts',(1.35974615823274,2.45402777277456,7.32088152610442));
#63296=CARTESIAN_POINT('Ctrl Pts',(-1.33023623090505,2.47014847617812,7.48003112449799));
#63297=CARTESIAN_POINT('Ctrl Pts',(-2.79728074300439,0.21536566391685,7.63918072289157));
#63298=CARTESIAN_POINT('Ctrl Pts',(-1.69267633000806,-2.23741117504315,
7.79833032128514));
#63299=CARTESIAN_POINT('Ctrl Pts',(0.968071232182813,-2.63324894641536,
7.95747991967872));
#63300=CARTESIAN_POINT('Ctrl Pts',(2.73883327901741,-0.608238599666532,
8.11662951807229));
#63301=CARTESIAN_POINT('Ctrl Pts',(1.99167942641439,1.9759491356751,8.27577911646587));
#63302=CARTESIAN_POINT('Ctrl Pts',(-0.586502744988177,2.74357001997377,
8.43492871485943));
#63303=CARTESIAN_POINT('Ctrl Pts',(-2.62549014393666,0.988920334743421,
8.59407831325302));
#63304=CARTESIAN_POINT('Ctrl Pts',(-2.25076239348891,-1.67488225628956,
8.75322791164658));
#63305=CARTESIAN_POINT('Ctrl Pts',(0.19317871866267,-2.79890048180234,8.91237751004016));
#63306=CARTESIAN_POINT('Ctrl Pts',(2.4595231253557,-1.34978069337877,9.07152710843373));
#63307=CARTESIAN_POINT('Ctrl Pts',(2.46473231443179,1.34024495618274,9.23067670682731));
#63308=CARTESIAN_POINT('Ctrl Pts',(0.204017275877662,2.79813131849115,9.38982630522089));
#63309=CARTESIAN_POINT('Ctrl Pts',(-2.2442587751075,1.68358678859467,9.54897590361444));
#63310=CARTESIAN_POINT('Ctrl Pts',(-2.62930049358051,-0.978744521739348,
9.70812550200804));
#63311=CARTESIAN_POINT('Ctrl Pts',(-0.597124060110883,-2.74127794672745,
9.86727510040159));
#63312=CARTESIAN_POINT('Ctrl Pts',(1.98401173368511,-1.98364799422109,10.0264246987952));
#63313=CARTESIAN_POINT('Ctrl Pts',(2.74116841667201,0.597626669265515,10.1855742971888));
#63314=CARTESIAN_POINT('Ctrl Pts',(0.978262417402176,2.6294799042921,10.3447238955823));
#63315=CARTESIAN_POINT('Ctrl Pts',(-1.68399824995572,2.24395004813468,10.5038734939759));
#63316=CARTESIAN_POINT('Ctrl Pts',(-2.79809386445219,-0.204530315827701,
10.6630230923695));
#63317=CARTESIAN_POINT('Ctrl Pts',(-1.33979301969774,-2.46497800978969,
10.8221726907631));
#63318=CARTESIAN_POINT('Ctrl Pts',(1.35023162953112,-2.4592755988281,10.9813222891566));
#63319=CARTESIAN_POINT('Ctrl Pts',(2.79893585448806,-0.192665531008406,
11.1404718875502));
#63320=CARTESIAN_POINT('Ctrl Pts',(1.67446954602361,2.25106944891023,11.2996214859438));
#63321=CARTESIAN_POINT('Ctrl Pts',(-0.989401707370339,2.62530877914012,
11.4587710843374));
#63322=CARTESIAN_POINT('Ctrl Pts',(-2.74367751039345,0.585999695681418,
11.6179206827309));
#63323=CARTESIAN_POINT('Ctrl Pts',(-1.97558392376629,-1.99204168744878,
11.7770702811245));
#63324=CARTESIAN_POINT('Ctrl Pts',(0.608740760399282,-2.7387217111284,11.9362198795181));
#63325=CARTESIAN_POINT('Ctrl Pts',(2.63342640009004,-0.967588404067735,
12.0953694779116));
#63326=CARTESIAN_POINT('Ctrl Pts',(2.23710078159852,1.69308653569416,12.2545190763052));
#63327=CARTESIAN_POINT('Ctrl Pts',(-0.21587854772131,2.79724120822844,12.4136686746988));
#63328=CARTESIAN_POINT('Ctrl Pts',(-2.47039233632374,1.3297833015234,12.5728182730924));
#63329=CARTESIAN_POINT('Ctrl Pts',(-2.45377841914996,-1.36019608663289,
12.7319678714859));
#63330=CARTESIAN_POINT('Ctrl Pts',(-0.181310616086829,-2.79969433775756,
12.8911174698795));
#63331=CARTESIAN_POINT('Ctrl Pts',(2.25784308439087,-1.66532475230686,13.0502670682731));
#63332=CARTESIAN_POINT('Ctrl Pts',(2.62127386877248,1.00004261372609,13.2094166666667));
#63333=CARTESIAN_POINT('Ctrl Pts',(0.574865689414601,2.74603193053384,13.3685662650602));
#63334=CARTESIAN_POINT('Ctrl Pts',(-2.00003886484401,1.96748734773341,13.5277158634538));
#63335=CARTESIAN_POINT('Ctrl Pts',(-2.73622994360017,-0.619844835522055,
13.6868654618474));
#63336=CARTESIAN_POINT('Ctrl Pts',(-0.956898470366649,-2.63732956639619,
13.846015060241));
#63337=CARTESIAN_POINT('Ctrl Pts',(1.70214696396934,-2.23021470657591,14.0051646586345));
#63338=CARTESIAN_POINT('Ctrl Pts',(2.79634252716041,0.227223227623548,14.1643142570281));
#63339=CARTESIAN_POINT('Ctrl Pts',(1.31975170355224,2.47576601587237,14.3234638554217));
#63340=CARTESIAN_POINT('Ctrl Pts',(-1.37013816353632,2.4482408658461,14.4826134538153));
#63341=CARTESIAN_POINT('Ctrl Pts',(-2.80040675581984,0.16995271794274,14.6417630522088));
#63342=CARTESIAN_POINT('Ctrl Pts',(-1.65615255790967,-2.26457957009835,
14.8009126506024));
#63343=CARTESIAN_POINT('Ctrl Pts',(1.01066706572481,-2.61719582886661,14.960062248996));
#63344=CARTESIAN_POINT('Ctrl Pts',(2.74834116840978,-0.563722224505545,
15.1192118473896));
#63345=CARTESIAN_POINT('Ctrl Pts',(1.95935839934075,2.00800313428798,15.2783614457831));
#63346=CARTESIAN_POINT('Ctrl Pts',(-0.630938711931175,2.73369315508602,
15.4375110441767));
#63347=CARTESIAN_POINT('Ctrl Pts',(-2.64118933898918,0.946192792187444,
15.5966606425703));
#63348=CARTESIAN_POINT('Ctrl Pts',(-2.22329193636798,-1.71117938570411,
15.7558102409639));
#63349=CARTESIAN_POINT('Ctrl Pts',(0.238564168873022,-2.7953978360347,15.9149598393574));
#63350=CARTESIAN_POINT('Ctrl Pts',(2.48109896001892,-1.30969839084066,16.074109437751));
#63351=CARTESIAN_POINT('Ctrl Pts',(2.4426630300295,1.38005769665789,16.2332590361446));
#63352=CARTESIAN_POINT('Ctrl Pts',(0.158592023455111,2.80107309695302,16.3924086345381));
#63353=CARTESIAN_POINT('Ctrl Pts',(-2.27127879519284,1.6469531137482,16.5515582329318));
#63354=CARTESIAN_POINT('Ctrl Pts',(-2.61307472652118,-1.02127488855538,
16.7107078313253));
#63355=CARTESIAN_POINT('Ctrl Pts',(-0.552569484305025,-2.75060518602588,
16.8698574297189));
#63356=CARTESIAN_POINT('Ctrl Pts',(2.01593436473937,-1.95119721233924,17.0290070281124));
#63357=CARTESIAN_POINT('Ctrl Pts',(2.73111138732539,0.642022207091869,17.188156626506));
#63358=CARTESIAN_POINT('Ctrl Pts',(0.935471545677604,2.64500565436165,17.3473062248996));
#63359=CARTESIAN_POINT('Ctrl Pts',(-1.72018365228211,2.21633258487957,17.5064558232932));
#63360=CARTESIAN_POINT('Ctrl Pts',(-2.79440715039491,-0.249901184869753,
17.6656054216867));
#63361=CARTESIAN_POINT('Ctrl Pts',(-1.29962352880245,-2.48639108101694,
17.8247550200804));
#63362=CARTESIAN_POINT('Ctrl Pts',(1.38995452278499,-2.43704500347595,17.9839046184738));
#63363=CARTESIAN_POINT('Ctrl Pts',(2.80169335019333,-0.147228719548932,
18.1430542168675));
#63364=CARTESIAN_POINT('Ctrl Pts',(1.63772657118694,2.27794064944762,18.302203815261));
#63365=CARTESIAN_POINT('Ctrl Pts',(-1.0318659076804,2.60891062954338,18.4613534136547));
#63366=CARTESIAN_POINT('Ctrl Pts',(-2.75282394613075,0.541407652316326,
18.6205030120482));
#63367=CARTESIAN_POINT('Ctrl Pts',(-1.94300392101022,-2.02383242570043,
18.7796526104418));
#63368=CARTESIAN_POINT('Ctrl Pts',(0.653095138640082,-2.7284846827978,18.9388022088353));
#63369=CARTESIAN_POINT('Ctrl Pts',(2.64877844972125,-0.924734907240888,
19.0979518072289));
#63370=CARTESIAN_POINT('Ctrl Pts',(2.20933676661749,1.7291596155502,19.2571014056225));
#63371=CARTESIAN_POINT('Ctrl Pts',(-0.261234089078342,2.79337048654149,
19.416251004016));
#63372=CARTESIAN_POINT('Ctrl Pts',(-2.49164229179172,1.28952728320592,19.5754006024097));
#63373=CARTESIAN_POINT('Ctrl Pts',(-2.43138687862253,-1.39982847907868,
19.7345502008032));
#63374=CARTESIAN_POINT('Ctrl Pts',(-0.135862993192047,-2.80226750533537,
19.8936997991968));
#63375=CARTESIAN_POINT('Ctrl Pts',(2.28456502325081,-1.62847308203622,20.0528493975903));
#63376=CARTESIAN_POINT('Ctrl Pts',(2.60470360644785,1.04243994883883,20.211998995984));
#63377=CARTESIAN_POINT('Ctrl Pts',(0.530236912192428,2.75499741221771,20.3711485943775));
#63378=CARTESIAN_POINT('Ctrl Pts',(-2.03169718721918,1.93477866016328,20.5302981927711));
#63379=CARTESIAN_POINT('Ctrl Pts',(-2.72581308472214,-0.664157324385632,
20.6894477911646));
#63380=CARTESIAN_POINT('Ctrl Pts',(-0.91398305353419,-2.65250766299173,
20.8485973895582));
#63381=CARTESIAN_POINT('Ctrl Pts',(1.73810712782103,-2.20230459668849,21.0077469879518));
#63382=CARTESIAN_POINT('Ctrl Pts',(2.79228786153128,0.272562695031161,21.1668965863454));
#63383=CARTESIAN_POINT('Ctrl Pts',(1.2794098201712,2.49685250594164,21.326046184739));
#63384=CARTESIAN_POINT('Ctrl Pts',(-1.40967940307629,2.42568874856607,21.4851957831325));
#63385=CARTESIAN_POINT('Ctrl Pts',(-2.80279555293216,0.12449503139221,21.6443453815261));
#63386=CARTESIAN_POINT('Ctrl Pts',(-1.61919279854979,-2.29115180760726,
21.8034949799196));
#63387=CARTESIAN_POINT('Ctrl Pts',(1.05299683804908,-2.60045372645548,21.9626445783133));
#63388=CARTESIAN_POINT('Ctrl Pts',(2.75712554852525,-0.519057447732828,
22.1217941767068));
#63389=CARTESIAN_POINT('Ctrl Pts',(1.92652156513405,2.03952851989154,22.2809437751004));
#63390=CARTESIAN_POINT('Ctrl Pts',(-0.675208582315117,2.72309663705597,
22.440093373494));
#63391=CARTESIAN_POINT('Ctrl Pts',(-2.65619323281388,0.903216161464837,
22.5992429718876));
#63392=CARTESIAN_POINT('Ctrl Pts',(-2.1952361907975,-1.74702604187528,22.7583925702811));
#63393=CARTESIAN_POINT('Ctrl Pts',(0.283886816331191,-2.79115929317747,
22.9175421686747));
#63394=CARTESIAN_POINT('Ctrl Pts',(2.50202163773962,-1.26927130616756,23.0766917670682));
#63395=CARTESIAN_POINT('Ctrl Pts',(2.41995070706164,1.41950713269408,23.2358413654619));
#63396=CARTESIAN_POINT('Ctrl Pts',(0.113125021193992,2.80327748429537,23.3949909638554));
#63397=CARTESIAN_POINT('Ctrl Pts',(-2.29770089414027,1.60988587342226,23.554140562249));
#63398=CARTESIAN_POINT('Ctrl Pts',(-2.59616105949236,-1.06353640161169,
23.7132901606426));
#63399=CARTESIAN_POINT('Ctrl Pts',(-0.507869442880617,-2.75920832003777,
23.8724397590362));
#63400=CARTESIAN_POINT('Ctrl Pts',(2.04732629486344,-1.91823277178195,24.0315893574297));
#63401=CARTESIAN_POINT('Ctrl Pts',(2.7203353844948,0.686248730594912,24.1907389558233));
#63402=CARTESIAN_POINT('Ctrl Pts',(0.892434408187573,2.6598350985466,24.3498885542168));
#63403=CARTESIAN_POINT('Ctrl Pts',(-1.75591621096422,2.18813166524563,24.5090381526105));
#63404=CARTESIAN_POINT('Ctrl Pts',(-2.78998480004911,-0.295206266655231,
24.668187751004));
#63405=CARTESIAN_POINT('Ctrl Pts',(-1.25911190801061,-2.50714960213454,
24.8273373493976));
#63406=CARTESIAN_POINT('Ctrl Pts',(1.42931150622999,-2.41417284852102,24.9864869477912));
#63407=CARTESIAN_POINT('Ctrl Pts',(2.80371329149552,-0.101753149675579,
25.1456365461847));
#63408=CARTESIAN_POINT('Ctrl Pts',(1.60055245978652,2.30421217509344,25.3047861445783));
#63409=CARTESIAN_POINT('Ctrl Pts',(-1.07405846611233,2.59182567618851,25.4639357429719));
#63410=CARTESIAN_POINT('Ctrl Pts',(-2.76124569248608,0.496673081719335,
25.6230853413655));
#63411=CARTESIAN_POINT('Ctrl Pts',(-1.90991241648788,-2.05509038383302,
25.782234939759));
#63412=CARTESIAN_POINT('Ctrl Pts',(0.697277587574235,-2.71752937247129,
25.9413845381526));
#63413=CARTESIAN_POINT('Ctrl Pts',(2.66343320026788,-0.881637971101683,
26.1005341365462));
#63414=CARTESIAN_POINT('Ctrl Pts',(2.18099113692833,1.76477748881203,26.2596837349398));
#63415=CARTESIAN_POINT('Ctrl Pts',(-0.306520859756921,2.78876440147091,
26.4188333333333));
#63416=CARTESIAN_POINT('Ctrl Pts',(-2.51223631475264,1.24893179285964,26.5779829317269));
#63417=CARTESIAN_POINT('Ctrl Pts',(-2.40835526801112,-1.4390923623662,26.7371325301205));
#63418=CARTESIAN_POINT('Ctrl Pts',(-0.0903796039458558,-2.80410296736195,
26.896282128514));
#63419=CARTESIAN_POINT('Ctrl Pts',(2.3106855433324,-1.59119271121138,27.0554317269076));
#63420=CARTESIAN_POINT('Ctrl Pts',(2.58744764787687,1.08456285842457,27.2145813253012));
#63421=CARTESIAN_POINT('Ctrl Pts',(0.48546854847008,2.76323763234795,27.3737309236948));
#63422=CARTESIAN_POINT('Ctrl Pts',(-2.0628206590526,1.90156063615214,27.5328805220883));
#63423=CARTESIAN_POINT('Ctrl Pts',(-2.71467864715462,-0.708294971788098,
27.6920301204819));
#63424=CARTESIAN_POINT('Ctrl Pts',(-0.870827027847972,-2.66698747877582,
27.8511797188755));
#63425=CARTESIAN_POINT('Ctrl Pts',(1.77360972961834,-2.17381472333333,28.0103293172691));
#63426=CARTESIAN_POINT('Ctrl Pts',(2.7874981175229,0.317830409469884,28.1694789156627));
#63427=CARTESIAN_POINT('Ctrl Pts',(1.23873112821468,2.51728169189892,28.3286285140562));
#63428=CARTESIAN_POINT('Ctrl Pts',(-1.44884954017187,2.40249806125235,28.4877781124498));
#63429=CARTESIAN_POINT('Ctrl Pts',(-2.80444650548309,0.0790045711412627,
28.6469277108434));
#63430=CARTESIAN_POINT('Ctrl Pts',(-1.58180678169894,-2.31712089234655,
28.8060773092369));
#63431=CARTESIAN_POINT('Ctrl Pts',(1.09504940571272,-2.58302704659199,28.9652269076305));
#63432=CARTESIAN_POINT('Ctrl Pts',(2.76518410684866,-0.474256027488414,
29.1243765060241));
#63433=CARTESIAN_POINT('Ctrl Pts',(1.89317756819207,2.07051699333089,29.2835261044177));
#63434=CARTESIAN_POINT('Ctrl Pts',(-0.719300701960229,2.71178325544964,
29.4426757028112));
#63435=CARTESIAN_POINT('Ctrl Pts',(-2.67049787558951,0.860001756306001,
29.6018253012049));
#63436=CARTESIAN_POINT('Ctrl Pts',(-2.16660254253892,-1.78241278806047,
29.7609748995983));
#63437=CARTESIAN_POINT('Ctrl Pts',(0.32913472971066,-2.78618596904008,29.920124497992));
#63438=CARTESIAN_POINT('Ctrl Pts',(2.52228565055847,-1.22851008191401,30.0792740963855));
#63439=CARTESIAN_POINT('Ctrl Pts',(2.39660132461721,1.4585828791058,30.2384236947791));
#63440=CARTESIAN_POINT('Ctrl Pts',(0.067628238422609,2.80474390020647,30.3975732931727));
#63441=CARTESIAN_POINT('Ctrl Pts',(-2.32351811625089,1.572394825682,30.5567228915663));
#63442=CARTESIAN_POINT('Ctrl Pts',(-2.57856394506895,-1.10551793543479,
30.7158724899598));
#63443=CARTESIAN_POINT('Ctrl Pts',(-0.463035703261235,-2.76708508396162,
30.8750220883534));
#63444=CARTESIAN_POINT('Ctrl Pts',(2.07817926003504,-1.88476335053973,31.034171686747));
#63445=CARTESIAN_POINT('Ctrl Pts',(2.70884324499614,0.730294597006095,31.1933212851405));
#63446=CARTESIAN_POINT('Ctrl Pts',(0.849162334591095,2.67396433295012,31.3524708835341));
#63447=CARTESIAN_POINT('Ctrl Pts',(-1.79118651929591,2.15935471321182,31.5116204819277));
#63448=CARTESIAN_POINT('Ctrl Pts',(-2.78482797761209,-0.340433634481819,
31.6707700803213));
#63449=CARTESIAN_POINT('Ctrl Pts',(-1.21826882213122,-2.52724810839787,
31.8299196787149));
#63450=CARTESIAN_POINT('Ctrl Pts',(1.46829221901895,-2.39066515512857,31.9890692771084));
#63451=CARTESIAN_POINT('Ctrl Pts',(2.80499514663885,-0.0562507929721938,
32.148218875502));
#63452=CARTESIAN_POINT('Ctrl Pts',(1.56295699802168,2.32987710978769,32.3073684738957));
#63453=CARTESIAN_POINT('Ctrl Pts',(-1.11596827534518,2.57405841674206,32.4665180722891));
#63454=CARTESIAN_POINT('Ctrl Pts',(-2.76894053240879,0.451807760403934,
32.6256676706828));
#63455=CARTESIAN_POINT('Ctrl Pts',(-1.87631812163978,-2.0858073330928,32.7848172690763));
#63456=CARTESIAN_POINT('Ctrl Pts',(0.741276476036008,-2.70585866416802,
32.9439668674699));
#63457=CARTESIAN_POINT('Ctrl Pts',(2.67738679382172,-0.838308941051334,
33.1031164658635));
#63458=CARTESIAN_POINT('Ctrl Pts',(2.15207135460536,1.79993077896479,33.262266064257));
#63459=CARTESIAN_POINT('Ctrl Pts',(-0.351726937875201,2.78342416558279,
33.4214156626506));
#63460=CARTESIAN_POINT('Ctrl Pts',(-2.5321689837664,1.20800751737253,33.5805652610442));
#63461=CARTESIAN_POINT('Ctrl Pts',(-2.38468965045838,-1.47797740015734,
33.7397148594378));
#63462=CARTESIAN_POINT('Ctrl Pts',(-0.0448724219901618,-2.805200240646,
33.8988644578313));
#63463=CARTESIAN_POINT('Ctrl Pts',(2.33619776832739,-1.55349345400542,34.0580140562249));
#63464=CARTESIAN_POINT('Ctrl Pts',(2.56951053574539,1.1264002534988,34.2171636546184));
#63465=CARTESIAN_POINT('Ctrl Pts',(0.440572383654118,2.77075042165889,34.3763132530121));
#63466=CARTESIAN_POINT('Ctrl Pts',(-2.09340108698849,1.86784202045169,34.5354628514056));
#63467=CARTESIAN_POINT('Ctrl Pts',(-2.70282956208393,-0.752246158366563,
34.6946124497992));
#63468=CARTESIAN_POINT('Ctrl Pts',(-0.827441754243024,-2.68076520187573,
34.8537620481927));
#63469=CARTESIAN_POINT('Ctrl Pts',(1.8086454231506,-2.14475258658905,35.0129116465864));
#63470=CARTESIAN_POINT('Ctrl Pts',(2.78197455612906,0.363014454134983,35.1720612449799));
#63471=CARTESIAN_POINT('Ctrl Pts',(1.19772633632314,2.53704819558261,35.3312108433735));
#63472=CARTESIAN_POINT('Ctrl Pts',(-1.48763826287672,2.37867490914512,35.4903604417671));
#63473=CARTESIAN_POINT('Ctrl Pts',(-2.80535917940216,0.033493312273267,
35.6495100401606));
#63474=CARTESIAN_POINT('Ctrl Pts',(-1.544004348296,-2.3424799870727,35.8086596385542));
#63475=CARTESIAN_POINT('Ctrl Pts',(1.13681369625387,-2.5649203784333,35.9678092369478));
#63476=CARTESIAN_POINT('Ctrl Pts',(2.77251472574384,-0.429329754965117,
36.1269588353414));
#63477=CARTESIAN_POINT('Ctrl Pts',(1.859335179167,2.10096039122589,36.2861084337349));
#63478=CARTESIAN_POINT('Ctrl Pts',(-0.763203449633773,2.69975599917453,
36.4452580321285));
#63479=CARTESIAN_POINT('Ctrl Pts',(-2.68409952799179,0.816560932765415,
36.6044076305221));
#63480=CARTESIAN_POINT('Ctrl Pts',(-2.13739847908868,-1.81733026991608,
36.7635572289156));
#63481=CARTESIAN_POINT('Ctrl Pts',(0.374295901203924,-2.78047924664893,
36.9227068273092));
#63482=CARTESIAN_POINT('Ctrl Pts',(2.54188584736079,-1.18742530783014,37.0818564257028));
#63483=CARTESIAN_POINT('Ctrl Pts',(2.37262067949971,1.49727438051885,37.2410060240964));
#63484=CARTESIAN_POINT('Ctrl Pts',(0.0221143200437823,2.8054724710268,37.40015562249));
#63485=CARTESIAN_POINT('Ctrl Pts',(-2.34872493899865,1.53448886261914,37.5593052208835));
#63486=CARTESIAN_POINT('Ctrl Pts',(-2.56028558526488,-1.14720657325335,
37.7184548192771));
#63487=CARTESIAN_POINT('Ctrl Pts',(-0.41808470505867,-2.7742369623609,37.8776044176707));
#63488=CARTESIAN_POINT('Ctrl Pts',(2.10849398479986,-1.85079097113315,38.0367540160642));
#63489=CARTESIAN_POINT('Ctrl Pts',(2.69662111602106,0.774135259850986,38.1959036144578));
#63490=CARTESIAN_POINT('Ctrl Pts',(0.805698917428903,2.68741434710406,38.3550532128514));
#63491=CARTESIAN_POINT('Ctrl Pts',(-1.82604672754298,2.12996216288546,38.514202811245));
#63492=CARTESIAN_POINT('Ctrl Pts',(-2.77882082650591,-0.38548144078392,
38.6733524096386));
#63493=CARTESIAN_POINT('Ctrl Pts',(-1.17732869269255,-2.54685292441361,
38.8325020080321));
#63494=CARTESIAN_POINT('Ctrl Pts',(1.50731350036759,-2.36620050995552,38.9916516064257));
#63495=CARTESIAN_POINT('Ctrl Pts',(2.80472045702593,-0.0113602674063951,
39.1508012048193));
#63496=CARTESIAN_POINT('Ctrl Pts',(1.52653968516444,2.35613848946071,39.3099508032129));
#63497=CARTESIAN_POINT('Ctrl Pts',(-1.16086793848797,2.55318010173628,39.4691004016064));
#63498=CARTESIAN_POINT('Ctrl Pts',(-2.23204672396583,1.1261196710573,39.5752001338688));
#63499=CARTESIAN_POINT('Ctrl Pts',(-2.34668236863851,0.343918483395665,
39.62825));
#63500=CARTESIAN_POINT('',(1.37702479013102,-1.93106208855765,0.));
#63501=CARTESIAN_POINT('Ctrl Pts',(1.37702479013085,-1.93106208855777,0.));
#63502=CARTESIAN_POINT('Ctrl Pts',(2.02069053684824,-1.47206923947237,0.0530498661311914));
#63503=CARTESIAN_POINT('Ctrl Pts',(2.80157597434148,0.132344484221863,0.159149598393574));
#63504=CARTESIAN_POINT('Ctrl Pts',(1.39973361494253,2.43361003431117,0.318299196787148));
#63505=CARTESIAN_POINT('Ctrl Pts',(-1.29016829261282,2.49039187166835,0.477448795180722));
#63506=CARTESIAN_POINT('Ctrl Pts',(-2.33890237726732,0.935144475115511,
0.588485765616658));
#63507=CARTESIAN_POINT('Ctrl Pts',(-2.37527771381695,0.0747453293793789,
0.646472869921401));
#63508=CARTESIAN_POINT('Ctrl Pts',(-2.37479956011642,0.00144393851757997,
0.651410108094952));
#63509=CARTESIAN_POINT('Ctrl Pts',(1.29201581877684,2.64862154577367,-1.02348685082632E-16));
#63510=CARTESIAN_POINT('Ctrl Pts',(1.34958683951914,2.6139027695176,-1.05335179962833E-16));
#63511=CARTESIAN_POINT('Ctrl Pts',(1.40579757808849,2.57711951310873,-7.026873643365E-17));
#63512=CARTESIAN_POINT('Ctrl Pts',(1.46052207638911,2.53826450414093,-3.81639164714898E-17));
#63513=CARTESIAN_POINT('Ctrl Pts',(1.54016250524111,2.48171890439427,5.08870273341264E-18));
#63514=CARTESIAN_POINT('Ctrl Pts',(1.61665719687035,2.42078661355511,-2.95171646394387E-16));
#63515=CARTESIAN_POINT('Ctrl Pts',(1.68983041078343,2.35584690071589,-3.71230823859037E-16));
#63516=CARTESIAN_POINT('Ctrl Pts',(1.72880905664705,2.32125415927566,-4.11746793905046E-16));
#63517=CARTESIAN_POINT('Ctrl Pts',(1.76684450913562,2.2855237047089,2.98781131615067E-18));
#63518=CARTESIAN_POINT('Ctrl Pts',(1.8039051241343,2.24870979089898,-9.71445146547012E-17));
#63519=CARTESIAN_POINT('Ctrl Pts',(1.83175376478358,2.22104653014029,-1.72387442043738E-16));
#63520=CARTESIAN_POINT('Ctrl Pts',(1.85905188698991,2.19277144505213,-3.58527894598338E-16));
#63521=CARTESIAN_POINT('Ctrl Pts',(1.88578464604575,2.16390703240831,-4.02455846426619E-16));
#63522=CARTESIAN_POINT('Ctrl Pts',(1.89741557092782,2.15134866480683,-4.21568078982574E-16));
#63523=CARTESIAN_POINT('Ctrl Pts',(1.90893301001484,2.13868568977461,-1.74418497724213E-16));
#63524=CARTESIAN_POINT('Ctrl Pts',(1.92033535624658,2.12592108303427,-1.73472347597681E-16));
#63525=CARTESIAN_POINT('Ctrl Pts',(1.98513247700578,2.05338252407569,-1.68095576645527E-16));
#63526=CARTESIAN_POINT('Ctrl Pts',(2.04622485478601,1.97755495337877,1.47867480362913E-16));
#63527=CARTESIAN_POINT('Ctrl Pts',(2.10343517400832,1.89881202362381,1.45716771982052E-16));
#63528=CARTESIAN_POINT('Ctrl Pts',(2.1498698585821,1.83490042244258,1.43971152194695E-16));
#63529=CARTESIAN_POINT('Ctrl Pts',(2.19374640661719,1.76906743351724,1.25074431252417E-16));
#63530=CARTESIAN_POINT('Ctrl Pts',(2.23494640511299,1.70150389183245,9.71445146547012E-17));
#63531=CARTESIAN_POINT('Ctrl Pts',(2.2529714044549,1.67194484234535,8.49251761432007E-17));
#63532=CARTESIAN_POINT('Ctrl Pts',(2.27048380976275,1.64205448628232,-3.94957526722027E-18));
#63533=CARTESIAN_POINT('Ctrl Pts',(2.28747233024776,1.61184859939393,-1.38777878078145E-17));
#63534=CARTESIAN_POINT('Ctrl Pts',(2.29692191410317,1.59504707383844,-1.94001920112555E-17));
#63535=CARTESIAN_POINT('Ctrl Pts',(2.30620939497628,1.57814792321238,-3.53600877506368E-16));
#63536=CARTESIAN_POINT('Ctrl Pts',(2.31533271265734,1.56115385938179,-3.60822483003176E-16));
#63537=CARTESIAN_POINT('Ctrl Pts',(2.32256102651894,1.54768963162543,-3.66544089214901E-16));
#63538=CARTESIAN_POINT('Ctrl Pts',(2.32968598712138,1.53416623918464,-2.42653694158405E-16));
#63539=CARTESIAN_POINT('Ctrl Pts',(2.33670051558313,1.52059718163605,-2.35922392732846E-16));
#63540=CARTESIAN_POINT('Ctrl Pts',(2.38036738874924,1.43612702541826,-1.94018665747421E-16));
#63541=CARTESIAN_POINT('Ctrl Pts',(2.41982387271352,1.34976845265731,1.4715862347523E-16));
#63542=CARTESIAN_POINT('Ctrl Pts',(2.4549039648554,1.26186702602105,1.38777878078145E-16));
#63543=CARTESIAN_POINT('Ctrl Pts',(2.49089795323757,1.17167561727776,1.30178799967504E-16));
#63544=CARTESIAN_POINT('Ctrl Pts',(2.52228513147818,1.07985893523056,-4.56104370496148E-16));
#63545=CARTESIAN_POINT('Ctrl Pts',(2.54882950886302,0.986780146350002,-4.16333634234434E-16));
#63546=CARTESIAN_POINT('Ctrl Pts',(2.57361253388436,0.899877601214398,-3.79201885480213E-16));
#63547=CARTESIAN_POINT('Ctrl Pts',(2.59417381411934,0.811874117600765,2.29384838853516E-16));
#63548=CARTESIAN_POINT('Ctrl Pts',(2.61027212391662,0.72306925843443,2.77555756156289E-16));
#63549=CARTESIAN_POINT('Ctrl Pts',(2.61929903017754,0.673273152551058,3.04566936862236E-16));
#63550=CARTESIAN_POINT('Ctrl Pts',(2.62692179109589,0.623225210006774,3.81625854467562E-16));
#63551=CARTESIAN_POINT('Ctrl Pts',(2.63309089404061,0.572980117688449,4.44089209850063E-16));
#63552=CARTESIAN_POINT('Ctrl Pts',(2.63571616911387,0.551598210205481,4.70670625551379E-16));
#63553=CARTESIAN_POINT('Ctrl Pts',(2.63807868307449,0.530173533712499,-2.82105728213271E-16));
#63554=CARTESIAN_POINT('Ctrl Pts',(2.64017105031311,0.508748320977571,-2.77555756156289E-16));
#63555=CARTESIAN_POINT('Ctrl Pts',(2.64883715014049,0.420010058899969,-2.58710827154487E-16));
#63556=CARTESIAN_POINT('Ctrl Pts',(2.65288772475143,0.331168392804234,-2.63733613808333E-16));
#63557=CARTESIAN_POINT('Ctrl Pts',(2.65213842907589,0.24251346567146,-1.66533453693773E-16));
#63558=CARTESIAN_POINT('Ctrl Pts',(2.65181580925284,0.204341836183571,-1.24682553602233E-16));
#63559=CARTESIAN_POINT('Ctrl Pts',(2.65060272221495,0.166204869721315,2.80550455053001E-16));
#63560=CARTESIAN_POINT('Ctrl Pts',(2.64848147823716,0.128126164156209,2.22044604925031E-16));
#63561=CARTESIAN_POINT('Ctrl Pts',(2.64345202732824,0.0378418864774469,
8.23152144247318E-17));
#63562=CARTESIAN_POINT('Ctrl Pts',(2.63332045212558,-0.052116414540607,
5.07700615603077E-16));
#63563=CARTESIAN_POINT('Ctrl Pts',(2.61828345471384,-0.141416240256498,
4.9960036108132E-16));
#63564=CARTESIAN_POINT('Ctrl Pts',(2.60278436204712,-0.233460299053213,
4.91251181253792E-16));
#63565=CARTESIAN_POINT('Ctrl Pts',(2.58207326188015,-0.324805869332984,
2.73776835990291E-16));
#63566=CARTESIAN_POINT('Ctrl Pts',(2.55631815458934,-0.415057098853101,
3.88578058618805E-16));
#63567=CARTESIAN_POINT('Ctrl Pts',(2.55164298986117,-0.431439844230992,
4.0941721182917E-16));
#63568=CARTESIAN_POINT('Ctrl Pts',(2.54680150944407,-0.447786422521825,
8.02355772890154E-17));
#63569=CARTESIAN_POINT('Ctrl Pts',(2.54179457675504,-0.464094314185775,
8.32667268468867E-17));
#63570=CARTESIAN_POINT('Ctrl Pts',(2.53779818455242,-0.477110812536128,
8.56861047795307E-17));
#63571=CARTESIAN_POINT('Ctrl Pts',(2.53369907715842,-0.490093861130131,
-2.80579978572094E-17));
#63572=CARTESIAN_POINT('Ctrl Pts',(2.52949874656044,-0.503040373434415,
-2.77555756156289E-17));
#63573=CARTESIAN_POINT('Ctrl Pts',(2.50210999497329,-0.587459635478357,
-2.57835956831298E-17));
#63574=CARTESIAN_POINT('Ctrl Pts',(2.47041261765305,-0.670355637708211,
4.53801252951917E-16));
#63575=CARTESIAN_POINT('Ctrl Pts',(2.43461854159303,-0.751424609131643,
4.16333634234434E-16));
#63576=CARTESIAN_POINT('Ctrl Pts',(2.39888342881732,-0.832360036311529,
3.78927735614187E-16));
#63577=CARTESIAN_POINT('Ctrl Pts',(2.35906444173415,-0.911475228111023,
2.85466068417674E-17));
#63578=CARTESIAN_POINT('Ctrl Pts',(2.31533040039922,-0.988437898460195,
0.));
#63579=CARTESIAN_POINT('Ctrl Pts',(2.27229963182651,-1.06416295737186,-2.80875582280819E-17));
#63580=CARTESIAN_POINT('Ctrl Pts',(2.22547803483335,-1.13780478243029,1.26518886312492E-16));
#63581=CARTESIAN_POINT('Ctrl Pts',(2.17499568445539,-1.20900757805061,1.11022302462516E-16));
#63582=CARTESIAN_POINT('Ctrl Pts',(2.15763280136466,-1.23349704430628,1.05692412477636E-16));
#63583=CARTESIAN_POINT('Ctrl Pts',(2.139836646293,-1.25769759925574,2.96543489227423E-16));
#63584=CARTESIAN_POINT('Ctrl Pts',(2.12161186800647,-1.28159346943437,2.77555756156289E-16));
#63585=CARTESIAN_POINT('Ctrl Pts',(2.11095501761041,-1.29556646321094,2.66452771663535E-16));
#63586=CARTESIAN_POINT('Ctrl Pts',(2.10015160389292,-1.30943526383152,1.50560739160337E-16));
#63587=CARTESIAN_POINT('Ctrl Pts',(2.08920251355156,-1.32319660086055,1.66533453693773E-16));
#63588=CARTESIAN_POINT('Ctrl Pts',(2.08026388843326,-1.33443108966228,1.7957326822492E-16));
#63589=CARTESIAN_POINT('Ctrl Pts',(2.07123261909841,-1.34558830018916,4.59673378436067E-16));
#63590=CARTESIAN_POINT('Ctrl Pts',(2.06211416739129,-1.35666111036041,4.44089209850063E-16));
#63591=CARTESIAN_POINT('Ctrl Pts',(2.00790902752559,-1.42248404207256,3.51448258839193E-16));
#63592=CARTESIAN_POINT('Ctrl Pts',(1.95057481796449,-1.48539172201629,-2.78080721237473E-16));
#63593=CARTESIAN_POINT('Ctrl Pts',(1.89026923526248,-1.54508768501287,-1.66533453693773E-16));
#63594=CARTESIAN_POINT('Ctrl Pts',(1.83091398083794,-1.60384292645194,-5.67440088568915E-17));
#63595=CARTESIAN_POINT('Ctrl Pts',(1.76867962675818,-1.65948739321344,3.75307511728794E-17));
#63596=CARTESIAN_POINT('Ctrl Pts',(1.7036906355759,-1.71169599621308,-5.55111512312578E-17));
#63597=CARTESIAN_POINT('Ctrl Pts',(1.64072966331149,-1.76227539967243,-1.45649627458181E-16));
#63598=CARTESIAN_POINT('Ctrl Pts',(1.57518272461921,-1.80963031643797,-6.78657436235449E-19));
#63599=CARTESIAN_POINT('Ctrl Pts',(1.50714729981333,-1.85341941089056,-1.66533453693773E-16));
#63600=CARTESIAN_POINT('Ctrl Pts',(1.46473327304936,-1.8807180105448,-2.6992914479841E-16));
#63601=CARTESIAN_POINT('Ctrl Pts',(1.42135183960329,-1.90662986293965,1.96676586340341E-17));
#63602=CARTESIAN_POINT('Ctrl Pts',(1.37702479013085,-1.93106208855777,0.));
#63603=CARTESIAN_POINT('Ctrl Pts',(0.260722923799077,2.92490787419796,39.0579999999999));
#63604=CARTESIAN_POINT('Ctrl Pts',(0.737297058639913,2.88302734391227,39.0322389374024));
#63605=CARTESIAN_POINT('Ctrl Pts',(1.20411394433562,2.73137775272334,39.0064778748049));
#63606=CARTESIAN_POINT('Ctrl Pts',(1.6022299374267,2.4739167068321,38.9807168122074));
#63607=CARTESIAN_POINT('Ctrl Pts',(2.42207190078732,1.94372607642437,38.9276669460763));
#63608=CARTESIAN_POINT('Ctrl Pts',(2.95057164862713,0.964817205660412,38.8746170799451));
#63609=CARTESIAN_POINT('Ctrl Pts',(2.94659684551607,-0.0114746559244529,
38.8215672138139));
#63610=CARTESIAN_POINT('Ctrl Pts',(2.942622042405,-0.987766517509207,38.7685173476827));
#63611=CARTESIAN_POINT('Ctrl Pts',(2.40617268834321,-1.96144136991487,38.7154674815515));
#63612=CARTESIAN_POINT('Ctrl Pts',(1.58292764435524,-2.48562670401527,38.6624176154203));
#63613=CARTESIAN_POINT('Ctrl Pts',(0.759682600367258,-3.00981203811569,
38.6093677492891));
#63614=CARTESIAN_POINT('Ctrl Pts',(-0.350358133546912,-3.08450785391083,
38.5563178831579));
#63615=CARTESIAN_POINT('Ctrl Pts',(-1.23646945708876,-2.67501588233558,
38.5032680170267));
#63616=CARTESIAN_POINT('Ctrl Pts',(-2.1225807806306,-2.26552391076032,38.4502181508955));
#63617=CARTESIAN_POINT('Ctrl Pts',(-2.78476269380013,-1.37184415181466,
38.3971682847643));
#63618=CARTESIAN_POINT('Ctrl Pts',(-2.91887804171701,-0.404963860410038,
38.3441184186332));
#63619=CARTESIAN_POINT('Ctrl Pts',(-2.93736881665659,-0.271657970073306,
38.3368043181186));
#63620=CARTESIAN_POINT('Ctrl Pts',(-2.94582171308893,-0.13696063005989,
38.3294902176041));
#63621=CARTESIAN_POINT('Ctrl Pts',(-2.94471098031246,-0.00212455505907094,
38.3221761170895));
#63622=CARTESIAN_POINT('Origin',(0.,0.,-1.84858989190508));
#63623=CARTESIAN_POINT('',(-1.37702479013119,-1.93106208855753,0.));
#63624=CARTESIAN_POINT('Ctrl Pts',(-1.3799850048903,-1.93364773575773,4.26633554873046E-16));
#63625=CARTESIAN_POINT('Ctrl Pts',(-0.787715267879867,-2.35133676185328,
0.0488167807402858));
#63626=CARTESIAN_POINT('Ctrl Pts',(0.877861752617119,-2.62654930074856,
0.150487376283488));
#63627=CARTESIAN_POINT('Ctrl Pts',(2.6974957852487,-0.758175742122775,0.305011786629609));
#63628=CARTESIAN_POINT('Ctrl Pts',(2.10214177353418,1.85307404405523,0.463573231038359));
#63629=CARTESIAN_POINT('Ctrl Pts',(-0.413064550041895,2.77131496429985,
0.622134675447112));
#63630=CARTESIAN_POINT('Ctrl Pts',(-2.14343282857647,1.46669785134097,0.750473562402662));
#63631=CARTESIAN_POINT('Ctrl Pts',(-2.36935871427084,0.339352278516582,
0.825958634555295));
#63632=CARTESIAN_POINT('Ctrl Pts',(-2.36820388529326,0.000916507492466252,
0.848589891905012));
#63633=CARTESIAN_POINT('Origin',(0.,0.,0.));
#63634=CARTESIAN_POINT('Ctrl Pts',(-1.03908919352469,2.13201587949063,-0.329233991005398));
#63635=CARTESIAN_POINT('Ctrl Pts',(-1.7471110134088,1.78694442439573,-0.276380176202481));
#63636=CARTESIAN_POINT('Ctrl Pts',(-2.78026471975083,0.342102824634871,
-0.170672546596647));
#63637=CARTESIAN_POINT('Ctrl Pts',(-1.79624709676258,-2.15298261314799,
-0.0121111021878947));
#63638=CARTESIAN_POINT('Ctrl Pts',(0.830322826211876,-2.67536157371565,
0.146450342220856));
#63639=CARTESIAN_POINT('Ctrl Pts',(2.6974957852487,-0.758175742122775,0.305011786629609));
#63640=CARTESIAN_POINT('Ctrl Pts',(2.10214177353418,1.85307404405523,0.463573231038359));
#63641=CARTESIAN_POINT('Ctrl Pts',(-0.413064550041895,2.77131496429985,
0.622134675447112));
#63642=CARTESIAN_POINT('Ctrl Pts',(-2.5509176989363,1.15947323231739,0.780696119855863));
#63643=CARTESIAN_POINT('Ctrl Pts',(-2.35954923822691,-1.51136660104342,
0.939257564264615));
#63644=CARTESIAN_POINT('Ctrl Pts',(-0.0135649315166644,-2.80200471609095,
1.09781900867337));
#63645=CARTESIAN_POINT('Ctrl Pts',(2.34478101694196,-1.53412545281777,1.25638045308212));
#63646=CARTESIAN_POINT('Ctrl Pts',(2.56205685808127,1.13464159452892,1.41494189749087));
#63647=CARTESIAN_POINT('Ctrl Pts',(0.439842266833678,2.76731764321101,1.57350334189962));
#63648=CARTESIAN_POINT('Ctrl Pts',(-2.08400064757574,1.87309085041683,1.73206478630837));
#63649=CARTESIAN_POINT('Ctrl Pts',(-2.70488792678447,-0.73151121296214,
1.89062623071712));
#63650=CARTESIAN_POINT('Ctrl Pts',(-0.855867697802383,-2.66814781527329,
2.04918767512588));
#63651=CARTESIAN_POINT('Ctrl Pts',(1.77466802262196,-2.16842771739956,2.20774911953463));
#63652=CARTESIAN_POINT('Ctrl Pts',(2.78470651107863,0.311343289720562,2.36631056394338));
#63653=CARTESIAN_POINT('Ctrl Pts',(1.25195381897505,2.50681790160282,2.52487200835213));
#63654=CARTESIAN_POINT('Ctrl Pts',(-1.42399178516171,2.41324930660116,2.68343345276089));
#63655=CARTESIAN_POINT('Ctrl Pts',(-2.7996519092107,0.116077212167865,2.84199489716963));
#63656=CARTESIAN_POINT('Ctrl Pts',(-1.61887392550448,-2.28708807616797,
3.00055634157839));
#63657=CARTESIAN_POINT('Ctrl Pts',(1.04014173421655,-2.60185124395797,3.15911778598714));
#63658=CARTESIAN_POINT('Ctrl Pts',(2.74937577244265,-0.540793460784857,
3.31767923039589));
#63659=CARTESIAN_POINT('Ctrl Pts',(1.94808022437453,2.01407749008101,3.47624067480464));
#63660=CARTESIAN_POINT('Ctrl Pts',(-0.632060208719933,2.72983966543523,
3.6348021192134));
#63661=CARTESIAN_POINT('Ctrl Pts',(-2.6350493239968,0.952911204334078,3.79336356362214));
#63662=CARTESIAN_POINT('Ctrl Pts',(-2.23190343620269,-1.69414632007928,
3.95192500803089));
#63663=CARTESIAN_POINT('Ctrl Pts',(0.20925401019493,-2.79423289347191,4.11048645243965));
#63664=CARTESIAN_POINT('Ctrl Pts',(2.45933594484265,-1.34282962940415,4.2690478968484));
#63665=CARTESIAN_POINT('Ctrl Pts',(2.46373152879142,1.33474778785059,4.42760934125715));
#63666=CARTESIAN_POINT('Ctrl Pts',(0.218427035218096,2.79353080054729,4.58617078566591));
#63667=CARTESIAN_POINT('Ctrl Pts',(-2.22632910816719,1.7014650761505,4.74473223007464));
#63668=CARTESIAN_POINT('Ctrl Pts',(-2.63816376282886,-0.94425455451785,
4.90329367448341));
#63669=CARTESIAN_POINT('Ctrl Pts',(-0.641019536282537,-2.72774974243608,
5.06185511889216));
#63670=CARTESIAN_POINT('Ctrl Pts',(1.94145701387202,-2.02046266150336,5.2204165633009));
#63671=CARTESIAN_POINT('Ctrl Pts',(2.75113651059875,0.531763672408809,5.37897800770967));
#63672=CARTESIAN_POINT('Ctrl Pts',(1.04867864620236,2.59842217513736,5.5375394521184));
#63673=CARTESIAN_POINT('Ctrl Pts',(-1.61135613114964,2.29239091820107,5.69610089652718));
#63674=CARTESIAN_POINT('Ctrl Pts',(-2.80001792372147,-0.106884657847206,
5.8546623409359));
#63675=CARTESIAN_POINT('Ctrl Pts',(-1.43190741113937,-2.40856095400742,
6.01322378534467));
#63676=CARTESIAN_POINT('Ctrl Pts',(1.24371659317073,-2.5109149207244,6.17178522975341));
#63677=CARTESIAN_POINT('Ctrl Pts',(2.78366924554423,-0.320484375057478,
6.33034667416217));
#63678=CARTESIAN_POINT('Ctrl Pts',(1.7817780141982,2.16258914529891,6.48890811857092));
#63679=CARTESIAN_POINT('Ctrl Pts',(-0.847103045334166,2.67094386572056,
6.64746956297967));
#63680=CARTESIAN_POINT('Ctrl Pts',(-2.70247133997559,0.740387303953358,
6.80603100738843));
#63681=CARTESIAN_POINT('Ctrl Pts',(-2.09013976063242,-1.86623698502313,
6.96459245179718));
#63682=CARTESIAN_POINT('Ctrl Pts',(0.430755120614024,-2.76874966894979,
7.12315389620592));
#63683=CARTESIAN_POINT('Ctrl Pts',(2.55831581876159,-1.14304193917764,7.28171534061469));
#63684=CARTESIAN_POINT('Ctrl Pts',(2.34980895897243,1.52640838558285,7.44027678502343));
#63685=CARTESIAN_POINT('Ctrl Pts',(-0.00437219018642784,2.80205381589964,
7.59883822943218));
#63686=CARTESIAN_POINT('Ctrl Pts',(-2.35456097390834,1.5190679126993,7.75739967384093));
#63687=CARTESIAN_POINT('Ctrl Pts',(-2.55473627454364,-1.15102010007455,
7.91596111824968));
#63688=CARTESIAN_POINT('Ctrl Pts',(-0.422112596148098,-2.77008044277018,
8.07452256265844));
#63689=CARTESIAN_POINT('Ctrl Pts',(2.09595354186346,-1.85970520609983,8.23308400706718));
#63690=CARTESIAN_POINT('Ctrl Pts',(2.70014765665469,0.748817291137776,8.39164545147595));
#63691=CARTESIAN_POINT('Ctrl Pts',(0.838763715722044,2.67357441123917,8.55020689588469));
#63692=CARTESIAN_POINT('Ctrl Pts',(-1.78851812206262,2.15701822669591,8.70876834029344));
#63693=CARTESIAN_POINT('Ctrl Pts',(-2.78265555637215,-0.32916980091735,
8.8673297847022));
#63694=CARTESIAN_POINT('Ctrl Pts',(-1.23587473403734,-2.51478395593197,
9.02589122911094));
#63695=CARTESIAN_POINT('Ctrl Pts',(1.43941682598108,-2.40408067758287,9.1844526735197));
#63696=CARTESIAN_POINT('Ctrl Pts',(2.8003378439175,-0.0981461317030541,
9.34301411792845));
#63697=CARTESIAN_POINT('Ctrl Pts',(1.60419442889238,2.29740830884616,9.5015755623372));
#63698=CARTESIAN_POINT('Ctrl Pts',(-1.05678242634981,2.59513691480873,9.66013700674596));
#63699=CARTESIAN_POINT('Ctrl Pts',(-2.7527825872023,0.523175621412691,9.8186984511547));
#63700=CARTESIAN_POINT('Ctrl Pts',(-1.93514230974122,-2.02651152088859,
9.97725989556346));
#63701=CARTESIAN_POINT('Ctrl Pts',(0.649528893544149,-2.72573603265175,
10.1358213399722));
#63702=CARTESIAN_POINT('Ctrl Pts',(2.64109764832668,-0.936017048588331,
10.294382784381));
#63703=CARTESIAN_POINT('Ctrl Pts',(2.22100851147896,1.70840448816513,10.4529442287897));
#63704=CARTESIAN_POINT('Ctrl Pts',(-0.22714373294823,2.79283555330906,10.6115056731985));
#63705=CARTESIAN_POINT('Ctrl Pts',(-2.46788487447809,1.32705273051488,10.7700671176072));
#63706=CARTESIAN_POINT('Ctrl Pts',(-2.45513340586504,-1.3504979313758,10.928628562016));
#63707=CARTESIAN_POINT('Ctrl Pts',(-0.200533038930914,-2.79487230540894,
11.0871900064247));
#63708=CARTESIAN_POINT('Ctrl Pts',(2.23717948448735,-1.68717297792302,11.2457514508335));
#63709=CARTESIAN_POINT('Ctrl Pts',(2.63206274630088,0.961129753352717,11.4043128952422));
#63710=CARTESIAN_POINT('Ctrl Pts',(0.623538130558561,2.73179884013891,11.562874339651));
#63711=CARTESIAN_POINT('Ctrl Pts',(-1.95435606311157,2.00798831715321,11.7214357840597));
#63712=CARTESIAN_POINT('Ctrl Pts',(-2.74767473166069,-0.549370796673882,
11.8799972284685));
#63713=CARTESIAN_POINT('Ctrl Pts',(-1.03201708332093,-2.60508453662804,
12.0385586728772));
#63714=CARTESIAN_POINT('Ctrl Pts',(1.6260033530305,-2.28202493395194,12.197120117286));
#63715=CARTESIAN_POINT('Ctrl Pts',(2.7992760290567,0.124813526483961,12.3556815616948));
#63716=CARTESIAN_POINT('Ctrl Pts',(1.41645384406812,2.41768137083226,12.5142430061035));
#63717=CARTESIAN_POINT('Ctrl Pts',(-1.25977076144102,2.50289878578082,12.6728044505123));
#63718=CARTESIAN_POINT('Ctrl Pts',(-2.78566451856249,0.302651438567153,
12.831365894921));
#63719=CARTESIAN_POINT('Ctrl Pts',(-1.76789245405787,-2.17395514538134,
12.9899273393298));
#63720=CARTESIAN_POINT('Ctrl Pts',(0.864190157080086,-2.66546432646371,
13.1484887837385));
#63721=CARTESIAN_POINT('Ctrl Pts',(2.70715729817405,-0.723065741262676,
13.3070502281472));
#63722=CARTESIAN_POINT('Ctrl Pts',(2.07814568976501,1.87958378247841,13.465611672556));
#63723=CARTESIAN_POINT('Ctrl Pts',(-0.448477109148286,2.76593437843611,
13.6241731169647));
#63724=CARTESIAN_POINT('Ctrl Pts',(-2.5655832965958,1.12663527881625,13.7827345613735));
#63725=CARTESIAN_POINT('Ctrl Pts',(-2.33998579499565,-1.54142504925259,
13.9412960057822));
#63726=CARTESIAN_POINT('Ctrl Pts',(0.022316198533973,-2.80196836001547,
14.099857450191));
#63727=CARTESIAN_POINT('Ctrl Pts',(2.36424066594685,-1.50395836934669,14.2584188945997));
#63728=CARTESIAN_POINT('Ctrl Pts',(2.5473128609508,1.16735679707592,14.4169803390085));
#63729=CARTESIAN_POINT('Ctrl Pts',(0.404364597205185,2.77272681232246,14.5755417834172));
#63730=CARTESIAN_POINT('Ctrl Pts',(-2.10781994697999,1.84624477639289,14.734103227826));
#63731=CARTESIAN_POINT('Ctrl Pts',(-2.69529693160535,-0.766093436679547,
14.8926646722347));
#63732=CARTESIAN_POINT('Ctrl Pts',(-0.821625189105414,-2.678890955577,15.0512261166435));
#63733=CARTESIAN_POINT('Ctrl Pts',(1.80229479678065,-2.14552048900545,15.2097875610522));
#63734=CARTESIAN_POINT('Ctrl Pts',(2.78049052387073,0.346982924521951,15.368349005461));
#63735=CARTESIAN_POINT('Ctrl Pts',(1.21974494421116,2.52264681917943,15.5269104498698));
#63736=CARTESIAN_POINT('Ctrl Pts',(-1.45478282458735,2.394813486794,15.6854718942785));
#63737=CARTESIAN_POINT('Ctrl Pts',(-2.80090894123675,0.0802110101217299,
15.8440333386872));
#63738=CARTESIAN_POINT('Ctrl Pts',(-1.58944914047375,-2.30763431528742,
16.002594783096));
#63739=CARTESIAN_POINT('Ctrl Pts',(1.07337977774581,-2.5883161622899,16.1611562275048));
#63740=CARTESIAN_POINT('Ctrl Pts',(2.75607650988087,-0.505536324043674,
16.3197176719135));
#63741=CARTESIAN_POINT('Ctrl Pts',(1.92212503357044,2.03886244228653,16.4782791163223));
#63742=CARTESIAN_POINT('Ctrl Pts',(-0.666970940652513,2.72152061678207,
16.636840560731));
#63743=CARTESIAN_POINT('Ctrl Pts',(-2.64703766011397,0.919084506007508,
16.7954020051398));
#63744=CARTESIAN_POINT('Ctrl Pts',(-2.21002250208375,-1.72259259360078,
16.9539634495485));
#63745=CARTESIAN_POINT('Ctrl Pts',(0.245024140396729,-2.79132367773206,
17.1125248939573));
#63746=CARTESIAN_POINT('Ctrl Pts',(2.47633259500592,-1.31122140851802,17.271086338366));
#63747=CARTESIAN_POINT('Ctrl Pts',(2.44643459674846,1.3661926903175,17.4296477827748));
#63748=CARTESIAN_POINT('Ctrl Pts',(0.182630818693805,2.79609919124984,17.5882092271835));
#63749=CARTESIAN_POINT('Ctrl Pts',(-2.24793811302219,1.67281168792754,17.7467706715923));
#63750=CARTESIAN_POINT('Ctrl Pts',(-2.62585378763459,-0.977965535798613,
17.905332116001));
#63751=CARTESIAN_POINT('Ctrl Pts',(-0.606031153241877,-2.7357359054823,
18.0638935604098));
#63752=CARTESIAN_POINT('Ctrl Pts',(1.96717496328582,-1.9954316242523,18.2224550048186));
#63753=CARTESIAN_POINT('Ctrl Pts',(2.7441002692833,0.566955390982473,18.3810164492273));
#63754=CARTESIAN_POINT('Ctrl Pts',(1.01531319693132,2.61164006237112,18.5395778936361));
#63755=CARTESIAN_POINT('Ctrl Pts',(-1.64058389174553,2.27156536278176,18.6981393380448));
#63756=CARTESIAN_POINT('Ctrl Pts',(-2.79841933475915,-0.142737276458901,
18.8567007824536));
#63757=CARTESIAN_POINT('Ctrl Pts',(-1.40094218755544,-2.42670263740165,
19.0152622268623));
#63758=CARTESIAN_POINT('Ctrl Pts',(1.27577326591705,-2.49478000577529,19.1738236712711));
#63759=CARTESIAN_POINT('Ctrl Pts',(2.7875455501625,-0.284806090198347,19.3323851156798));
#63760=CARTESIAN_POINT('Ctrl Pts',(1.75393439181258,2.18523199053596,19.4909465600886));
#63761=CARTESIAN_POINT('Ctrl Pts',(-0.88124182797927,2.65987547525528,19.6495080044973));
#63762=CARTESIAN_POINT('Ctrl Pts',(-2.71173223457244,0.705714525304297,
19.8080694489061));
#63763=CARTESIAN_POINT('Ctrl Pts',(-2.06606639316088,-1.89285349731455,
19.9666308933148));
#63764=CARTESIAN_POINT('Ctrl Pts',(0.466180705424317,-2.76300565564655,
20.1251923377236));
#63765=CARTESIAN_POINT('Ctrl Pts',(2.57274555864665,-1.11018241460974,20.2837537821323));
#63766=CARTESIAN_POINT('Ctrl Pts',(2.33006666709568,1.55637849835264,20.4423152265411));
#63767=CARTESIAN_POINT('Ctrl Pts',(-0.0402592916836527,2.80176799408478,
20.6008766709498));
#63768=CARTESIAN_POINT('Ctrl Pts',(-2.37382339935842,1.48878714795069,20.7594381153585));
#63769=CARTESIAN_POINT('Ctrl Pts',(-2.53978498085384,-1.18364562022337,
20.9179995597673));
#63770=CARTESIAN_POINT('Ctrl Pts',(-0.386600015079116,-2.7752594710379,
21.0765610041761));
#63771=CARTESIAN_POINT('Ctrl Pts',(2.11959990940443,-1.83270863131529,21.2351224485848));
#63772=CARTESIAN_POINT('Ctrl Pts',(2.69033567115523,0.783338164367446,21.3936838929936));
#63773=CARTESIAN_POINT('Ctrl Pts',(0.804452967251542,2.68409763733083,21.5522453374023));
#63774=CARTESIAN_POINT('Ctrl Pts',(-1.81599755853736,2.13393476250589,21.7108067818111));
#63775=CARTESIAN_POINT('Ctrl Pts',(-2.77821146213903,-0.364781818192803,
21.8693682262198));
#63776=CARTESIAN_POINT('Ctrl Pts',(-1.20356513206848,-2.53040622748872,
22.0279296706286));
#63777=CARTESIAN_POINT('Ctrl Pts',(1.47008916186248,-2.38544808357241,22.1864911150373));
#63778=CARTESIAN_POINT('Ctrl Pts',(2.80136517195679,-0.0622725990490076,
22.3450525594461));
#63779=CARTESIAN_POINT('Ctrl Pts',(1.5746386679948,2.31776568455491,22.5036140038548));
#63780=CARTESIAN_POINT('Ctrl Pts',(-1.08993310932985,2.58138926170217,22.6621754482636));
#63781=CARTESIAN_POINT('Ctrl Pts',(-2.7592574045594,0.487876294391167,22.8207368926723));
#63782=CARTESIAN_POINT('Ctrl Pts',(-1.90902893014377,-2.05112974897222,
22.9792983370811));
#63783=CARTESIAN_POINT('Ctrl Pts',(0.684385634967381,-2.71719359006588,
23.1378597814898));
#63784=CARTESIAN_POINT('Ctrl Pts',(2.65286911563599,-0.902114271336809,
23.2964212258986));
#63785=CARTESIAN_POINT('Ctrl Pts',(2.19894585862139,1.73671005470014,23.4549826703074));
#63786=CARTESIAN_POINT('Ctrl Pts',(-0.262894499289412,2.789697328652,23.6135441147161));
#63787=CARTESIAN_POINT('Ctrl Pts',(-2.48467875996383,1.29533631271162,23.7721055591249));
#63788=CARTESIAN_POINT('Ctrl Pts',(-2.43763545819304,-1.38183142105133,
23.9306670035336));
#63789=CARTESIAN_POINT('Ctrl Pts',(-0.164721108680563,-2.79721140774162,
24.0892284479423));
#63790=CARTESIAN_POINT('Ctrl Pts',(2.25860455255274,-1.6583817951343,24.2477898923511));
#63791=CARTESIAN_POINT('Ctrl Pts',(2.61953714146364,0.99476121141571,24.4063513367598));
#63792=CARTESIAN_POINT('Ctrl Pts',(0.588499322301271,2.73956077700343,24.5649127811686));
#63793=CARTESIAN_POINT('Ctrl Pts',(-1.9799131886852,1.98279309775759,24.7234742255773));
#63794=CARTESIAN_POINT('Ctrl Pts',(-2.74041327005717,-0.584516734182513,
24.8820356699861));
#63795=CARTESIAN_POINT('Ctrl Pts',(-0.998567672067767,-2.61808848352113,
25.0405971143948));
#63796=CARTESIAN_POINT('Ctrl Pts',(1.65509714933991,-2.26101263364264,25.1991585588037));
#63797=CARTESIAN_POINT('Ctrl Pts',(2.79744787596231,0.16065517271071,25.3577200032123));
#63798=CARTESIAN_POINT('Ctrl Pts',(1.3853730777416,2.43562438374916,25.5162814476211));
#63799=CARTESIAN_POINT('Ctrl Pts',(-1.29172345032858,2.48655891366281,25.6748428920299));
#63800=CARTESIAN_POINT('Ctrl Pts',(-2.78931226320224,0.266949061797221,
25.8334043364386));
#63801=CARTESIAN_POINT('Ctrl Pts',(-1.7399043998891,-2.19641921829403,25.9919657808474));
#63802=CARTESIAN_POINT('Ctrl Pts',(0.898257358734679,-2.65417754129669,
26.1505272252561));
#63803=CARTESIAN_POINT('Ctrl Pts',(2.71619596155049,-0.688334367659731,
26.3090886696649));
#63804=CARTESIAN_POINT('Ctrl Pts',(2.05390236619762,1.90604558533434,26.4676501140736));
#63805=CARTESIAN_POINT('Ctrl Pts',(-0.483865183409376,2.7599636206894,26.6262115584824));
#63806=CARTESIAN_POINT('Ctrl Pts',(-2.57980231118642,1.09368402129775,26.7847730028911));
#63807=CARTESIAN_POINT('Ctrl Pts',(-2.32005198206061,-1.57126811963504,
26.9433344472999));
#63808=CARTESIAN_POINT('Ctrl Pts',(0.0582007337807619,-2.8014527263247,
27.1018958917086));
#63809=CARTESIAN_POINT('Ctrl Pts',(2.38330878115067,-1.47355487069022,27.2604573361174));
#63810=CARTESIAN_POINT('Ctrl Pts',(2.53215294297463,1.19988590150465,27.4190187805261));
#63811=CARTESIAN_POINT('Ctrl Pts',(0.368819578303693,2.77767831505101,27.5775802249349));
#63812=CARTESIAN_POINT('Ctrl Pts',(-2.13129294603499,1.81909732599064,27.7361416693437));
#63813=CARTESIAN_POINT('Ctrl Pts',(-2.6852640787679,-0.80055076698708,27.8947031137524));
#63814=CARTESIAN_POINT('Ctrl Pts',(-0.787247754401329,-2.68919424297219,
28.0532645581612));
#63815=CARTESIAN_POINT('Ctrl Pts',(1.82962584537607,-2.12226152233333,28.2118260025699));
#63816=CARTESIAN_POINT('Ctrl Pts',(2.77581846464243,0.382565751988956,28.3703874469787));
#63817=CARTESIAN_POINT('Ctrl Pts',(1.18733596115095,2.53806186264293,28.5289488913874));
#63818=CARTESIAN_POINT('Ctrl Pts',(-1.48533521008643,2.37598485199765,28.6875103357962));
#63819=CARTESIAN_POINT('Ctrl Pts',(-2.80170651736734,0.0443316341475483,
28.8460717802049));
#63820=CARTESIAN_POINT('Ctrl Pts',(-1.55976361883997,-2.32780200115644,
29.0046332246137));
#63821=CARTESIAN_POINT('Ctrl Pts',(1.10644174224207,-2.57435649712099,29.1631946690224));
#63822=CARTESIAN_POINT('Ctrl Pts',(2.7623251407879,-0.470196256701246,29.3217561134311));
#63823=CARTESIAN_POINT('Ctrl Pts',(1.89585453653854,2.06331293785769,29.4803175578399));
#63824=CARTESIAN_POINT('Ctrl Pts',(-0.701772262303996,2.71275512995654,
29.6388790022487));
#63825=CARTESIAN_POINT('Ctrl Pts',(-2.65859177574196,0.885107040533527,
29.7974404466574));
#63826=CARTESIAN_POINT('Ctrl Pts',(-2.18777903535026,-1.7507562924995,29.9560018910662));
#63827=CARTESIAN_POINT('Ctrl Pts',(0.28075407675448,-2.78795657276624,30.1145633354749));
#63828=CARTESIAN_POINT('Ctrl Pts',(2.49292302707169,-1.27939809455089,30.2731247798837));
#63829=CARTESIAN_POINT('Ctrl Pts',(2.42873635105556,1.39741348222569,30.4316862242924));
#63830=CARTESIAN_POINT('Ctrl Pts',(0.146804643376738,2.79820890927176,30.5902476687012));
#63831=CARTESIAN_POINT('Ctrl Pts',(-2.26917836564331,1.64388389131991,30.7488091131099));
#63832=CARTESIAN_POINT('Ctrl Pts',(-2.61311306683666,-1.01151609140548,
30.9073705575187));
#63833=CARTESIAN_POINT('Ctrl Pts',(-0.570943356725327,-2.74327329784255,
31.0659320019274));
#63834=CARTESIAN_POINT('Ctrl Pts',(1.99257021690915,-1.97007325598095,31.2244934463362));
#63835=CARTESIAN_POINT('Ctrl Pts',(2.73661388518784,0.602054106075114,31.3830548907449));
#63836=CARTESIAN_POINT('Ctrl Pts',(0.981781195472087,2.62442953562526,31.5416163351537));
#63837=CARTESIAN_POINT('Ctrl Pts',(-1.6695425306181,2.25036717930698,31.7001777795624));
#63838=CARTESIAN_POINT('Ctrl Pts',(-2.79636169250615,-0.178566480417973,
31.8587392239712));
#63839=CARTESIAN_POINT('Ctrl Pts',(-1.3697471531232,-2.44444624398976,32.0173006683799));
#63840=CARTESIAN_POINT('Ctrl Pts',(1.30762066055104,-2.47823584659426,32.1758621127887));
#63841=CARTESIAN_POINT('Ctrl Pts',(2.79096458522799,-0.249081085688892,
32.3344235571974));
#63842=CARTESIAN_POINT('Ctrl Pts',(1.72580305366397,2.20751636986205,32.4929850016062));
#63843=CARTESIAN_POINT('Ctrl Pts',(-0.915236051531332,2.64837075826291,
32.6515464460149));
#63844=CARTESIAN_POINT('Ctrl Pts',(-2.72054829604864,0.670925981097476,
32.8101078904237));
#63845=CARTESIAN_POINT('Ctrl Pts',(-2.04165410772776,-1.91915950552399,
32.9686693348324));
#63846=CARTESIAN_POINT('Ctrl Pts',(0.5015298178546,-2.75680839831995,33.1272307792412));
#63847=CARTESIAN_POINT('Ctrl Pts',(2.58675326481436,-1.07714077548725,33.2857922236499));
#63848=CARTESIAN_POINT('Ctrl Pts',(2.30994215059737,1.58609330246939,33.4443536680588));
#63849=CARTESIAN_POINT('Ctrl Pts',(-0.076139789038159,2.80102256966442,
33.6029151124674));
#63850=CARTESIAN_POINT('Ctrl Pts',(-2.39269642232381,1.45826216224833,33.7614765568762));
#63851=CARTESIAN_POINT('Ctrl Pts',(-2.52441706030621,-1.21607697489841,
33.920038001285));
#63852=CARTESIAN_POINT('Ctrl Pts',(-0.351024016063958,-2.77998324516326,
34.0785994456937));
#63853=CARTESIAN_POINT('Ctrl Pts',(2.14289857733639,-1.80541141862616,34.2371608901025));
#63854=CARTESIAN_POINT('Ctrl Pts',(2.68008236242858,0.817730538643591,34.3957223345112));
#63855=CARTESIAN_POINT('Ctrl Pts',(0.770010256154827,2.69418056348283,34.55428377892));
#63856=CARTESIAN_POINT('Ctrl Pts',(-1.84317909840598,2.11050124722063,34.7128452233287));
#63857=CARTESIAN_POINT('Ctrl Pts',(-2.7733116294966,-0.400333996597624,
34.8714066677375));
#63858=CARTESIAN_POINT('Ctrl Pts',(-1.17105809706712,-2.54561341065258,
35.0299681121462));
#63859=CARTESIAN_POINT('Ctrl Pts',(1.50052034409269,-2.36642418021518,35.188529556555));
#63860=CARTESIAN_POINT('Ctrl Pts',(2.80193296331482,-0.0263888510821259,
35.3470910009637));
#63861=CARTESIAN_POINT('Ctrl Pts',(1.54482460333755,2.33774285330196,35.5056524453724));
#63862=CARTESIAN_POINT('Ctrl Pts',(-1.12290500001934,2.56721815733726,35.6642138897812));
#63863=CARTESIAN_POINT('Ctrl Pts',(-2.76527959168139,0.452496935327245,
35.8227753341899));
#63864=CARTESIAN_POINT('Ctrl Pts',(-1.88260239509527,-2.0754115079434,35.9813367785987));
#63865=CARTESIAN_POINT('Ctrl Pts',(0.719130113544572,-2.70820542107464,
36.1398982230075));
#63866=CARTESIAN_POINT('Ctrl Pts',(2.66420539827102,-0.86806350611665,36.2984596674162));
#63867=CARTESIAN_POINT('Ctrl Pts',(2.17652250448365,1.76473072150059,36.457021111825));
#63868=CARTESIAN_POINT('Ctrl Pts',(-0.298602167564159,2.78610149950517,
36.6155825562337));
#63869=CARTESIAN_POINT('Ctrl Pts',(-2.50106500632603,1.26340737324662,36.7741440006425));
#63870=CARTESIAN_POINT('Ctrl Pts',(-2.41973773932351,-1.41293816913244,
36.9327054450512));
#63871=CARTESIAN_POINT('Ctrl Pts',(-0.128881968591299,-2.79909178025225,
37.09126688946));
#63872=CARTESIAN_POINT('Ctrl Pts',(2.27965875812724,-1.62931833193606,37.2498283338687));
#63873=CARTESIAN_POINT('Ctrl Pts',(2.60658251510917,1.02822903240515,37.4083897782775));
#63874=CARTESIAN_POINT('Ctrl Pts',(0.553362663956598,2.74687418626157,37.5669512226862));
#63875=CARTESIAN_POINT('Ctrl Pts',(-2.00514302452926,1.95727095960215,37.725512667095));
#63876=CARTESIAN_POINT('Ctrl Pts',(-2.732707048879,-0.619563618269777,37.8840741115037));
#63877=CARTESIAN_POINT('Ctrl Pts',(-0.964945338256294,-2.63066900551404,
38.0426355559125));
#63878=CARTESIAN_POINT('Ctrl Pts',(1.68390204706478,-2.23961789871709,38.2011970003212));
#63879=CARTESIAN_POINT('Ctrl Pts',(2.79519402126786,0.196448450834139,38.35975844473));
#63880=CARTESIAN_POINT('Ctrl Pts',(1.35400172213932,2.45320986049924,38.5183198891387));
#63881=CARTESIAN_POINT('Ctrl Pts',(-1.3233434007851,2.46973099698168,38.6768813335475));
#63882=CARTESIAN_POINT('Ctrl Pts',(-2.79273305520996,0.231355853883896,
38.8354427779563));
#63883=CARTESIAN_POINT('Ctrl Pts',(-1.71119063643581,-2.21881512820523,
38.994004222365));
#63884=CARTESIAN_POINT('Ctrl Pts',(0.931334562612731,-2.64189543289012,
39.1525656667738));
#63885=CARTESIAN_POINT('Ctrl Pts',(2.72641926444476,-0.654580598253606,
39.3111271111825));
#63886=CARTESIAN_POINT('Ctrl Pts',(2.02601511878175,1.93446865908499,39.4696885555913));
#63887=CARTESIAN_POINT('Ctrl Pts',(0.334552217316969,2.47661908313362,39.5753961851971));
#63888=CARTESIAN_POINT('Ctrl Pts',(-0.439445221993938,2.33068358199192,
39.62825));
#63889=CARTESIAN_POINT('Ctrl Pts',(-1.12236674703412,2.30288577939285,-0.219489327336937));
#63890=CARTESIAN_POINT('Ctrl Pts',(-1.88713280539037,1.9301586555206,-0.16663551253402));
#63891=CARTESIAN_POINT('Ctrl Pts',(-3.00308836704896,0.369520573237848,
-0.060927882928185));
#63892=CARTESIAN_POINT('Ctrl Pts',(-1.94020688832694,-2.32553288687669,
0.0976335614805664));
#63893=CARTESIAN_POINT('Ctrl Pts',(0.896868849422307,-2.88977778360442,
0.256195005889318));
#63894=CARTESIAN_POINT('Ctrl Pts',(2.91368593619747,-0.818939554630395,
0.41475645029807));
#63895=CARTESIAN_POINT('Ctrl Pts',(2.27061742039935,2.00158821764338,0.573317894706821));
#63896=CARTESIAN_POINT('Ctrl Pts',(-0.4461695090612,2.99342133559979,0.731879339115573));
#63897=CARTESIAN_POINT('Ctrl Pts',(-2.75536038441027,1.25239893566279,0.890440783524324));
#63898=CARTESIAN_POINT('Ctrl Pts',(-2.54865474444223,-1.63249471379359,
1.04900222793308));
#63899=CARTESIAN_POINT('Ctrl Pts',(-0.0146520896905362,-3.02657071016718,
1.20756367234183));
#63900=CARTESIAN_POINT('Ctrl Pts',(2.53270292761432,-1.65707756826962,1.36612511675058));
#63901=CARTESIAN_POINT('Ctrl Pts',(2.76739228878582,1.22557717223607,1.52468656115933));
#63902=CARTESIAN_POINT('Ctrl Pts',(0.475093319524896,2.98910365017368,1.68324800556808));
#63903=CARTESIAN_POINT('Ctrl Pts',(-2.25102237826412,2.02320926613654,1.84180944997683));
#63904=CARTESIAN_POINT('Ctrl Pts',(-2.92167051913873,-0.790138003193314,
2.00037089438559));
#63905=CARTESIAN_POINT('Ctrl Pts',(-0.924461008602584,-2.88198588022671,
2.15893233879434));
#63906=CARTESIAN_POINT('Ctrl Pts',(1.91689836447934,-2.34221583529375,2.31749378320309));
#63907=CARTESIAN_POINT('Ctrl Pts',(3.00788614467443,0.33629582279584,2.47605522761184));
#63908=CARTESIAN_POINT('Ctrl Pts',(1.35229135669612,2.70772621942572,2.63461667202059));
#63909=CARTESIAN_POINT('Ctrl Pts',(-1.53811726430708,2.60665859188122,2.79317811642934));
#63910=CARTESIAN_POINT('Ctrl Pts',(-3.02402933814537,0.12538019241986,2.9517395608381));
#63911=CARTESIAN_POINT('Ctrl Pts',(-1.74861818691741,-2.47038619997742,
3.11030100524684));
#63912=CARTESIAN_POINT('Ctrl Pts',(1.12350364334661,-2.81037598614788,3.26886244965561));
#63913=CARTESIAN_POINT('Ctrl Pts',(2.9697238324877,-0.584135222636071,3.42742389406434));
#63914=CARTESIAN_POINT('Ctrl Pts',(2.10420864543479,2.17549524612882,3.58598533847311));
#63915=CARTESIAN_POINT('Ctrl Pts',(-0.682716522134537,2.94862200888265,
3.74454678288185));
#63916=CARTESIAN_POINT('Ctrl Pts',(-2.84623471832721,1.02928204362586,3.90310822729061));
#63917=CARTESIAN_POINT('Ctrl Pts',(-2.41077880031416,-1.82992326945222,
4.06166967169936));
#63918=CARTESIAN_POINT('Ctrl Pts',(0.226024622515564,-3.01817601669349,
4.22023111610811));
#63919=CARTESIAN_POINT('Ctrl Pts',(2.65643883266062,-1.45045038709602,4.37879256051686));
#63920=CARTESIAN_POINT('Ctrl Pts',(2.66118669962771,1.44172082829505,4.53735400492561));
#63921=CARTESIAN_POINT('Ctrl Pts',(0.235932817422852,3.01741765470029,4.69591544933437));
#63922=CARTESIAN_POINT('Ctrl Pts',(-2.40475771909903,1.83782858546841,4.85447689374311));
#63923=CARTESIAN_POINT('Ctrl Pts',(-2.84959876311035,-1.01993160869226,
5.01303833815187));
#63924=CARTESIAN_POINT('Ctrl Pts',(-0.692393892849685,-2.94636458950742,
5.17159978256062));
#63925=CARTESIAN_POINT('Ctrl Pts',(2.09705461931962,-2.18239215557902,5.33016122696938));
#63926=CARTESIAN_POINT('Ctrl Pts',(2.97162568457982,0.574381744042531,5.48872267137811));
#63927=CARTESIAN_POINT('Ctrl Pts',(1.13272474409016,2.80667209543142,5.64728411578688));
#63928=CARTESIAN_POINT('Ctrl Pts',(-1.74049788074223,2.47611403700979,5.80584556019562));
#63929=CARTESIAN_POINT('Ctrl Pts',(-3.02442468680107,-0.115450903044226,
5.96440700460438));
#63930=CARTESIAN_POINT('Ctrl Pts',(-1.5466672862248,-2.60159449239653,6.12296844901313));
#63931=CARTESIAN_POINT('Ctrl Pts',(1.34339396041099,-2.71215159315935,6.28152989342187));
#63932=CARTESIAN_POINT('Ctrl Pts',(3.00676574774326,-0.346169518218407,
6.44009133783064));
#63933=CARTESIAN_POINT('Ctrl Pts',(1.92457818462032,2.33590933223643,6.59865278223937));
#63934=CARTESIAN_POINT('Ctrl Pts',(-0.914993915170435,2.88500601946456,
6.75721422664814));
#63935=CARTESIAN_POINT('Ctrl Pts',(-2.9190602555613,0.799725466362086,6.91577567105688));
#63936=CARTESIAN_POINT('Ctrl Pts',(-2.25765350906011,-2.01580609934939,
7.07433711546564));
#63937=CARTESIAN_POINT('Ctrl Pts',(0.46527788615717,-2.99065044527086,7.23289855987439));
#63938=CARTESIAN_POINT('Ctrl Pts',(2.76335142476968,-1.23465076048616,7.39146000428313));
#63939=CARTESIAN_POINT('Ctrl Pts',(2.53813383284947,1.64874201853731,7.55002144869191));
#63940=CARTESIAN_POINT('Ctrl Pts',(-0.00472259831748953,3.02662374506822,
7.70858289310063));
#63941=CARTESIAN_POINT('Ctrl Pts',(-2.54326669687965,1.64081324521975,7.86714433750941));
#63942=CARTESIAN_POINT('Ctrl Pts',(-2.7594849988412,-1.24326832916955,8.02570578191813));
#63943=CARTESIAN_POINT('Ctrl Pts',(-0.455942708646288,-2.99208787363906,
8.18426722632691));
#63944=CARTESIAN_POINT('Ctrl Pts',(2.26393323438981,-2.00875083257506,8.34282867073565));
#63945=CARTESIAN_POINT('Ctrl Pts',(2.91655034119946,0.808831072842144,8.50139011514441));
#63946=CARTESIAN_POINT('Ctrl Pts',(0.905986231991998,2.88784738942115,8.65995155955315));
#63947=CARTESIAN_POINT('Ctrl Pts',(-1.93185847680866,2.3298919337017,8.81851300396191));
#63948=CARTESIAN_POINT('Ctrl Pts',(-3.00567081669626,-0.355551035445139,
8.97707444837065));
#63949=CARTESIAN_POINT('Ctrl Pts',(-1.33492361736317,-2.7163307112632,9.13563589277941));
#63950=CARTESIAN_POINT('Ctrl Pts',(1.55477854131312,-2.59675514529536,9.29419733718816));
#63951=CARTESIAN_POINT('Ctrl Pts',(3.02477024692428,-0.106012029823702,
9.45275878159692));
#63952=CARTESIAN_POINT('Ctrl Pts',(1.73276220557981,2.48153354522155,9.61132022600566));
#63953=CARTESIAN_POINT('Ctrl Pts',(-1.14147799974873,2.8031235387038,9.76988167041442));
#63954=CARTESIAN_POINT('Ctrl Pts',(-2.97340368559691,0.565105405764596,
9.92844311482316));
#63955=CARTESIAN_POINT('Ctrl Pts',(-2.09023382474483,-2.18892579934503,
10.0870045592319));
#63956=CARTESIAN_POINT('Ctrl Pts',(0.701585230502688,-2.94418949143668,
10.2455660036407));
#63957=CARTESIAN_POINT('Ctrl Pts',(2.85276778415585,-1.01103390983099,10.4041274480494));
#63958=CARTESIAN_POINT('Ctrl Pts',(2.39901070446873,1.84532415499016,10.5626888924582));
#63959=CARTESIAN_POINT('Ctrl Pts',(-0.245348112796364,3.01666668703935,
10.7212503368669));
#63960=CARTESIAN_POINT('Ctrl Pts',(-2.66567291420564,1.43340905243968,10.8798117812757));
#63961=CARTESIAN_POINT('Ctrl Pts',(-2.65189948220728,-1.45873326328511,
11.0383732256844));
#63962=CARTESIAN_POINT('Ctrl Pts',(-0.216604711106824,-3.01886667414644,
11.1969346700932));
#63963=CARTESIAN_POINT('Ctrl Pts',(2.4164776962198,-1.8223910504658,11.3554961145019));
#63964=CARTESIAN_POINT('Ctrl Pts',(2.84300878208006,1.03815926627918,11.5140575589107));
#63965=CARTESIAN_POINT('Ctrl Pts',(0.67351144406832,2.95073820117182,11.6726190033194));
#63966=CARTESIAN_POINT('Ctrl Pts',(-2.11098745975819,2.16891805790105,11.8311804477282));
#63967=CARTESIAN_POINT('Ctrl Pts',(-2.96788646220135,-0.593399987047231,
11.9897418921369));
#63968=CARTESIAN_POINT('Ctrl Pts',(-1.11472784425878,-2.81386841028145,
12.1483033365457));
#63969=CARTESIAN_POINT('Ctrl Pts',(1.75631900069801,-2.46491727344607,12.3068647809544));
#63970=CARTESIAN_POINT('Ctrl Pts',(3.02362333316682,0.134816676545898,12.4654262253632));
#63971=CARTESIAN_POINT('Ctrl Pts',(1.52997519673727,2.6114458628343,12.6239876697719));
#63972=CARTESIAN_POINT('Ctrl Pts',(-1.36073478613619,2.70349300700863,12.7825491141807));
#63973=CARTESIAN_POINT('Ctrl Pts',(-3.0089209314377,0.326907365321966,12.9411105585894));
#63974=CARTESIAN_POINT('Ctrl Pts',(-1.90957976960207,-2.34818625766188,
13.0996720029982));
#63975=CARTESIAN_POINT('Ctrl Pts',(0.9334504693777,-2.87908732385182,13.2582334474069));
#63976=CARTESIAN_POINT('Ctrl Pts',(2.92412176875259,-0.781015671195471,
13.4167948918157));
#63977=CARTESIAN_POINT('Ctrl Pts',(2.24469817626766,2.03022257267676,13.5753563362244));
#63978=CARTESIAN_POINT('Ctrl Pts',(-0.484420199200288,2.98760952397606,
13.7339177806332));
#63979=CARTESIAN_POINT('Ctrl Pts',(-2.77120135286706,1.21692919227597,13.892479225042));
#63980=CARTESIAN_POINT('Ctrl Pts',(-2.52752339375828,-1.66496218910528,
14.0510406694507));
#63981=CARTESIAN_POINT('Ctrl Pts',(0.0241047248984299,-3.02653144034276,
14.2096021138595));
#63982=CARTESIAN_POINT('Ctrl Pts',(2.55372216550858,-1.62449275114906,14.3681635582682));
#63983=CARTESIAN_POINT('Ctrl Pts',(2.75146663755133,1.26091432682304,14.526725002677));
#63984=CARTESIAN_POINT('Ctrl Pts',(0.436772300596569,2.99494633584264,14.6852864470857));
#63985=CARTESIAN_POINT('Ctrl Pts',(-2.27675066969048,1.99421161996656,14.8438478914945));
#63986=CARTESIAN_POINT('Ctrl Pts',(-2.91131085595766,-0.827491810913372,
15.0024093359032));
#63987=CARTESIAN_POINT('Ctrl Pts',(-0.887474142281572,-2.89359002692629,
15.160970780312));
#63988=CARTESIAN_POINT('Ctrl Pts',(1.94673927980861,-2.31747271258928,15.3195322247207));
#63989=CARTESIAN_POINT('Ctrl Pts',(3.00333226818571,0.374791787556893,15.4780936691295));
#63990=CARTESIAN_POINT('Ctrl Pts',(1.31750110941066,2.72482374179457,15.6366551135382));
#63991=CARTESIAN_POINT('Ctrl Pts',(-1.5713760441821,2.58674523772951,15.795216557947));
#63992=CARTESIAN_POINT('Ctrl Pts',(-3.02538711470083,0.0866395022367191,
15.9537780023557));
#63993=CARTESIAN_POINT('Ctrl Pts',(-1.71683515956719,-2.49257911248963,
16.1123394467645));
#63994=CARTESIAN_POINT('Ctrl Pts',(1.15940554188062,-2.79575613861477,16.2709008911732));
#63995=CARTESIAN_POINT('Ctrl Pts',(2.97696159891635,-0.546052411150268,
16.429462335582));
#63996=CARTESIAN_POINT('Ctrl Pts',(2.07617328210605,2.20226658236796,16.5880237799907));
#63997=CARTESIAN_POINT('Ctrl Pts',(-0.720425166281659,2.93963623207596,
16.7465852243995));
#63998=CARTESIAN_POINT('Ctrl Pts',(-2.85918385675924,0.992744312697378,
16.9051466688082));
#63999=CARTESIAN_POINT('Ctrl Pts',(-2.38714422399272,-1.86064936272363,
17.063708113217));
#64000=CARTESIAN_POINT('Ctrl Pts',(0.264661541199501,-3.01503364255784,
17.2222695576257));
#64001=CARTESIAN_POINT('Ctrl Pts',(2.67479767526346,-1.41630893294889,17.3808310020345));
#64002=CARTESIAN_POINT('Ctrl Pts',(2.64250350912616,1.47568587490753,17.5393924464433));
#64003=CARTESIAN_POINT('Ctrl Pts',(0.197267721734377,3.02019188845799,17.697953890852));
#64004=CARTESIAN_POINT('Ctrl Pts',(-2.42809857245107,1.80687877833759,17.8565153352607));
#64005=CARTESIAN_POINT('Ctrl Pts',(-2.83630220791474,-1.05634434846013,
18.0150767796695));
#64006=CARTESIAN_POINT('Ctrl Pts',(-0.654601374265098,-2.95499080167026,
18.1736382240782));
#64007=CARTESIAN_POINT('Ctrl Pts',(2.12483372760391,-2.15535501186755,18.332199668487));
#64008=CARTESIAN_POINT('Ctrl Pts',(2.96402552539639,0.612393894437513,18.4907611128958));
#64009=CARTESIAN_POINT('Ctrl Pts',(1.09668522891184,2.82094932705857,18.6493225573045));
#64010=CARTESIAN_POINT('Ctrl Pts',(-1.77206809318166,2.45361942246004,18.8078840017132));
#64011=CARTESIAN_POINT('Ctrl Pts',(-3.02269797931083,-0.154176921151835,
18.966445446122));
#64012=CARTESIAN_POINT('Ctrl Pts',(-1.51322036224401,-2.62119013664323,
19.1250068905308));
#64013=CARTESIAN_POINT('Ctrl Pts',(1.37801980748479,-2.69472354933216,19.2835683349395));
#64014=CARTESIAN_POINT('Ctrl Pts',(3.01095271786289,-0.307631805800035,
19.4421297793482));
#64015=CARTESIAN_POINT('Ctrl Pts',(1.89450304181512,2.3603668828593,19.600691223757));
#64016=CARTESIAN_POINT('Ctrl Pts',(-0.951868742340097,2.87305055550742,
19.7592526681658));
#64017=CARTESIAN_POINT('Ctrl Pts',(-2.92906336232834,0.76227384620716,19.9178141125745));
#64018=CARTESIAN_POINT('Ctrl Pts',(-2.23165078734232,-2.04455578561703,
20.0763755569833));
#64019=CARTESIAN_POINT('Ctrl Pts',(0.503542645942066,-2.98444607940289,
20.234937001392));
#64020=CARTESIAN_POINT('Ctrl Pts',(2.77893763268742,-1.19915771722462,20.3934984458008));
#64021=CARTESIAN_POINT('Ctrl Pts',(2.51680929973837,1.68111407878709,20.5520598902095));
#64022=CARTESIAN_POINT('Ctrl Pts',(-0.0434858629331975,3.02631501613275,
20.7106213346183));
#64023=CARTESIAN_POINT('Ctrl Pts',(-2.56407290478473,1.60810563586303,20.869182779027));
#64024=CARTESIAN_POINT('Ctrl Pts',(-2.74333543731449,-1.27850861378411,
21.0277442234358));
#64025=CARTESIAN_POINT('Ctrl Pts',(-0.417583980308469,-2.99768197388171,
21.1863056678445));
#64026=CARTESIAN_POINT('Ctrl Pts',(2.28947473437029,-1.97959062379721,21.3448671122533));
#64027=CARTESIAN_POINT('Ctrl Pts',(2.90595197648197,0.846118613154382,21.503428556662));
#64028=CARTESIAN_POINT('Ctrl Pts',(0.868925656837218,2.89921399693704,21.6619900010708));
#64029=CARTESIAN_POINT('Ctrl Pts',(-1.96154024611074,2.30495845082584,21.8205514454795));
#64030=CARTESIAN_POINT('Ctrl Pts',(-3.00087055159965,-0.39401716928028,
21.9791128898883));
#64031=CARTESIAN_POINT('Ctrl Pts',(-1.30002457011512,-2.73320502601664,
22.137674334297));
#64032=CARTESIAN_POINT('Ctrl Pts',(1.5879091041769,-2.57662924651915,22.2962357787058));
#64033=CARTESIAN_POINT('Ctrl Pts',(3.0258799099222,-0.0672634215228445,
22.4547972231145));
#64034=CARTESIAN_POINT('Ctrl Pts',(1.70083770533339,2.50352245791043,22.6133586675233));
#64035=CARTESIAN_POINT('Ctrl Pts',(-1.17728553624331,2.78827408324539,22.771920111932));
#64036=CARTESIAN_POINT('Ctrl Pts',(-2.98039742563387,0.526977022668581,
22.9304815563408));
#64037=CARTESIAN_POINT('Ctrl Pts',(-2.06202759461993,-2.21551704939764,
23.0890430007495));
#64038=CARTESIAN_POINT('Ctrl Pts',(0.739235557084079,-2.93496241684426,
23.2476044451583));
#64039=CARTESIAN_POINT('Ctrl Pts',(2.86548267288157,-0.974414002650417,
23.406165889567));
#64040=CARTESIAN_POINT('Ctrl Pts',(2.37517984560405,1.87589826434749,23.5647273339758));
#64041=CARTESIAN_POINT('Ctrl Pts',(-0.283964115707739,3.0132769501219,23.7232887783845));
#64042=CARTESIAN_POINT('Ctrl Pts',(-2.68381274160463,1.39915072995952,23.8818502227933));
#64043=CARTESIAN_POINT('Ctrl Pts',(-2.63299916572745,-1.49257796795484,
24.0404116672021));
#64044=CARTESIAN_POINT('Ctrl Pts',(-0.177922642319488,-3.02139324327301,
24.1989731116108));
#64045=CARTESIAN_POINT('Ctrl Pts',(2.43961987121247,-1.79129240525688,24.3575345560196));
#64046=CARTESIAN_POINT('Ctrl Pts',(2.8294793156556,1.07448610946012,24.5160960004283));
#64047=CARTESIAN_POINT('Ctrl Pts',(0.635664458950241,2.95912221659957,24.6746574448371));
#64048=CARTESIAN_POINT('Ctrl Pts',(-2.13859285501431,2.14170357370654,24.8332188892458));
#64049=CARTESIAN_POINT('Ctrl Pts',(-2.96004303250402,-0.631362687264734,
24.9917803336546));
#64050=CARTESIAN_POINT('Ctrl Pts',(-1.07859763798547,-2.82791455537078,
25.1503417780633));
#64051=CARTESIAN_POINT('Ctrl Pts',(1.78774451231545,-2.44222094738204,25.3089032224721));
#64052=CARTESIAN_POINT('Ctrl Pts',(3.02164866318236,0.173530842889411,25.4674646668808));
#64053=CARTESIAN_POINT('Ctrl Pts',(1.49640346986859,2.63082691420604,25.6260261112896));
#64054=CARTESIAN_POINT('Ctrl Pts',(-1.39524831558989,2.68584357976953,25.7845875556983));
#64055=CARTESIAN_POINT('Ctrl Pts',(-3.0128610236943,0.288343630152394,25.9431490001071));
#64056=CARTESIAN_POINT('Ctrl Pts',(-1.87934861956321,-2.37245070829545,
26.1017104445158));
#64057=CARTESIAN_POINT('Ctrl Pts',(0.970247978715583,-2.8668959620021,26.2602718889246));
#64058=CARTESIAN_POINT('Ctrl Pts',(2.93388483363149,-0.743500760008172,
26.4188333333333));
#64059=CARTESIAN_POINT('Ctrl Pts',(2.2185118773636,2.0588051503584,26.5773947777421));
#64060=CARTESIAN_POINT('Ctrl Pts',(-0.522644442162044,2.98116024128573,
26.7359562221508));
#64061=CARTESIAN_POINT('Ctrl Pts',(-2.7865599469623,1.18133706414857,26.8945176665596));
#64062=CARTESIAN_POINT('Ctrl Pts',(-2.50599199017975,-1.69719702518614,
27.0530791109683));
#64063=CARTESIAN_POINT('Ctrl Pts',(0.0628652175921859,-3.02597448131387,
27.2116405553771));
#64064=CARTESIAN_POINT('Ctrl Pts',(2.57431849021943,-1.59165257140494,27.3702019997858));
#64065=CARTESIAN_POINT('Ctrl Pts',(2.73509173159499,1.29605046850281,27.5287634441946));
#64066=CARTESIAN_POINT('Ctrl Pts',(0.398378534703953,3.00029467556651,27.6873248886033));
#64067=CARTESIAN_POINT('Ctrl Pts',(-2.30210490660938,1.9648884436809,27.8458863330121));
#64068=CARTESIAN_POINT('Ctrl Pts',(-2.90047392254249,-0.864710715671257,
28.0044477774208));
#64069=CARTESIAN_POINT('Ctrl Pts',(-0.85034153634106,-2.90471906881178,
28.1630092218296));
#64070=CARTESIAN_POINT('Ctrl Pts',(1.97626076872048,-2.29234966162712,28.3215706662384));
#64071=CARTESIAN_POINT('Ctrl Pts',(2.99828576789421,0.413226392173409,28.4801321106471));
#64072=CARTESIAN_POINT('Ctrl Pts',(1.2824947161976,2.74147422020906,28.6386935550559));
#64073=CARTESIAN_POINT('Ctrl Pts',(-1.60437704326902,2.56640758652578,28.7972549994646));
#64074=CARTESIAN_POINT('Ctrl Pts',(-3.02624861237858,0.0478845823042429,
28.9558164438734));
#64075=CARTESIAN_POINT('Ctrl Pts',(-1.68477049894157,-2.51436313269221,
29.1143778882821));
#64076=CARTESIAN_POINT('Ctrl Pts',(1.19511724956988,-2.78067767943826,29.2729393326909));
#64077=CARTESIAN_POINT('Ctrl Pts',(2.98371102484459,-0.507880022610132,
29.4315007770996));
#64078=CARTESIAN_POINT('Ctrl Pts',(2.0477973424077,2.22867665702622,29.5900622215084));
#64079=CARTESIAN_POINT('Ctrl Pts',(-0.758015631487026,2.93016823741693,
29.7486236659171));
#64080=CARTESIAN_POINT('Ctrl Pts',(-2.87166397420542,0.956043731424721,
29.9071851103259));
#64081=CARTESIAN_POINT('Ctrl Pts',(-2.36311805996753,-1.8910702344971,30.0657465547346));
#64082=CARTESIAN_POINT('Ctrl Pts',(0.303255044713435,-3.01139668177433,
30.2243079991434));
#64083=CARTESIAN_POINT('Ctrl Pts',(2.69271774351707,-1.38193514713752,30.3828694435521));
#64084=CARTESIAN_POINT('Ctrl Pts',(2.62338684178872,1.50940884967445,30.5414308879609));
#64085=CARTESIAN_POINT('Ctrl Pts',(0.158570266212879,3.02247068932337,30.6999923323696));
#64086=CARTESIAN_POINT('Ctrl Pts',(-2.45104112001013,1.77563257042811,30.8585537767784));
#64087=CARTESIAN_POINT('Ctrl Pts',(-2.82254038511267,-1.09258380527705,
31.0171152211871));
#64088=CARTESIAN_POINT('Ctrl Pts',(-0.616701474735501,-2.96313227652845,
31.1756766655959));
#64089=CARTESIAN_POINT('Ctrl Pts',(2.15226427772119,-2.12796430326989,31.3342381100046));
#64090=CARTESIAN_POINT('Ctrl Pts',(2.95593914684811,0.65030558760985,31.4927995544134));
#64091=CARTESIAN_POINT('Ctrl Pts',(1.06046581326025,2.83476380957074,31.6513609988221));
#64092=CARTESIAN_POINT('Ctrl Pts',(-1.80334761520199,2.43072231566893,31.8099224432309));
#64093=CARTESIAN_POINT('Ctrl Pts',(-3.02047542781434,-0.19287764804512,
31.9684838876396));
#64094=CARTESIAN_POINT('Ctrl Pts',(-1.47952520927975,-2.64035580031392,
32.1270453320484));
#64095=CARTESIAN_POINT('Ctrl Pts',(1.41241960390228,-2.67685346249252,32.2856067764571));
#64096=CARTESIAN_POINT('Ctrl Pts',(3.01464577067142,-0.269043629396191,
32.4441682208659));
#64097=CARTESIAN_POINT('Ctrl Pts',(1.8641171243363,2.38443723840698,32.6027296652746));
#64098=CARTESIAN_POINT('Ctrl Pts',(-0.988587424762973,2.86062379573864,
32.7612911096834));
#64099=CARTESIAN_POINT('Ctrl Pts',(-2.93858598493123,0.724697182491683,
32.9198525540921));
#64100=CARTESIAN_POINT('Ctrl Pts',(-2.20528198516443,-2.07297008252769,
33.0784139985009));
#64101=CARTESIAN_POINT('Ctrl Pts',(0.541724804486454,-2.97775214437831,
33.2369754429096));
#64102=CARTESIAN_POINT('Ctrl Pts',(2.79406798309702,-1.16346796388132,33.3955368873184));
#64103=CARTESIAN_POINT('Ctrl Pts',(2.49507190870534,1.71321036873323,33.5540983317272));
#64104=CARTESIAN_POINT('Ctrl Pts',(-0.0822419941187573,3.0255098498515,
33.7126597761359));
#64105=CARTESIAN_POINT('Ctrl Pts',(-2.58445850163663,1.57513423252295,33.8712212205446));
#64106=CARTESIAN_POINT('Ctrl Pts',(-2.72673585847062,-1.31353917157969,
34.0297826649534));
#64107=CARTESIAN_POINT('Ctrl Pts',(-0.379156751408429,-3.00278433374826,
34.1883441093622));
#64108=CARTESIAN_POINT('Ctrl Pts',(2.31464066844022,-1.95010568256221,34.3469055537709));
#64109=CARTESIAN_POINT('Ctrl Pts',(2.89487691879338,0.883267355995366,34.5054669981796));
#64110=CARTESIAN_POINT('Ctrl Pts',(0.831722542943288,2.9101050167805,34.6640284425885));
#64111=CARTESIAN_POINT('Ctrl Pts',(-1.99090024395484,2.27964686209391,34.8225898869971));
#64112=CARTESIAN_POINT('Ctrl Pts',(-2.99557802304852,-0.432418668472894,
34.9811513314059));
#64113=CARTESIAN_POINT('Ctrl Pts',(-1.26491226661167,-2.74963098521777,
35.1397127758147));
#64114=CARTESIAN_POINT('Ctrl Pts',(1.62077918618811,-2.55608067700269,35.2982742202234));
#64115=CARTESIAN_POINT('Ctrl Pts',(3.02649320678206,-0.0285037792053614,
35.4568356646322));
#64116=CARTESIAN_POINT('Ctrl Pts',(1.6686341996346,2.52510069204211,35.6153971090409));
#64117=CARTESIAN_POINT('Ctrl Pts',(-1.21289995118223,2.77296723912937,35.7739585534497));
#64118=CARTESIAN_POINT('Ctrl Pts',(-2.98690225949438,0.488762193381373,
35.9325199978584));
#64119=CARTESIAN_POINT('Ctrl Pts',(-2.03348311127567,-2.24174486410168,
36.0910814422672));
#64120=CARTESIAN_POINT('Ctrl Pts',(0.776764623540637,-2.92525389321091,
36.2496428866759));
#64121=CARTESIAN_POINT('Ctrl Pts',(2.87772749916196,-0.937634247041048,
36.4082043310847));
#64122=CARTESIAN_POINT('Ctrl Pts',(2.35095937714186,1.90616464074957,36.5667657754934));
#64123=CARTESIAN_POINT('Ctrl Pts',(-0.322533566468511,3.00939293411291,
36.7253272199022));
#64124=CARTESIAN_POINT('Ctrl Pts',(-2.70151225974056,1.36466285332016,36.883888664311));
#64125=CARTESIAN_POINT('Ctrl Pts',(-2.61366703848361,-1.52617775887959,
37.0424501087197));
#64126=CARTESIAN_POINT('Ctrl Pts',(-0.139211182967247,-3.02342431778626,
37.2010115531285));
#64127=CARTESIAN_POINT('Ctrl Pts',(2.4623614610291,-1.75989965779052,37.3595729975371));
#64128=CARTESIAN_POINT('Ctrl Pts',(2.8154864438876,1.1106362009136,37.518134441946));
#64129=CARTESIAN_POINT('Ctrl Pts',(0.597711781573062,2.96702175728379,37.6766958863547));
#64130=CARTESIAN_POINT('Ctrl Pts',(-2.16584472998421,2.11413596992682,37.8352573307635));
#64131=CARTESIAN_POINT('Ctrl Pts',(-2.9517191980829,-0.669218395448239,
37.9938187751722));
#64132=CARTESIAN_POINT('Ctrl Pts',(-1.04228065031701,-2.84150334027313,
38.152380219581));
#64133=CARTESIAN_POINT('Ctrl Pts',(1.81885797164076,-2.41911153657142,38.3109416639897));
#64134=CARTESIAN_POINT('Ctrl Pts',(3.01921417384548,0.212192764679598,38.4695031083984));
#64135=CARTESIAN_POINT('Ctrl Pts',(1.46251786451651,2.64982177476087,38.6280645528072));
#64136=CARTESIAN_POINT('Ctrl Pts',(-1.429402439371,2.66766699375318,38.786625997216));
#64137=CARTESIAN_POINT('Ctrl Pts',(-3.01655597425476,0.249897813151183,
38.9451874416247));
#64138=CARTESIAN_POINT('Ctrl Pts',(-1.84833359844375,-2.39664153302016,
39.1037488860335));
#64139=CARTESIAN_POINT('Ctrl Pts',(1.00597614714323,-2.85362950697119,39.2623103304422));
#64140=CARTESIAN_POINT('Ctrl Pts',(2.94492748067747,-0.707041802870931,
39.420871774851));
#64141=CARTESIAN_POINT('Ctrl Pts',(2.18838961321059,2.08950618451892,39.5794332192597));
#64142=CARTESIAN_POINT('Ctrl Pts',(0.361364824312418,2.67510712391322,39.6851408488656));
#64143=CARTESIAN_POINT('Ctrl Pts',(-0.474664453622152,2.51747565713064,
39.7379946636685));
#64144=CARTESIAN_POINT('Ctrl Pts',(-1.20564430054356,2.47375567929507,-0.109744663668475));
#64145=CARTESIAN_POINT('Ctrl Pts',(-2.02715459737193,2.07337288664547,-0.0568908488655582));
#64146=CARTESIAN_POINT('Ctrl Pts',(-3.22591201434709,0.396938321840822,
0.0488167807402761));
#64147=CARTESIAN_POINT('Ctrl Pts',(-2.08416667989131,-2.49808316060539,
0.207378225149028));
#64148=CARTESIAN_POINT('Ctrl Pts',(0.963414872632741,-3.1041939934932,0.365939669557779));
#64149=CARTESIAN_POINT('Ctrl Pts',(3.12987608714624,-0.879703367138011,
0.524501113966532));
#64150=CARTESIAN_POINT('Ctrl Pts',(2.43909306726452,2.15010239123153,0.683062558375283));
#64151=CARTESIAN_POINT('Ctrl Pts',(-0.479274468080505,3.21552770689972,
0.841624002784034));
#64152=CARTESIAN_POINT('Ctrl Pts',(-2.95980306988425,1.34532463900819,1.00018544719279));
#64153=CARTESIAN_POINT('Ctrl Pts',(-2.73776025065754,-1.75362282654376,
1.15874689160154));
#64154=CARTESIAN_POINT('Ctrl Pts',(-0.0157392478644119,-3.2511367042434,
1.31730833601029));
#64155=CARTESIAN_POINT('Ctrl Pts',(2.72062483828669,-1.78002968372146,1.47586978041904));
#64156=CARTESIAN_POINT('Ctrl Pts',(2.97272771949037,1.31651274994322,1.63443122482779));
#64157=CARTESIAN_POINT('Ctrl Pts',(0.510344372216115,3.21088965713636,1.79299266923654));
#64158=CARTESIAN_POINT('Ctrl Pts',(-2.41804410895251,2.17332768185625,1.9515541136453));
#64159=CARTESIAN_POINT('Ctrl Pts',(-3.13845311149299,-0.848764793424488,
2.11011555805404));
#64160=CARTESIAN_POINT('Ctrl Pts',(-0.993054319402781,-3.09582394518012,
2.2686770024628));
#64161=CARTESIAN_POINT('Ctrl Pts',(2.05912870633672,-2.51600395318794,2.42723844687155));
#64162=CARTESIAN_POINT('Ctrl Pts',(3.23106577827023,0.361248355871118,2.58579989128031));
#64163=CARTESIAN_POINT('Ctrl Pts',(1.45262889441719,2.90863453724861,2.74436133568905));
#64164=CARTESIAN_POINT('Ctrl Pts',(-1.65224274345245,2.80006787716128,2.90292278009781));
#64165=CARTESIAN_POINT('Ctrl Pts',(-3.24840676708004,0.134683172671852,
3.06148422450655));
#64166=CARTESIAN_POINT('Ctrl Pts',(-1.87836244833034,-2.65368432378687,
3.22004566891531));
#64167=CARTESIAN_POINT('Ctrl Pts',(1.20686555247667,-3.01890072833779,3.37860711332406));
#64168=CARTESIAN_POINT('Ctrl Pts',(3.19007189253275,-0.627476984487285,
3.53716855773281));
#64169=CARTESIAN_POINT('Ctrl Pts',(2.26033706649506,2.33691300217663,3.69573000214156));
#64170=CARTESIAN_POINT('Ctrl Pts',(-0.73337283554914,3.16740435233008,3.85429144655032));
#64171=CARTESIAN_POINT('Ctrl Pts',(-3.05742011265761,1.10565288291763,4.01285289095907));
#64172=CARTESIAN_POINT('Ctrl Pts',(-2.58965416442564,-1.96570021882515,
4.17141433536782));
#64173=CARTESIAN_POINT('Ctrl Pts',(0.242795234836198,-3.24211913991506,
4.32997577977658));
#64174=CARTESIAN_POINT('Ctrl Pts',(2.8535417204786,-1.55807114478789,4.48853722418531));
#64175=CARTESIAN_POINT('Ctrl Pts',(2.85864187046401,1.54869386873951,4.64709866859408));
#64176=CARTESIAN_POINT('Ctrl Pts',(0.253438599627609,3.24130450885329,4.80566011300282));
#64177=CARTESIAN_POINT('Ctrl Pts',(-2.58318633003087,1.97419209478631,4.96422155741158));
#64178=CARTESIAN_POINT('Ctrl Pts',(-3.06103376339185,-1.09560866286668,
5.12278300182033));
#64179=CARTESIAN_POINT('Ctrl Pts',(-0.743768249416836,-3.16497943657876,
5.28134444622908));
#64180=CARTESIAN_POINT('Ctrl Pts',(2.25265222476723,-2.34432164965467,5.43990589063783));
#64181=CARTESIAN_POINT('Ctrl Pts',(3.19211485856089,0.616999815676252,5.59846733504658));
#64182=CARTESIAN_POINT('Ctrl Pts',(1.21677084197797,3.01492201572549,5.75702877945533));
#64183=CARTESIAN_POINT('Ctrl Pts',(-1.86963963033482,2.65983715581851,5.91559022386409));
#64184=CARTESIAN_POINT('Ctrl Pts',(-3.24883144988067,-0.124017148241245,
6.07415166827284));
#64185=CARTESIAN_POINT('Ctrl Pts',(-1.66142716131023,-2.79462803078564,
6.23271311268159));
#64186=CARTESIAN_POINT('Ctrl Pts',(1.44307132765125,-2.9133882655943,6.39127455709034));
#64187=CARTESIAN_POINT('Ctrl Pts',(3.22986224994229,-0.371854661379337,
6.54983600149909));
#64188=CARTESIAN_POINT('Ctrl Pts',(2.06737835504244,2.50922951917395,6.70839744590785));
#64189=CARTESIAN_POINT('Ctrl Pts',(-0.982884785006702,3.09906817320855,
6.86695889031659));
#64190=CARTESIAN_POINT('Ctrl Pts',(-3.13564917114702,0.859063628770815,
7.02552033472535));
#64191=CARTESIAN_POINT('Ctrl Pts',(-2.42516725748781,-2.16537521367566,
7.1840817791341));
#64192=CARTESIAN_POINT('Ctrl Pts',(0.499800651700313,-3.21255122159192,
7.34264322354285));
#64193=CARTESIAN_POINT('Ctrl Pts',(2.96838703077778,-1.32625958179467,7.5012046679516));
#64194=CARTESIAN_POINT('Ctrl Pts',(2.72645870672651,1.77107565149178,7.65976611236035));
#64195=CARTESIAN_POINT('Ctrl Pts',(-0.00507300644854954,3.2511936742368,
7.8183275567691));
#64196=CARTESIAN_POINT('Ctrl Pts',(-2.73197241985096,1.76255857774021,7.97688900117786));
#64197=CARTESIAN_POINT('Ctrl Pts',(-2.96423372313876,-1.33551655826455,
8.1354504455866));
#64198=CARTESIAN_POINT('Ctrl Pts',(-0.489772821144476,-3.21409530450794,
8.29401188999536));
#64199=CARTESIAN_POINT('Ctrl Pts',(2.43191292691616,-2.15779645905029,8.45257333440411));
#64200=CARTESIAN_POINT('Ctrl Pts',(3.13295302574422,0.868844854546515,8.61113477881286));
#64201=CARTESIAN_POINT('Ctrl Pts',(0.973208748261957,3.10212036760313,8.76969622322162));
#64202=CARTESIAN_POINT('Ctrl Pts',(-2.0751988315547,2.50276564070748,8.92825766763037));
#64203=CARTESIAN_POINT('Ctrl Pts',(-3.22868607702037,-0.381932269972927,
9.08681911203912));
#64204=CARTESIAN_POINT('Ctrl Pts',(-1.43397250068901,-2.91787746659443,
9.24538055644787));
#64205=CARTESIAN_POINT('Ctrl Pts',(1.67014025664517,-2.78942961300785,9.40394200085662));
#64206=CARTESIAN_POINT('Ctrl Pts',(3.24920264993105,-0.11387792794435,9.56250344526537));
#64207=CARTESIAN_POINT('Ctrl Pts',(1.86132998226725,2.66565878159693,9.72106488967412));
#64208=CARTESIAN_POINT('Ctrl Pts',(-1.22617357314765,3.01111016259887,9.87962633408288));
#64209=CARTESIAN_POINT('Ctrl Pts',(-3.19402478399152,0.607035190116496,
10.0381877784916));
#64210=CARTESIAN_POINT('Ctrl Pts',(-2.24532533974844,-2.35134007780147,
10.1967492229004));
#64211=CARTESIAN_POINT('Ctrl Pts',(0.753641567461229,-3.16264295022161,
10.3553106673091));
#64212=CARTESIAN_POINT('Ctrl Pts',(3.06443791998503,-1.08605077107364,10.5138721117179));
#64213=CARTESIAN_POINT('Ctrl Pts',(2.57701289745849,1.98224382181518,10.6724335561266));
#64214=CARTESIAN_POINT('Ctrl Pts',(-0.263552492644499,3.24049782076964,
10.8309950005354));
#64215=CARTESIAN_POINT('Ctrl Pts',(-2.86346095393319,1.53976537436449,10.9895564449442));
#64216=CARTESIAN_POINT('Ctrl Pts',(-2.84866555854953,-1.56696859519441,
11.1481178893529));
#64217=CARTESIAN_POINT('Ctrl Pts',(-0.232676383282734,-3.24286104288395,
11.3066793337616));
#64218=CARTESIAN_POINT('Ctrl Pts',(2.59577590795226,-1.95760912300858,11.4652407781704));
#64219=CARTESIAN_POINT('Ctrl Pts',(3.05395481785924,1.11518877920565,11.6238022225792));
#64220=CARTESIAN_POINT('Ctrl Pts',(0.723484757578079,3.16967756220472,11.7823636669879));
#64221=CARTESIAN_POINT('Ctrl Pts',(-2.26761885640482,2.3298477986489,11.9409251113967));
#64222=CARTESIAN_POINT('Ctrl Pts',(-3.188098192742,-0.637429177420582,12.0994865558054));
#64223=CARTESIAN_POINT('Ctrl Pts',(-1.19743860519664,-3.02265228393486,
12.2580480002142));
#64224=CARTESIAN_POINT('Ctrl Pts',(1.88663464836552,-2.64780961294021,12.4166094446229));
#64225=CARTESIAN_POINT('Ctrl Pts',(3.24797063727694,0.144819826607834,12.5751708890317));
#64226=CARTESIAN_POINT('Ctrl Pts',(1.64349654940643,2.80521035483633,12.7337323334404));
#64227=CARTESIAN_POINT('Ctrl Pts',(-1.46169881083137,2.90408722823644,12.8922937778492));
#64228=CARTESIAN_POINT('Ctrl Pts',(-3.23217734431291,0.351163292076785,
13.0508552222579));
#64229=CARTESIAN_POINT('Ctrl Pts',(-2.05126708514628,-2.52241736994243,
13.2094166666667));
#64230=CARTESIAN_POINT('Ctrl Pts',(1.00271078167531,-3.09271032123992,13.3679781110754));
#64231=CARTESIAN_POINT('Ctrl Pts',(3.14108623933113,-0.838965601128271,
13.5265395554842));
#64232=CARTESIAN_POINT('Ctrl Pts',(2.41125066277032,2.18086136287512,13.6851009998929));
#64233=CARTESIAN_POINT('Ctrl Pts',(-0.520363289252294,3.209284669516,13.8436624443017));
#64234=CARTESIAN_POINT('Ctrl Pts',(-2.97681940913832,1.3072231057357,14.0022238887104));
#64235=CARTESIAN_POINT('Ctrl Pts',(-2.71506099252092,-1.78849932895798,
14.1607853331192));
#64236=CARTESIAN_POINT('Ctrl Pts',(0.0258932512628897,-3.25109452067006,
14.3193467775279));
#64237=CARTESIAN_POINT('Ctrl Pts',(2.74320366507031,-1.74502713295143,14.4779082219367));
#64238=CARTESIAN_POINT('Ctrl Pts',(2.95562041415185,1.35447185657016,14.6364696663454));
#64239=CARTESIAN_POINT('Ctrl Pts',(0.469180003987954,3.21716585936283,14.7950311107542));
#64240=CARTESIAN_POINT('Ctrl Pts',(-2.44568139240097,2.14217846354022,14.9535925551629));
#64241=CARTESIAN_POINT('Ctrl Pts',(-3.12732478030997,-0.888890185147194,
15.1121539995717));
#64242=CARTESIAN_POINT('Ctrl Pts',(-0.953323095457733,-3.10828909827557,
15.2707154439804));
#64243=CARTESIAN_POINT('Ctrl Pts',(2.09118376283658,-2.48942493617312,15.4292768883892));
#64244=CARTESIAN_POINT('Ctrl Pts',(3.2261740125007,0.402600650591831,15.5878383327979));
#64245=CARTESIAN_POINT('Ctrl Pts',(1.41525727461016,2.92700066440971,15.7463997772067));
#64246=CARTESIAN_POINT('Ctrl Pts',(-1.68796926377685,2.77867698866502,15.9049612216154));
#64247=CARTESIAN_POINT('Ctrl Pts',(-3.2498652881649,0.0930679943517114,
16.0635226660242));
#64248=CARTESIAN_POINT('Ctrl Pts',(-1.84422117866062,-2.67752390969185,
16.2220841104329));
#64249=CARTESIAN_POINT('Ctrl Pts',(1.24543130601543,-3.00319611493964,16.3806455548417));
#64250=CARTESIAN_POINT('Ctrl Pts',(3.19784668795183,-0.586568498256862,
16.5392069992504));
#64251=CARTESIAN_POINT('Ctrl Pts',(2.23022153064166,2.36567072244939,16.6977684436592));
#64252=CARTESIAN_POINT('Ctrl Pts',(-0.773879391910806,3.15775184736984,
16.856329888068));
#64253=CARTESIAN_POINT('Ctrl Pts',(-3.07133005340451,1.06640411938725,17.0148913324767));
#64254=CARTESIAN_POINT('Ctrl Pts',(-2.56426594590169,-1.99870613184649,
17.1734527768855));
#64255=CARTESIAN_POINT('Ctrl Pts',(0.28429894200228,-3.23874360738362,17.3320142212942));
#64256=CARTESIAN_POINT('Ctrl Pts',(2.873262755521,-1.52139645737976,17.4905756657029));
#64257=CARTESIAN_POINT('Ctrl Pts',(2.83857242150387,1.58517905949756,17.6491371101117));
#64258=CARTESIAN_POINT('Ctrl Pts',(0.211904624774947,3.24428458566613,17.8076985545204));
#64259=CARTESIAN_POINT('Ctrl Pts',(-2.60825903187995,1.94094586874764,17.9662599989292));
#64260=CARTESIAN_POINT('Ctrl Pts',(-3.04675062819489,-1.13472316112164,
18.124821443338));
#64261=CARTESIAN_POINT('Ctrl Pts',(-0.703171595288318,-3.17424569785823,
18.2833828877467));
#64262=CARTESIAN_POINT('Ctrl Pts',(2.28249249192199,-2.3152783994828,18.4419443321555));
#64263=CARTESIAN_POINT('Ctrl Pts',(3.18395078150948,0.657832397892554,18.6005057765642));
#64264=CARTESIAN_POINT('Ctrl Pts',(1.17805726089236,3.03025859174602,18.759067220973));
#64265=CARTESIAN_POINT('Ctrl Pts',(-1.9035522946178,2.63567348213832,18.9176286653817));
#64266=CARTESIAN_POINT('Ctrl Pts',(-3.24697662386251,-0.165616565844775,
19.0761901097904));
#64267=CARTESIAN_POINT('Ctrl Pts',(-1.62549853693258,-2.8156776358848,19.2347515541992));
#64268=CARTESIAN_POINT('Ctrl Pts',(1.48026634905252,-2.89466709288903,19.393312998608));
#64269=CARTESIAN_POINT('Ctrl Pts',(3.23435988556329,-0.330457521401717,
19.5518744430167));
#64270=CARTESIAN_POINT('Ctrl Pts',(2.03507169181765,2.53550177518263,19.7104358874255));
#64271=CARTESIAN_POINT('Ctrl Pts',(-1.02249565670092,3.08622563575957,19.8689973318342));
#64272=CARTESIAN_POINT('Ctrl Pts',(-3.14639449008423,0.818833167110018,
20.027558776243));
#64273=CARTESIAN_POINT('Ctrl Pts',(-2.39723518152376,-2.1962580739195,20.1861202206517));
#64274=CARTESIAN_POINT('Ctrl Pts',(0.540904586459818,-3.20588650315923,
20.3446816650605));
#64275=CARTESIAN_POINT('Ctrl Pts',(2.98512970672818,-1.2881330198395,20.5032431094692));
#64276=CARTESIAN_POINT('Ctrl Pts',(2.70355193238106,1.80584965922154,20.661804553878));
#64277=CARTESIAN_POINT('Ctrl Pts',(-0.0467124341827413,3.25086203818072,
20.8203659982867));
#64278=CARTESIAN_POINT('Ctrl Pts',(-2.75432241021104,1.72742412377537,20.9789274426955));
#64279=CARTESIAN_POINT('Ctrl Pts',(-2.94688589377513,-1.37337160734485,
21.1374888871042));
#64280=CARTESIAN_POINT('Ctrl Pts',(-0.448567945537823,-3.22010447672553,
21.296050331513));
#64281=CARTESIAN_POINT('Ctrl Pts',(2.45934955933615,-2.12647261627913,21.4546117759217));
#64282=CARTESIAN_POINT('Ctrl Pts',(3.1215682818087,0.908899061941314,21.6131732203305));
#64283=CARTESIAN_POINT('Ctrl Pts',(0.933398346422899,3.11433035654325,21.7717346647392));
#64284=CARTESIAN_POINT('Ctrl Pts',(-2.10708293368412,2.47598213914579,21.930296109148));
#64285=CARTESIAN_POINT('Ctrl Pts',(-3.22352964106027,-0.423252520367754,
22.0888575535567));
#64286=CARTESIAN_POINT('Ctrl Pts',(-1.39648400816177,-2.93600382454456,
22.2474189979655));
#64287=CARTESIAN_POINT('Ctrl Pts',(1.70572904649132,-2.76781040946589,22.4059804423742));
#64288=CARTESIAN_POINT('Ctrl Pts',(3.25039464788761,-0.0722542439966821,
22.564541886783));
#64289=CARTESIAN_POINT('Ctrl Pts',(1.82703674267198,2.68927923126595,22.7231033311917));
#64290=CARTESIAN_POINT('Ctrl Pts',(-1.26463796315678,2.99515890478861,22.8816647756005));
#64291=CARTESIAN_POINT('Ctrl Pts',(-3.20153744670834,0.56607775094599,23.0402262200092));
#64292=CARTESIAN_POINT('Ctrl Pts',(-2.21502625909608,-2.37990434982304,
23.198787664418));
#64293=CARTESIAN_POINT('Ctrl Pts',(0.79408547920078,-3.15273124362265,23.3573491088267));
#64294=CARTESIAN_POINT('Ctrl Pts',(3.07809623012716,-1.04671373396402,23.5159105532355));
#64295=CARTESIAN_POINT('Ctrl Pts',(2.55141383258672,2.01508647399485,23.6744719976443));
#64296=CARTESIAN_POINT('Ctrl Pts',(-0.305033732126069,3.23685657159181,
23.833033442053));
#64297=CARTESIAN_POINT('Ctrl Pts',(-2.88294672324543,1.50296514720743,23.9915948864617));
#64298=CARTESIAN_POINT('Ctrl Pts',(-2.82836287326186,-1.60332451485834,
24.1501563308705));
#64299=CARTESIAN_POINT('Ctrl Pts',(-0.191124175958415,-3.24557507880439,
24.3087177752792));
#64300=CARTESIAN_POINT('Ctrl Pts',(2.6206351898722,-1.92420301537947,24.4672792196881));
#64301=CARTESIAN_POINT('Ctrl Pts',(3.03942148984757,1.15421100750453,24.6258406640967));
#64302=CARTESIAN_POINT('Ctrl Pts',(0.682829595599215,3.17868365619569,24.7844021085055));
#64303=CARTESIAN_POINT('Ctrl Pts',(-2.29727252134343,2.30061404965549,24.9429635529143));
#64304=CARTESIAN_POINT('Ctrl Pts',(-3.17967279495086,-0.678208640346959,
25.101524997323));
#64305=CARTESIAN_POINT('Ctrl Pts',(-1.15862760390318,-3.03774062722042,
25.2600864417318));
#64306=CARTESIAN_POINT('Ctrl Pts',(1.92039187529098,-2.62342926112145,25.4186478861405));
#64307=CARTESIAN_POINT('Ctrl Pts',(3.24584945040241,0.186406513068115,25.5772093305493));
#64308=CARTESIAN_POINT('Ctrl Pts',(1.60743386199557,2.82602944466292,25.735770774958));
#64309=CARTESIAN_POINT('Ctrl Pts',(-1.49877318085119,2.88512824587626,25.8943322193668));
#64310=CARTESIAN_POINT('Ctrl Pts',(-3.23640978418636,0.309738198507568,
26.0528936637755));
#64311=CARTESIAN_POINT('Ctrl Pts',(-2.01879283923732,-2.54848219829688,
26.2114551081843));
#64312=CARTESIAN_POINT('Ctrl Pts',(1.04223859869649,-3.07961438270751,26.370016552593));
#64313=CARTESIAN_POINT('Ctrl Pts',(3.15157370571249,-0.798667152356616,
26.5285779970018));
#64314=CARTESIAN_POINT('Ctrl Pts',(2.38312138852957,2.21156471538246,26.6871394414106));
#64315=CARTESIAN_POINT('Ctrl Pts',(-0.561423700914708,3.20235686188205,
26.8457008858193));
#64316=CARTESIAN_POINT('Ctrl Pts',(-2.99331758273818,1.26899010699941,27.0042623302281));
#64317=CARTESIAN_POINT('Ctrl Pts',(-2.69193199829888,-1.82312593073724,
27.1628237746367));
#64318=CARTESIAN_POINT('Ctrl Pts',(0.0675297014036026,-3.25049623630303,
27.3213852190456));
#64319=CARTESIAN_POINT('Ctrl Pts',(2.7653281992882,-1.70975027211967,27.4799466634543));
#64320=CARTESIAN_POINT('Ctrl Pts',(2.93803052021534,1.39221503550097,27.6385081078631));
#64321=CARTESIAN_POINT('Ctrl Pts',(0.427937491104215,3.22291103608202,27.7970695522718));
#64322=CARTESIAN_POINT('Ctrl Pts',(-2.47291686718377,2.11067956137115,27.9556309966806));
#64323=CARTESIAN_POINT('Ctrl Pts',(-3.11568376631709,-0.928870664355431,
28.1141924410893));
#64324=CARTESIAN_POINT('Ctrl Pts',(-0.91343531828079,-3.12024389465136,
28.2727538854981));
#64325=CARTESIAN_POINT('Ctrl Pts',(2.12289569206488,-2.4624378009209,28.4313153299068));
#64326=CARTESIAN_POINT('Ctrl Pts',(3.22075307114599,0.443887032357858,28.5898767743156));
#64327=CARTESIAN_POINT('Ctrl Pts',(1.37765347124425,2.9448865777752,28.7484382187243));
#64328=CARTESIAN_POINT('Ctrl Pts',(-1.72341887645161,2.75683032105391,28.9069996631331));
#64329=CARTESIAN_POINT('Ctrl Pts',(-3.25079070738982,0.0514375304609387,
29.0655611075418));
#64330=CARTESIAN_POINT('Ctrl Pts',(-1.80977737904317,-2.70092426422798,
29.2241225519506));
#64331=CARTESIAN_POINT('Ctrl Pts',(1.28379275689769,-2.98699886175553,29.3826839963593));
#64332=CARTESIAN_POINT('Ctrl Pts',(3.20509690890129,-0.545563788519015,
29.541245440768));
#64333=CARTESIAN_POINT('Ctrl Pts',(2.19974014827687,2.39404037619475,29.6998068851769));
#64334=CARTESIAN_POINT('Ctrl Pts',(-0.814259000670061,3.14758134487732,
29.8583683295855));
#64335=CARTESIAN_POINT('Ctrl Pts',(-3.08473617266887,1.02698042231591,30.0169297739943));
#64336=CARTESIAN_POINT('Ctrl Pts',(-2.53845708458481,-2.03138417649469,
30.1754912184031));
#64337=CARTESIAN_POINT('Ctrl Pts',(0.325756012672393,-3.23483679078243,
30.3340526628118));
#64338=CARTESIAN_POINT('Ctrl Pts',(2.89251245996244,-1.48447219972415,30.4926141072206));
#64339=CARTESIAN_POINT('Ctrl Pts',(2.81803733252187,1.62140421712322,30.6511755516294));
#64340=CARTESIAN_POINT('Ctrl Pts',(0.170335889049024,3.24673246937499,30.8097369960381));
#64341=CARTESIAN_POINT('Ctrl Pts',(-2.63290387437695,1.9073812495363,30.9682984404469));
#64342=CARTESIAN_POINT('Ctrl Pts',(-3.03196770338867,-1.17365151914861,
31.1268598848556));
#64343=CARTESIAN_POINT('Ctrl Pts',(-0.66245959274568,-3.18299125521435,
31.2854213292644));
#64344=CARTESIAN_POINT('Ctrl Pts',(2.31195833853325,-2.28585535055883,31.4439827736731));
#64345=CARTESIAN_POINT('Ctrl Pts',(3.17526440850837,0.698557069144588,31.6025442180818));
#64346=CARTESIAN_POINT('Ctrl Pts',(1.13915043104843,3.04509808351621,31.7611056624906));
#64347=CARTESIAN_POINT('Ctrl Pts',(-1.93715269978589,2.61107745203088,31.9196671068993));
#64348=CARTESIAN_POINT('Ctrl Pts',(-3.24458916312253,-0.207188815672271,
32.0782285513081));
#64349=CARTESIAN_POINT('Ctrl Pts',(-1.58930326543629,-2.83626535663808,
32.2367899957168));
#64350=CARTESIAN_POINT('Ctrl Pts',(1.51721854725351,-2.87547107839077,32.3953514401256));
#64351=CARTESIAN_POINT('Ctrl Pts',(3.23832695611484,-0.289006173103491,
32.5539128845344));
#64352=CARTESIAN_POINT('Ctrl Pts',(2.00243119500863,2.5613581069519,32.7124743289431));
#64353=CARTESIAN_POINT('Ctrl Pts',(-1.06193879799461,3.07287683321437,32.8710357733519));
#64354=CARTESIAN_POINT('Ctrl Pts',(-3.15662367381384,0.778468383885889,
33.0295972177606));
#64355=CARTESIAN_POINT('Ctrl Pts',(-2.36890986260109,-2.22678065953139,
33.1881586621693));
#64356=CARTESIAN_POINT('Ctrl Pts',(0.581919791118306,-3.19869589043669,
33.3467201065781));
#64357=CARTESIAN_POINT('Ctrl Pts',(3.00138270137967,-1.24979515227539,33.5052815509869));
#64358=CARTESIAN_POINT('Ctrl Pts',(2.68020166681331,1.84032743499706,33.6638429953956));
#64359=CARTESIAN_POINT('Ctrl Pts',(-0.0883441991993578,3.24999713003858,
33.8224044398044));
#64360=CARTESIAN_POINT('Ctrl Pts',(-2.77622058094945,1.69200630279757,33.9809658842131));
#64361=CARTESIAN_POINT('Ctrl Pts',(-2.92905465663503,-1.41100136826097,
34.1395273286219));
#64362=CARTESIAN_POINT('Ctrl Pts',(-0.4072894867529,-3.22558542233326,34.2980887730306));
#64363=CARTESIAN_POINT('Ctrl Pts',(2.48638275954405,-2.09479994649826,34.4566502174393));
#64364=CARTESIAN_POINT('Ctrl Pts',(3.10967147515819,0.948804173347135,34.6152116618481));
#64365=CARTESIAN_POINT('Ctrl Pts',(0.893434829731745,3.12602947007818,34.7737731062569));
#64366=CARTESIAN_POINT('Ctrl Pts',(-2.13862138950371,2.44879247696718,34.9323345506656));
#64367=CARTESIAN_POINT('Ctrl Pts',(-3.21784441660045,-0.464503340348162,
35.0908959950743));
#64368=CARTESIAN_POINT('Ctrl Pts',(-1.35876643615622,-2.95364855978295,
35.2494574394831));
#64369=CARTESIAN_POINT('Ctrl Pts',(1.74103802828354,-2.7457371737902,35.4080188838919));
#64370=CARTESIAN_POINT('Ctrl Pts',(3.25105345024931,-0.0306187073285951,
35.5665803283006));
#64371=CARTESIAN_POINT('Ctrl Pts',(1.79244379593166,2.71245853078226,35.7251417727094));
#64372=CARTESIAN_POINT('Ctrl Pts',(-1.30289490234511,2.97871632092147,35.8837032171181));
#64373=CARTESIAN_POINT('Ctrl Pts',(-3.20852492730738,0.525027451435503,
36.0422646615269));
#64374=CARTESIAN_POINT('Ctrl Pts',(-2.18436382745606,-2.40807822025996,
36.2008261059356));
#64375=CARTESIAN_POINT('Ctrl Pts',(0.834399133536698,-3.14230236534719,
36.3593875503444));
#64376=CARTESIAN_POINT('Ctrl Pts',(3.0912496000529,-1.00720498796545,36.5179489947531));
#64377=CARTESIAN_POINT('Ctrl Pts',(2.52539624980007,2.04759855999854,36.6765104391619));
#64378=CARTESIAN_POINT('Ctrl Pts',(-0.346464965372859,3.23268436872066,
36.8350718835706));
#64379=CARTESIAN_POINT('Ctrl Pts',(-2.90195951315509,1.4659183333937,36.9936333279794));
#64380=CARTESIAN_POINT('Ctrl Pts',(-2.8075963376437,-1.63941734862674,37.1521947723881));
#64381=CARTESIAN_POINT('Ctrl Pts',(-0.149540397343195,-3.24775685532027,
37.3107562167969));
#64382=CARTESIAN_POINT('Ctrl Pts',(2.64506416393096,-1.89048098364498,37.4693176612057));
#64383=CARTESIAN_POINT('Ctrl Pts',(3.02439037266604,1.19304336942204,37.6278791056144));
#64384=CARTESIAN_POINT('Ctrl Pts',(0.642060899189524,3.187169328306,37.7864405500232));
#64385=CARTESIAN_POINT('Ctrl Pts',(-2.32654643543915,2.27100098025149,37.9450019944319));
#64386=CARTESIAN_POINT('Ctrl Pts',(-3.1707313472868,-0.7188731726267,38.1035634388407));
#64387=CARTESIAN_POINT('Ctrl Pts',(-1.11961596237772,-3.05233767503222,
38.2621248832494));
#64388=CARTESIAN_POINT('Ctrl Pts',(1.95381389621675,-2.59860517442575,38.4206863276582));
#64389=CARTESIAN_POINT('Ctrl Pts',(3.24323432642311,0.227937078525055,38.5792477720669));
#64390=CARTESIAN_POINT('Ctrl Pts',(1.57103400689371,2.8464336890225,38.7378092164756));
#64391=CARTESIAN_POINT('Ctrl Pts',(-1.5354614779569,2.86560299052469,38.8963706608845));
#64392=CARTESIAN_POINT('Ctrl Pts',(-3.24037889329957,0.268439772418473,
39.0549321052931));
#64393=CARTESIAN_POINT('Ctrl Pts',(-1.98547656045168,-2.5744679378351,39.213493549702));
#64394=CARTESIAN_POINT('Ctrl Pts',(1.08061773167372,-3.06536358105226,39.3720549941106));
#64395=CARTESIAN_POINT('Ctrl Pts',(3.16343569691019,-0.759503007488255,
39.5306164385195));
#64396=CARTESIAN_POINT('Ctrl Pts',(2.35076410763942,2.24454370995285,39.6891778829282));
#64397=CARTESIAN_POINT('Ctrl Pts',(0.388177431307865,2.87359516469282,39.794885512534));
#64398=CARTESIAN_POINT('Ctrl Pts',(-0.509883685250365,2.70426773226936,
39.8477393273369));
#64399=CARTESIAN_POINT('Ctrl Pts',(-1.28892185405299,2.64462557919729,-1.41553435639707E-14));
#64400=CARTESIAN_POINT('Ctrl Pts',(-2.1671763893535,2.21658711777033,0.0528538148029031));
#64401=CARTESIAN_POINT('Ctrl Pts',(-3.44873566164522,0.424356070443797,
0.158561444408738));
#64402=CARTESIAN_POINT('Ctrl Pts',(-2.22812647145566,-2.67063343433409,
0.317122888817489));
#64403=CARTESIAN_POINT('Ctrl Pts',(1.02996089584317,-3.31861020338198,0.475684333226241));
#64404=CARTESIAN_POINT('Ctrl Pts',(3.34606623809502,-0.940467179645626,
0.634245777634992));
#64405=CARTESIAN_POINT('Ctrl Pts',(2.60756871412969,2.29861656481967,0.792807222043744));
#64406=CARTESIAN_POINT('Ctrl Pts',(-0.51237942709981,3.43763407819966,0.951368666452495));
#64407=CARTESIAN_POINT('Ctrl Pts',(-3.16424575535823,1.43825034235358,1.10993011086125));
#64408=CARTESIAN_POINT('Ctrl Pts',(-2.92686575687285,-1.87475093929392,
1.26849155527));
#64409=CARTESIAN_POINT('Ctrl Pts',(-0.0168264060382829,-3.47570269831962,
1.42705299967875));
#64410=CARTESIAN_POINT('Ctrl Pts',(2.90854674895906,-1.9029817991733,1.5856144440875));
#64411=CARTESIAN_POINT('Ctrl Pts',(3.17806315019492,1.40744832765037,1.74417588849625));
#64412=CARTESIAN_POINT('Ctrl Pts',(0.545595424907332,3.43267566409904,1.90273733290501));
#64413=CARTESIAN_POINT('Ctrl Pts',(-2.5850658396409,2.32344609757596,2.06129877731376));
#64414=CARTESIAN_POINT('Ctrl Pts',(-3.35523570384725,-0.907391583655662,
2.21986022172251));
#64415=CARTESIAN_POINT('Ctrl Pts',(-1.06164763020298,-3.30966201013354,
2.37842166613126));
#64416=CARTESIAN_POINT('Ctrl Pts',(2.2013590481941,-2.68979207108213,2.53698311054001));
#64417=CARTESIAN_POINT('Ctrl Pts',(3.45424541186603,0.386200888946397,2.69554455494876));
#64418=CARTESIAN_POINT('Ctrl Pts',(1.55296643213827,3.1095428550715,2.85410599935752));
#64419=CARTESIAN_POINT('Ctrl Pts',(-1.76636822259782,2.99347716244134,3.01266744376627));
#64420=CARTESIAN_POINT('Ctrl Pts',(-3.47278419601471,0.143986152923845,
3.17122888817502));
#64421=CARTESIAN_POINT('Ctrl Pts',(-2.00810670974327,-2.83698244759632,
3.32979033258377));
#64422=CARTESIAN_POINT('Ctrl Pts',(1.29022746160673,-3.2274254705277,3.48835177699252));
#64423=CARTESIAN_POINT('Ctrl Pts',(3.41041995257781,-0.670818746338501,
3.64691322140127));
#64424=CARTESIAN_POINT('Ctrl Pts',(2.41646548755533,2.49833075822444,3.80547466581002));
#64425=CARTESIAN_POINT('Ctrl Pts',(-0.784029148963742,3.3861866957775,3.96403611021878));
#64426=CARTESIAN_POINT('Ctrl Pts',(-3.26860550698802,1.18202372220942,4.12259755462753));
#64427=CARTESIAN_POINT('Ctrl Pts',(-2.76852952853711,-2.10147716819809,
4.28115899903628));
#64428=CARTESIAN_POINT('Ctrl Pts',(0.25956584715683,-3.46606226313663,4.43972044344503));
#64429=CARTESIAN_POINT('Ctrl Pts',(3.05064460829658,-1.66569190247976,4.59828188785378));
#64430=CARTESIAN_POINT('Ctrl Pts',(3.05609704130031,1.65566690918397,4.75684333226253));
#64431=CARTESIAN_POINT('Ctrl Pts',(0.270944381832366,3.46519136300629,4.91540477667129));
#64432=CARTESIAN_POINT('Ctrl Pts',(-2.7616149409627,2.11055560410422,5.07396622108003));
#64433=CARTESIAN_POINT('Ctrl Pts',(-3.27246876367335,-1.17128571704109,
5.23252766548879));
#64434=CARTESIAN_POINT('Ctrl Pts',(-0.795142605983985,-3.3835942836501,
5.39108910989755));
#64435=CARTESIAN_POINT('Ctrl Pts',(2.40824983021483,-2.50625114373032,5.54965055430628));
#64436=CARTESIAN_POINT('Ctrl Pts',(3.41260403254196,0.659617887309973,5.70821199871505));
#64437=CARTESIAN_POINT('Ctrl Pts',(1.30081693986578,3.22317193601956,5.86677344312379));
#64438=CARTESIAN_POINT('Ctrl Pts',(-1.99878137992741,2.84356027462723,6.02533488753255));
#64439=CARTESIAN_POINT('Ctrl Pts',(-3.47323821296028,-0.132583393438264,
6.1838963319413));
#64440=CARTESIAN_POINT('Ctrl Pts',(-1.77618703639565,-2.98766156917474,
6.34245777635005));
#64441=CARTESIAN_POINT('Ctrl Pts',(1.54274869489151,-3.11462493802925,6.5010192207588));
#64442=CARTESIAN_POINT('Ctrl Pts',(3.45295875214133,-0.397539804540268,
6.65958066516755));
#64443=CARTESIAN_POINT('Ctrl Pts',(2.21017852546455,2.68254970611146,6.81814210957631));
#64444=CARTESIAN_POINT('Ctrl Pts',(-1.05077565484297,3.31313032695253,6.97670355398506));
#64445=CARTESIAN_POINT('Ctrl Pts',(-3.35223808673274,0.918401791179546,
7.13526499839381));
#64446=CARTESIAN_POINT('Ctrl Pts',(-2.5926810059155,-2.31494432800193,7.29382644280256));
#64447=CARTESIAN_POINT('Ctrl Pts',(0.53432341724346,-3.43445199791299,7.45238788721131));
#64448=CARTESIAN_POINT('Ctrl Pts',(3.17342263678587,-1.41786840310318,7.61094933162007));
#64449=CARTESIAN_POINT('Ctrl Pts',(2.91478358060356,1.89340928444624,7.76951077602881));
#64450=CARTESIAN_POINT('Ctrl Pts',(-0.00542341457961224,3.47576360340539,
7.92807222043756));
#64451=CARTESIAN_POINT('Ctrl Pts',(-2.92067814282227,1.88430391026066,8.08663366484632));
#64452=CARTESIAN_POINT('Ctrl Pts',(-3.16898244743632,-1.42776478735954,
8.24519510925507));
#64453=CARTESIAN_POINT('Ctrl Pts',(-0.523602933642665,-3.43610273537683,
8.40375655366383));
#64454=CARTESIAN_POINT('Ctrl Pts',(2.59989261944251,-2.30684208552552,8.56231799807257));
#64455=CARTESIAN_POINT('Ctrl Pts',(3.34935571028899,0.928858636250884,8.72087944248133));
#64456=CARTESIAN_POINT('Ctrl Pts',(1.04043126453191,3.31639334578512,8.87944088689007));
#64457=CARTESIAN_POINT('Ctrl Pts',(-2.21853918630074,2.67563934771326,9.03800233129883));
#64458=CARTESIAN_POINT('Ctrl Pts',(-3.45170133734449,-0.408313504500715,
9.19656377570758));
#64459=CARTESIAN_POINT('Ctrl Pts',(-1.53302138401484,-3.11942422192565,
9.35512522011632));
#64460=CARTESIAN_POINT('Ctrl Pts',(1.78550197197721,-2.98210408072033,9.51368666452509));
#64461=CARTESIAN_POINT('Ctrl Pts',(3.47363505293783,-0.121743826064997,
9.67224810893383));
#64462=CARTESIAN_POINT('Ctrl Pts',(1.98989775895469,2.84978401797231,9.83080955334259));
#64463=CARTESIAN_POINT('Ctrl Pts',(-1.31086914654657,3.21909678649394,9.98937099775133));
#64464=CARTESIAN_POINT('Ctrl Pts',(-3.41464588238613,0.6489649744684,10.1479324421601));
#64465=CARTESIAN_POINT('Ctrl Pts',(-2.40041685475204,-2.51375435625792,
10.3064938865688));
#64466=CARTESIAN_POINT('Ctrl Pts',(0.805697904419769,-3.38109640900654,
10.4650553309776));
#64467=CARTESIAN_POINT('Ctrl Pts',(3.2761080558142,-1.1610676323163,10.6236167753863));
#64468=CARTESIAN_POINT('Ctrl Pts',(2.75501509044826,2.1191634886402,10.7821782197951));
#64469=CARTESIAN_POINT('Ctrl Pts',(-0.281756872492634,3.46432895449993,
10.9407396642038));
#64470=CARTESIAN_POINT('Ctrl Pts',(-3.06124899366075,1.64612169628929,11.0993011086126));
#64471=CARTESIAN_POINT('Ctrl Pts',(-3.04543163489178,-1.67520392710372,
11.2578625530213));
#64472=CARTESIAN_POINT('Ctrl Pts',(-0.248748055458642,-3.46685541162145,
11.4164239974301));
#64473=CARTESIAN_POINT('Ctrl Pts',(2.77507411968471,-2.09282719555137,11.5749854418389));
#64474=CARTESIAN_POINT('Ctrl Pts',(3.26490085363842,1.19221829213213,11.7335468862476));
#64475=CARTESIAN_POINT('Ctrl Pts',(0.773458071087839,3.38861692323762,11.8921083306564));
#64476=CARTESIAN_POINT('Ctrl Pts',(-2.42425025305144,2.49077753939675,12.0506697750651));
#64477=CARTESIAN_POINT('Ctrl Pts',(-3.40830992328265,-0.681458367793936,
12.2092312194739));
#64478=CARTESIAN_POINT('Ctrl Pts',(-1.2801493661345,-3.23143615758826,12.3677926638826));
#64479=CARTESIAN_POINT('Ctrl Pts',(2.01695029603303,-2.83070195243435,12.5263541082914));
#64480=CARTESIAN_POINT('Ctrl Pts',(3.47231794138706,0.154822976669773,12.6849155527001));
#64481=CARTESIAN_POINT('Ctrl Pts',(1.75701790207559,2.99897484683836,12.8434769971089));
#64482=CARTESIAN_POINT('Ctrl Pts',(-1.56266283552656,3.10468144946425,13.0020384415176));
#64483=CARTESIAN_POINT('Ctrl Pts',(-3.45543375718812,0.375419218831596,
13.1605998859264));
#64484=CARTESIAN_POINT('Ctrl Pts',(-2.19295440069049,-2.69664848222298,
13.3191613303351));
#64485=CARTESIAN_POINT('Ctrl Pts',(1.07197109397293,-3.30633331862803,13.4777227747439));
#64486=CARTESIAN_POINT('Ctrl Pts',(3.35805070990966,-0.896915531061065,
13.6362842191526));
#64487=CARTESIAN_POINT('Ctrl Pts',(2.57780314927297,2.33150015307347,13.7948456635614));
#64488=CARTESIAN_POINT('Ctrl Pts',(-0.556306379304298,3.43095981505594,
13.9534071079701));
#64489=CARTESIAN_POINT('Ctrl Pts',(-3.18243746540957,1.39751701919542,14.1119685523789));
#64490=CARTESIAN_POINT('Ctrl Pts',(-2.90259859128356,-1.91203646881067,
14.2705299967876));
#64491=CARTESIAN_POINT('Ctrl Pts',(0.0276817776273479,-3.47565760099736,
14.4290914411964));
#64492=CARTESIAN_POINT('Ctrl Pts',(2.93268516463204,-1.86556151475381,14.5876528856051));
#64493=CARTESIAN_POINT('Ctrl Pts',(3.15977419075238,1.44802938631728,14.7462143300139));
#64494=CARTESIAN_POINT('Ctrl Pts',(0.501587707379338,3.43938538288301,14.9047757744226));
#64495=CARTESIAN_POINT('Ctrl Pts',(-2.61461211511146,2.29014530711388,15.0633372188314));
#64496=CARTESIAN_POINT('Ctrl Pts',(-3.34333870466228,-0.950288559381016,
15.2218986632402));
#64497=CARTESIAN_POINT('Ctrl Pts',(-1.01917204863389,-3.32298816962486,
15.3804601076489));
#64498=CARTESIAN_POINT('Ctrl Pts',(2.23562824586454,-2.66137715975695,15.5390215520576));
#64499=CARTESIAN_POINT('Ctrl Pts',(3.44901575681568,0.430409513626772,15.6975829964664));
#64500=CARTESIAN_POINT('Ctrl Pts',(1.51301343980967,3.12917758702485,15.8561444408751));
#64501=CARTESIAN_POINT('Ctrl Pts',(-1.8045624833716,2.97060873960054,16.0147058852839));
#64502=CARTESIAN_POINT('Ctrl Pts',(-3.47434346162898,0.099496486466701,
16.1732673296926));
#64503=CARTESIAN_POINT('Ctrl Pts',(-1.97160719775406,-2.86246870689406,
16.3318287741014));
#64504=CARTESIAN_POINT('Ctrl Pts',(1.33145707015024,-3.21063609126451,16.4903902185102));
#64505=CARTESIAN_POINT('Ctrl Pts',(3.41873177698731,-0.627084585363457,
16.6489516629189));
#64506=CARTESIAN_POINT('Ctrl Pts',(2.38426977917728,2.52907486253082,16.8075131073277));
#64507=CARTESIAN_POINT('Ctrl Pts',(-0.827333617539956,3.37586746266372,
16.9660745517364));
#64508=CARTESIAN_POINT('Ctrl Pts',(-3.28347625004977,1.14006392607712,17.1246359961451));
#64509=CARTESIAN_POINT('Ctrl Pts',(-2.74138766781067,-2.13676290096935,
17.2831974405539));
#64510=CARTESIAN_POINT('Ctrl Pts',(0.303936342805055,-3.4624535722094,17.4417588849627));
#64511=CARTESIAN_POINT('Ctrl Pts',(3.07172783577854,-1.62648398181063,17.6003203293714));
#64512=CARTESIAN_POINT('Ctrl Pts',(3.03464133388157,1.69467224408758,17.7588817737802));
#64513=CARTESIAN_POINT('Ctrl Pts',(0.226541527815518,3.46837728287428,17.9174432181889));
#64514=CARTESIAN_POINT('Ctrl Pts',(-2.78841949130883,2.07501295915769,18.0760046625977));
#64515=CARTESIAN_POINT('Ctrl Pts',(-3.25719904847505,-1.21310197378316,
18.2345661070064));
#64516=CARTESIAN_POINT('Ctrl Pts',(-0.751741816311538,-3.3935005940462,
18.3931275514152));
#64517=CARTESIAN_POINT('Ctrl Pts',(2.44015125624008,-2.47520178709804,18.5516889958239));
#64518=CARTESIAN_POINT('Ctrl Pts',(3.40387603762256,0.703270901347592,18.7102504402327));
#64519=CARTESIAN_POINT('Ctrl Pts',(1.25942929287289,3.23956785643348,18.8688118846414));
#64520=CARTESIAN_POINT('Ctrl Pts',(-2.03503649605394,2.8177275418166,19.0273733290502));
#64521=CARTESIAN_POINT('Ctrl Pts',(-3.4712552684142,-0.177056210537707,
19.1859347734589));
#64522=CARTESIAN_POINT('Ctrl Pts',(-1.73777671162116,-3.01016513512639,
19.3444962178677));
#64523=CARTESIAN_POINT('Ctrl Pts',(1.58251289062026,-3.0946106364459,19.5030576622764));
#64524=CARTESIAN_POINT('Ctrl Pts',(3.45776705326368,-0.353283237003404,
19.6616191066852));
#64525=CARTESIAN_POINT('Ctrl Pts',(2.17564034182019,2.71063666750596,19.8201805510939));
#64526=CARTESIAN_POINT('Ctrl Pts',(-1.09312257106175,3.29940071601172,19.9787419955027));
#64527=CARTESIAN_POINT('Ctrl Pts',(-3.36372561784012,0.875392488012878,
20.1373034399114));
#64528=CARTESIAN_POINT('Ctrl Pts',(-2.5628195757052,-2.34796036222197,20.2958648843202));
#64529=CARTESIAN_POINT('Ctrl Pts',(0.578266526977567,-3.42732692691558,
20.4544263287289));
#64530=CARTESIAN_POINT('Ctrl Pts',(3.19132178076895,-1.37710832245438,20.6129877731377));
#64531=CARTESIAN_POINT('Ctrl Pts',(2.89029456502375,1.93058523965599,20.7715492175465));
#64532=CARTESIAN_POINT('Ctrl Pts',(-0.0499390054322844,3.4754090602287,
20.9301106619552));
#64533=CARTESIAN_POINT('Ctrl Pts',(-2.94457191563734,1.84674261168771,21.088672106364));
#64534=CARTESIAN_POINT('Ctrl Pts',(-3.15043635023577,-1.46823460090559,
21.2472335507727));
#64535=CARTESIAN_POINT('Ctrl Pts',(-0.479551910767174,-3.44252697956934,
21.4057949951815));
#64536=CARTESIAN_POINT('Ctrl Pts',(2.62922438430201,-2.27335460876106,21.5643564395902));
#64537=CARTESIAN_POINT('Ctrl Pts',(3.33718458713544,0.971679510728251,21.722917883999));
#64538=CARTESIAN_POINT('Ctrl Pts',(0.997871036008576,3.32944671614946,21.8814793284077));
#64539=CARTESIAN_POINT('Ctrl Pts',(-2.2526256212575,2.64700582746574,22.0400407728164));
#64540=CARTESIAN_POINT('Ctrl Pts',(-3.44618873052089,-0.452487871455233,
22.1986022172252));
#64541=CARTESIAN_POINT('Ctrl Pts',(-1.49294344620842,-3.13880262307247,
22.3571636616339));
#64542=CARTESIAN_POINT('Ctrl Pts',(1.82354898880575,-2.95899157241263,22.5157251060427));
#64543=CARTESIAN_POINT('Ctrl Pts',(3.47490938585301,-0.0772450664705207,
22.6742865504514));
#64544=CARTESIAN_POINT('Ctrl Pts',(1.95323578001058,2.87503600462147,22.8328479948602));
#64545=CARTESIAN_POINT('Ctrl Pts',(-1.35199039007024,3.20204372633183,22.991409439269));
#64546=CARTESIAN_POINT('Ctrl Pts',(-3.42267746778281,0.605178479223403,
23.1499708836777));
#64547=CARTESIAN_POINT('Ctrl Pts',(-2.36802492357223,-2.54429165024845,
23.3085323280865));
#64548=CARTESIAN_POINT('Ctrl Pts',(0.848935401317481,-3.37050007040103,
23.4670937724952));
#64549=CARTESIAN_POINT('Ctrl Pts',(3.29070978737274,-1.11901346527762,23.625655216904));
#64550=CARTESIAN_POINT('Ctrl Pts',(2.72764781956938,2.1542746836422,23.7842166613127));
#64551=CARTESIAN_POINT('Ctrl Pts',(-0.326103348544396,3.46043619306171,
23.9427781057215));
#64552=CARTESIAN_POINT('Ctrl Pts',(-3.08208070488623,1.60677956445533,24.1013395501302));
#64553=CARTESIAN_POINT('Ctrl Pts',(-3.02372658079627,-1.71407106176184,
24.259900994539));
#64554=CARTESIAN_POINT('Ctrl Pts',(-0.204325709597339,-3.46975691433578,
24.4184624389477));
#64555=CARTESIAN_POINT('Ctrl Pts',(2.80165050853192,-2.05711362550206,24.5770238833565));
#64556=CARTESIAN_POINT('Ctrl Pts',(3.24936366403954,1.23393590554894,24.7355853277652));
#64557=CARTESIAN_POINT('Ctrl Pts',(0.729994732248181,3.39824509579182,24.894146772174));
#64558=CARTESIAN_POINT('Ctrl Pts',(-2.45595218767254,2.45952452560444,25.0527082165827));
#64559=CARTESIAN_POINT('Ctrl Pts',(-3.39930255739772,-0.725054593429181,
25.2112696609915));
#64560=CARTESIAN_POINT('Ctrl Pts',(-1.23865756982089,-3.24756669907006,
25.3698311054002));
#64561=CARTESIAN_POINT('Ctrl Pts',(2.05303923826652,-2.80463757486085,25.528392549809));
#64562=CARTESIAN_POINT('Ctrl Pts',(3.47005023762246,0.199282183246816,25.6869539942178));
#64563=CARTESIAN_POINT('Ctrl Pts',(1.71846425412255,3.0212319751198,25.8455154386265));
#64564=CARTESIAN_POINT('Ctrl Pts',(-1.6022980461125,3.08441291198299,26.0040768830352));
#64565=CARTESIAN_POINT('Ctrl Pts',(-3.45995854467842,0.331132766862739,
26.162638327444));
#64566=CARTESIAN_POINT('Ctrl Pts',(-2.15823705891142,-2.7245136882983,26.3211997718528));
#64567=CARTESIAN_POINT('Ctrl Pts',(1.11422921867739,-3.29233280341293,26.4797612162615));
#64568=CARTESIAN_POINT('Ctrl Pts',(3.3692625777935,-0.853833544705057,26.6383226606703));
#64569=CARTESIAN_POINT('Ctrl Pts',(2.54773089969555,2.36432428040652,26.796884105079));
#64570=CARTESIAN_POINT('Ctrl Pts',(-0.600202959667374,3.42355348247838,
26.9554455494878));
#64571=CARTESIAN_POINT('Ctrl Pts',(-3.20007521851407,1.35664314985023,27.1140069938965));
#64572=CARTESIAN_POINT('Ctrl Pts',(-2.87787200641801,-1.94905483628834,
27.2725684383053));
#64573=CARTESIAN_POINT('Ctrl Pts',(0.072194185215024,-3.47501799129219,
27.431129882714));
#64574=CARTESIAN_POINT('Ctrl Pts',(2.95633790835697,-1.8278479728344,27.5896913271228));
#64575=CARTESIAN_POINT('Ctrl Pts',(3.1409693088357,1.48837960249914,27.7482527715315));
#64576=CARTESIAN_POINT('Ctrl Pts',(0.457496447504475,3.44552739659752,27.9068142159403));
#64577=CARTESIAN_POINT('Ctrl Pts',(-2.64372882775816,2.25647067906141,28.065375660349));
#64578=CARTESIAN_POINT('Ctrl Pts',(-3.33089361009169,-0.993030613039605,
28.2239371047578));
#64579=CARTESIAN_POINT('Ctrl Pts',(-0.976529100220519,-3.33576872049095,
28.3824985491665));
#64580=CARTESIAN_POINT('Ctrl Pts',(2.26953061540928,-2.63252594021469,28.5410599935753));
#64581=CARTESIAN_POINT('Ctrl Pts',(3.44322037439778,0.474547672542312,28.699621437984));
#64582=CARTESIAN_POINT('Ctrl Pts',(1.4728122262909,3.14829893534133,28.8581828823928));
#64583=CARTESIAN_POINT('Ctrl Pts',(-1.84246070963419,2.94725305558204,29.0167443268015));
#64584=CARTESIAN_POINT('Ctrl Pts',(-3.47533280240106,0.0549904786176304,
29.1753057712103));
#64585=CARTESIAN_POINT('Ctrl Pts',(-1.93478425914477,-2.88748539576375,
29.333867215619));
#64586=CARTESIAN_POINT('Ctrl Pts',(1.3724682642255,-3.1933200440728,29.4924286600278));
#64587=CARTESIAN_POINT('Ctrl Pts',(3.42648279295799,-0.583247554427895,
29.6509901044365));
#64588=CARTESIAN_POINT('Ctrl Pts',(2.35168295414604,2.55940409536327,29.8095515488453));
#64589=CARTESIAN_POINT('Ctrl Pts',(-0.870502369853091,3.36499445233771,
29.968112993254));
#64590=CARTESIAN_POINT('Ctrl Pts',(-3.29780837113232,1.0979171132071,30.1266744376629));
#64591=CARTESIAN_POINT('Ctrl Pts',(-2.71379610920208,-2.17169811849229,
30.2852358820715));
#64592=CARTESIAN_POINT('Ctrl Pts',(0.348256980631351,-3.45827689979053,
30.4437973264803));
#64593=CARTESIAN_POINT('Ctrl Pts',(3.09230717640782,-1.58700925231077,30.602358770889));
#64594=CARTESIAN_POINT('Ctrl Pts',(3.01268782325502,1.73339958457198,30.7609202152978));
#64595=CARTESIAN_POINT('Ctrl Pts',(0.182101511885165,3.4709942494266,30.9194816597066));
#64596=CARTESIAN_POINT('Ctrl Pts',(-2.81476662874377,2.0391299286445,31.0780431041153));
#64597=CARTESIAN_POINT('Ctrl Pts',(-3.24139502166468,-1.25471923302017,
31.2366045485241));
#64598=CARTESIAN_POINT('Ctrl Pts',(-0.708217710755854,-3.40285023390025,
31.3951659929327));
#64599=CARTESIAN_POINT('Ctrl Pts',(2.4716523993453,-2.44374639784777,31.5537274373416));
#64600=CARTESIAN_POINT('Ctrl Pts',(3.39458967016864,0.746808550679325,31.7122888817503));
#64601=CARTESIAN_POINT('Ctrl Pts',(1.2178350488366,3.25543235746169,31.8708503261591));
#64602=CARTESIAN_POINT('Ctrl Pts',(-2.07095778436978,2.79143258839283,32.0294117705678));
#64603=CARTESIAN_POINT('Ctrl Pts',(-3.46870289843071,-0.221499983299419,
32.1879732149766));
#64604=CARTESIAN_POINT('Ctrl Pts',(-1.69908132159284,-3.03217491296225,
32.3465346593853));
#64605=CARTESIAN_POINT('Ctrl Pts',(1.62201749060475,-3.07408869428902,32.5050961037941));
#64606=CARTESIAN_POINT('Ctrl Pts',(3.46200814155826,-0.308968716810793,
32.6636575482028));
#64607=CARTESIAN_POINT('Ctrl Pts',(2.14074526568096,2.73827897549683,32.8222189926116));
#64608=CARTESIAN_POINT('Ctrl Pts',(-1.13529017122625,3.2851298706901,32.9807804370203));
#64609=CARTESIAN_POINT('Ctrl Pts',(-3.37466136269644,0.832239585280099,
33.139341881429));
#64610=CARTESIAN_POINT('Ctrl Pts',(-2.53253774003776,-2.38059123653509,
33.2979033258378));
#64611=CARTESIAN_POINT('Ctrl Pts',(0.622114777750159,-3.41963963649505,
33.4564647702466));
#64612=CARTESIAN_POINT('Ctrl Pts',(3.20869741966233,-1.33612234066947,33.6150262146553));
#64613=CARTESIAN_POINT('Ctrl Pts',(2.86533142492128,1.9674445012609,33.7735876590641));
#64614=CARTESIAN_POINT('Ctrl Pts',(-0.0944464042799534,3.47448441022565,
33.9321491034729));
#64615=CARTESIAN_POINT('Ctrl Pts',(-2.96798266026227,1.80887837307219,34.0907105478815));
#64616=CARTESIAN_POINT('Ctrl Pts',(-3.13137345479944,-1.50846356494225,
34.2492719922904));
#64617=CARTESIAN_POINT('Ctrl Pts',(-0.435422222097375,-3.44838651091826,
34.407833436699));
#64618=CARTESIAN_POINT('Ctrl Pts',(2.65812485064789,-2.23949421043432,34.5663948811079));
#64619=CARTESIAN_POINT('Ctrl Pts',(3.32446603152299,1.01434099069891,34.7249563255165));
#64620=CARTESIAN_POINT('Ctrl Pts',(0.95514711652021,3.34195392337585,34.8835177699254));
#64621=CARTESIAN_POINT('Ctrl Pts',(-2.28634253505258,2.61793809184046,35.042079214334));
#64622=CARTESIAN_POINT('Ctrl Pts',(-3.44011081015237,-0.496588012223433,
35.2006406587429));
#64623=CARTESIAN_POINT('Ctrl Pts',(-1.45262060570077,-3.15766613434814,
35.3592021031516));
#64624=CARTESIAN_POINT('Ctrl Pts',(1.86129687037896,-2.9353936705777,35.5177635475603));
#64625=CARTESIAN_POINT('Ctrl Pts',(3.47561369371654,-0.0327336354518328,
35.6763249919691));
#64626=CARTESIAN_POINT('Ctrl Pts',(1.91625339222871,2.89981636952241,35.8348864363779));
#64627=CARTESIAN_POINT('Ctrl Pts',(-1.39288985350799,3.18446540271358,35.9934478807866));
#64628=CARTESIAN_POINT('Ctrl Pts',(-3.43014759512038,0.561292709489631,
36.1520093251954));
#64629=CARTESIAN_POINT('Ctrl Pts',(-2.33524454363645,-2.57441157641824,
36.3105707696041));
#64630=CARTESIAN_POINT('Ctrl Pts',(0.892033643532763,-3.35935083748346,
36.4691322140128));
#64631=CARTESIAN_POINT('Ctrl Pts',(3.30477170094384,-1.07677572888985,36.6276936584217));
#64632=CARTESIAN_POINT('Ctrl Pts',(2.69983312245829,2.18903247924752,36.7862551028303));
#64633=CARTESIAN_POINT('Ctrl Pts',(-0.370396364277214,3.4559758033284,36.9448165472391));
#64634=CARTESIAN_POINT('Ctrl Pts',(-3.10240676656962,1.56717381346724,37.1033779916479));
#64635=CARTESIAN_POINT('Ctrl Pts',(-3.0015256368038,-1.75265693837389,37.2619394360566));
#64636=CARTESIAN_POINT('Ctrl Pts',(-0.159869611719143,-3.47208939285428,
37.4205008804654));
#64637=CARTESIAN_POINT('Ctrl Pts',(2.82776686683283,-2.02106230949944,37.5790623248741));
#64638=CARTESIAN_POINT('Ctrl Pts',(3.23329430144447,1.27545053793049,37.7376237692828));
#64639=CARTESIAN_POINT('Ctrl Pts',(0.686410016805987,3.40731689932821,37.8961852136916));
#64640=CARTESIAN_POINT('Ctrl Pts',(-2.4872481408941,2.42786599057616,38.0547466581004));
#64641=CARTESIAN_POINT('Ctrl Pts',(-3.38974349649071,-0.768527949805165,
38.2133081025091));
#64642=CARTESIAN_POINT('Ctrl Pts',(-1.19695127443843,-3.26317200979131,
38.3718695469179));
#64643=CARTESIAN_POINT('Ctrl Pts',(2.08876982079273,-2.77809881228007,38.5304309913266));
#64644=CARTESIAN_POINT('Ctrl Pts',(3.46725447900073,0.243681392370514,38.6889924357354));
#64645=CARTESIAN_POINT('Ctrl Pts',(1.6795501492709,3.04304560328413,38.8475538801441));
#64646=CARTESIAN_POINT('Ctrl Pts',(-1.6415205165428,3.0635389872962,39.0061153245529));
#64647=CARTESIAN_POINT('Ctrl Pts',(-3.46420181234437,0.28698173168576,39.1646767689616));
#64648=CARTESIAN_POINT('Ctrl Pts',(-2.12261952245961,-2.75229434265003,
39.3232382133705));
#64649=CARTESIAN_POINT('Ctrl Pts',(1.15525931620421,-3.27709765513333,39.481799657779));
#64650=CARTESIAN_POINT('Ctrl Pts',(3.3819439131429,-0.81196421210558,39.640361102188));
#64651=CARTESIAN_POINT('Ctrl Pts',(2.51313860206826,2.39958123538677,39.7989225465966));
#64652=CARTESIAN_POINT('Ctrl Pts',(0.414990038303313,3.07208320547242,39.9046301762025));
#64653=CARTESIAN_POINT('Ctrl Pts',(-0.545102916878579,2.89105980740808,
39.9574839910054));
#64654=CARTESIAN_POINT('Ctrl Pts',(-2.9422704459833,-0.00265502083472174,
38.1778238829104));
#64655=CARTESIAN_POINT('Ctrl Pts',(-2.94427742279841,-0.221182694545831,
38.18965195611));
#64656=CARTESIAN_POINT('Ctrl Pts',(-2.9219878224732,-0.439304875887155,
38.2014800293096));
#64657=CARTESIAN_POINT('Ctrl Pts',(-2.87386223354923,-0.651569636405941,
38.2133081025091));
#64658=CARTESIAN_POINT('Ctrl Pts',(-2.65881275580662,-1.60007596980054,
38.266161917312));
#64659=CARTESIAN_POINT('Ctrl Pts',(-1.92788201512251,-2.43162398979594,
38.319015732115));
#64660=CARTESIAN_POINT('Ctrl Pts',(-1.01479646224192,-2.76655246687509,
38.3718695469179));
#64661=CARTESIAN_POINT('Ctrl Pts',(-0.101710909361328,-3.10148094395424,
38.4247233617208));
#64662=CARTESIAN_POINT('Ctrl Pts',(0.993529455715749,-2.93978987811714,
38.4775771765237));
#64663=CARTESIAN_POINT('Ctrl Pts',(1.77089708128894,-2.35531431109013,38.5304309913266));
#64664=CARTESIAN_POINT('Ctrl Pts',(2.54826470686207,-1.77083874406317,38.5832848061296));
#64665=CARTESIAN_POINT('Ctrl Pts',(3.00775959293139,-0.763578675846303,
38.6361386209325));
#64666=CARTESIAN_POINT('Ctrl Pts',(2.93955631434443,0.206612060081017,38.6889924357354));
#64667=CARTESIAN_POINT('Ctrl Pts',(2.87135303575745,1.17680279600839,38.7418462505383));
#64668=CARTESIAN_POINT('Ctrl Pts',(2.27545159251423,2.10992419964619,38.7947000653412));
#64669=CARTESIAN_POINT('Ctrl Pts',(1.42398909325699,2.57990046546716,38.8475538801441));
#64670=CARTESIAN_POINT('Ctrl Pts',(0.572526593999702,3.04987673128816,38.900407694947));
#64671=CARTESIAN_POINT('Ctrl Pts',(-0.534496961271609,3.05670785929219,
38.95326150975));
#64672=CARTESIAN_POINT('Ctrl Pts',(-1.39178895487418,2.59736388069241,39.0061153245529));
#64673=CARTESIAN_POINT('Ctrl Pts',(-1.67231312023668,2.44705676576241,39.0234102163686));
#64674=CARTESIAN_POINT('Ctrl Pts',(-1.92609759023508,2.24683453296096,39.0407051081843));
#64675=CARTESIAN_POINT('Ctrl Pts',(-2.14341454569378,2.01149633185929,39.058));
#64676=CARTESIAN_POINT('Ctrl Pts',(-1.3799850048903,-1.93364773575773,1.50920942409982E-16));
#64677=CARTESIAN_POINT('Ctrl Pts',(-1.43331552021448,-1.9046528475011,1.23773392155628E-16));
#64678=CARTESIAN_POINT('Ctrl Pts',(-1.48535269583483,-1.87353821396734,
3.98761059851725E-16));
#64679=CARTESIAN_POINT('Ctrl Pts',(-1.53595409369946,-1.84033239929008,
4.04190569902596E-16));
#64680=CARTESIAN_POINT('Ctrl Pts',(-1.604148816696,-1.79558143529797,4.20181454187173E-16));
#64681=CARTESIAN_POINT('Ctrl Pts',(-1.66973713239356,-1.74703457128715,
1.05440529867363E-16));
#64682=CARTESIAN_POINT('Ctrl Pts',(-1.73263418143615,-1.69505071632867,
1.6306400674182E-16));
#64683=CARTESIAN_POINT('Ctrl Pts',(-1.76925523715114,-1.66478373754839,
1.96614588036684E-16));
#64684=CARTESIAN_POINT('Ctrl Pts',(-1.80496365153929,-1.63335064415344,
2.27902642928896E-16));
#64685=CARTESIAN_POINT('Ctrl Pts',(-1.83973953560591,-1.60081498486991,
2.22044604925031E-16));
#64686=CARTESIAN_POINT('Ctrl Pts',(-1.85332304959686,-1.5881065061369,2.19756446239185E-16));
#64687=CARTESIAN_POINT('Ctrl Pts',(-1.86676425940608,-1.57522975614015,
8.38314136196732E-16));
#64688=CARTESIAN_POINT('Ctrl Pts',(-1.88006186427144,-1.56218832508201,
8.74300631892311E-16));
#64689=CARTESIAN_POINT('Ctrl Pts',(-1.89032248524922,-1.55212537145611,
9.02068323622498E-16));
#64690=CARTESIAN_POINT('Ctrl Pts',(-1.90049621943027,-1.541965647287,6.20660402139477E-16));
#64691=CARTESIAN_POINT('Ctrl Pts',(-1.91057614643099,-1.53171754005162,
5.96744875736022E-16));
#64692=CARTESIAN_POINT('Ctrl Pts',(-1.97048681206202,-1.47080728485966,
4.54601474732619E-16));
#64693=CARTESIAN_POINT('Ctrl Pts',(-2.02715048831372,-1.40671555173584,
3.98298047110711E-16));
#64694=CARTESIAN_POINT('Ctrl Pts',(-2.08047392334861,-1.33983470059731,
4.44089209850063E-16));
#64695=CARTESIAN_POINT('Ctrl Pts',(-2.12704705061845,-1.28142041445932,
4.8408358846985E-16));
#64696=CARTESIAN_POINT('Ctrl Pts',(-2.17107203351392,-1.22087734268402,
2.12674681454476E-16));
#64697=CARTESIAN_POINT('Ctrl Pts',(-2.21247079422441,-1.15843840004056,
1.11022302462516E-16));
#64698=CARTESIAN_POINT('Ctrl Pts',(-2.23235211616136,-1.1284527507411,6.2204810399683E-17));
#64699=CARTESIAN_POINT('Ctrl Pts',(-2.25162750605615,-1.09802950060355,
6.56803286684185E-16));
#64700=CARTESIAN_POINT('Ctrl Pts',(-2.27028681415291,-1.06719266209682,
6.80011602582908E-16));
#64701=CARTESIAN_POINT('Ctrl Pts',(-2.28194103140091,-1.04793261165253,
6.94507035856293E-16));
#64702=CARTESIAN_POINT('Ctrl Pts',(-2.29335807228086,-1.02850535079581,
4.25198681390034E-16));
#64703=CARTESIAN_POINT('Ctrl Pts',(-2.30451762944014,-1.00894825067258,
4.02455846426619E-16));
#64704=CARTESIAN_POINT('Ctrl Pts',(-2.34844909879478,-0.931958444314987,
3.1292486029765E-16));
#64705=CARTESIAN_POINT('Ctrl Pts',(-2.38843712460482,-0.852891211717048,
-9.72483045965204E-17));
#64706=CARTESIAN_POINT('Ctrl Pts',(-2.42438430062746,-0.772143474284519,
-1.11022302462516E-16));
#64707=CARTESIAN_POINT('Ctrl Pts',(-2.46273528155508,-0.685996096914061,
-1.25717374173389E-16));
#64708=CARTESIAN_POINT('Ctrl Pts',(-2.49648798427418,-0.597935475902931,
5.41089475014295E-17));
#64709=CARTESIAN_POINT('Ctrl Pts',(-2.52548424257669,-0.50839454562273,
9.71445146547012E-17));
#64710=CARTESIAN_POINT('Ctrl Pts',(-2.54723143630358,-0.441238847912579,
1.29421190019655E-16));
#64711=CARTESIAN_POINT('Ctrl Pts',(-2.56630236075426,-0.373249325614532,
2.04320780950305E-16));
#64712=CARTESIAN_POINT('Ctrl Pts',(-2.58261145214044,-0.304595415567763,
1.66533453693773E-16));
#64713=CARTESIAN_POINT('Ctrl Pts',(-2.59484327068007,-0.253104983032686,
1.38192958251375E-16));
#64714=CARTESIAN_POINT('Ctrl Pts',(-2.60552123925938,-0.201240582374946,
1.5471389960288E-16));
#64715=CARTESIAN_POINT('Ctrl Pts',(-2.61460229316052,-0.149071024239955,
1.11022302462516E-16));
#64716=CARTESIAN_POINT('Ctrl Pts',(-2.61710931909131,-0.134668462988168,
9.89602699957222E-17));
#64717=CARTESIAN_POINT('Ctrl Pts',(-2.61949459731049,-0.12024263420335,
1.16564317379691E-16));
#64718=CARTESIAN_POINT('Ctrl Pts',(-2.62175713377957,-0.105794966493652,
1.11022302462516E-16));
#64719=CARTESIAN_POINT('Ctrl Pts',(-2.62409044163309,-0.090895380567459,
1.05306935171277E-16));
#64720=CARTESIAN_POINT('Ctrl Pts',(-2.6262918233183,-0.0759811813352656,
7.70470624417152E-17));
#64721=CARTESIAN_POINT('Ctrl Pts',(-2.62835986373368,-0.0610601137217946,
8.32667268468867E-17));
#64722=CARTESIAN_POINT('Ctrl Pts',(-2.64106933028015,0.0306396462349494,
1.21490649406612E-16));
#64723=CARTESIAN_POINT('Ctrl Pts',(-2.64875729230249,0.122667828184756,
-4.14607165871163E-17));
#64724=CARTESIAN_POINT('Ctrl Pts',(-2.65128955031192,0.214630073542032,
2.77555756156289E-17));
#64725=CARTESIAN_POINT('Ctrl Pts',(-2.6522874300278,0.250869374168836,5.50314431378172E-17));
#64726=CARTESIAN_POINT('Ctrl Pts',(-2.65248421901964,0.287098764165966,
-2.21971999331922E-16));
#64727=CARTESIAN_POINT('Ctrl Pts',(-2.65186976537464,0.323295201004453,
-1.94289029309402E-16));
#64728=CARTESIAN_POINT('Ctrl Pts',(-2.65036470656989,0.411955698680346,
-1.5423721520059E-16));
#64729=CARTESIAN_POINT('Ctrl Pts',(-2.64399624125764,0.500417941371144,
2.04597414681203E-16));
#64730=CARTESIAN_POINT('Ctrl Pts',(-2.63300888454151,0.588420542790668,
3.05311331771918E-16));
#64731=CARTESIAN_POINT('Ctrl Pts',(-2.62180125647045,0.678187394953273,
4.08044332391981E-16));
#64732=CARTESIAN_POINT('Ctrl Pts',(-2.60578758503461,0.767476722877809,
2.99792977684327E-16));
#64733=CARTESIAN_POINT('Ctrl Pts',(-2.58517343697646,0.856014478842741,
3.60822483003176E-16));
#64734=CARTESIAN_POINT('Ctrl Pts',(-2.58085119192177,0.874578519267442,
3.73618766255344E-16));
#64735=CARTESIAN_POINT('Ctrl Pts',(-2.57632651353202,0.893109507092954,
2.82887540844693E-16));
#64736=CARTESIAN_POINT('Ctrl Pts',(-2.57160101103184,0.911604886184466,
2.77555756156289E-16));
#64737=CARTESIAN_POINT('Ctrl Pts',(-2.56852674851983,0.923637395020121,
2.74087065622529E-16));
#64738=CARTESIAN_POINT('Ctrl Pts',(-2.56536774805562,0.935653628378105,
4.46031676548968E-16));
#64739=CARTESIAN_POINT('Ctrl Pts',(-2.5621271994808,0.94764335418908,4.44089209850063E-16));
#64740=CARTESIAN_POINT('Ctrl Pts',(-2.53799030793295,1.03694758923018,4.29620947158036E-16));
#64741=CARTESIAN_POINT('Ctrl Pts',(-2.5092973140664,1.1249247517235,-6.39262323456962E-17));
#64742=CARTESIAN_POINT('Ctrl Pts',(-2.47633894099238,1.21129265927984,-2.77555756156289E-17));
#64743=CARTESIAN_POINT('Ctrl Pts',(-2.44273663726984,1.29934799669203,9.12177238205123E-18));
#64744=CARTESIAN_POINT('Ctrl Pts',(-2.40470049237272,1.38573136318406,4.0019736649877E-16));
#64745=CARTESIAN_POINT('Ctrl Pts',(-2.36248309795556,1.47014709570666,4.71844785465692E-16));
#64746=CARTESIAN_POINT('Ctrl Pts',(-2.31988758449421,1.55531889564026,5.44133912760492E-16));
#64747=CARTESIAN_POINT('Ctrl Pts',(-2.27303530164497,1.63848852974037,3.07321867395325E-16));
#64748=CARTESIAN_POINT('Ctrl Pts',(-2.22213328141617,1.71934315364419,2.77555756156289E-16));
#64749=CARTESIAN_POINT('Ctrl Pts',(-2.19269440901531,1.76610493137767,2.60340707584599E-16));
#64750=CARTESIAN_POINT('Ctrl Pts',(-2.16190002568321,1.81209214358458,2.90467042585057E-16));
#64751=CARTESIAN_POINT('Ctrl Pts',(-2.12978288301151,1.85724110714762,2.77555756156289E-16));
#64752=CARTESIAN_POINT('Ctrl Pts',(-2.12127057434455,1.8692073619845,2.74133756369675E-16));
#64753=CARTESIAN_POINT('Ctrl Pts',(-2.11266398018409,1.88111653721518,-2.91895564785909E-16));
#64754=CARTESIAN_POINT('Ctrl Pts',(-2.1039679732652,1.89296153585496,-2.77555756156289E-16));
#64755=CARTESIAN_POINT('Ctrl Pts',(-2.04579977039086,1.97219356618236,-1.81635766058884E-16));
#64756=CARTESIAN_POINT('Ctrl Pts',(-1.98380145034343,2.0483310193058,-8.17499915602886E-17));
#64757=CARTESIAN_POINT('Ctrl Pts',(-1.91824824132448,2.1210661916555,0.));
#64758=CARTESIAN_POINT('Ctrl Pts',(-1.85247574695605,2.19404467410286,8.20234575848791E-17));
#64759=CARTESIAN_POINT('Ctrl Pts',(-1.78312414776718,2.26359897673652,7.51967810516288E-17));
#64760=CARTESIAN_POINT('Ctrl Pts',(-1.71042093086391,2.32940356785321,5.55111512312578E-17));
#64761=CARTESIAN_POINT('Ctrl Pts',(-1.63906649560604,2.39398735982976,3.61907269315061E-17));
#64762=CARTESIAN_POINT('Ctrl Pts',(-1.56448311831147,2.45496005537572,4.87793435120361E-16));
#64763=CARTESIAN_POINT('Ctrl Pts',(-1.48684438145143,2.51198742522398,4.9960036108132E-16));
#64764=CARTESIAN_POINT('Ctrl Pts',(-1.42291629818212,2.55894401668503,5.09322236739183E-16));
#64765=CARTESIAN_POINT('Ctrl Pts',(-1.35691584895575,2.60322544461548,2.73980132176117E-17));
#64766=CARTESIAN_POINT('Ctrl Pts',(-1.28892185405323,2.64462557919718,0.));
#64767=CARTESIAN_POINT('Origin',(0.,0.,0.));
#64768=CARTESIAN_POINT('Origin',(-1.44337567297407,-2.5,-6.));
#64769=CARTESIAN_POINT('',(-1.44337567297407,-2.5,-6.));
#64770=CARTESIAN_POINT('',(1.44337567297406,-2.5,-6.));
#64771=CARTESIAN_POINT('',(-0.721687836487033,-2.5,-6.));
#64772=CARTESIAN_POINT('',(-1.44337567297407,-2.5,-3.));
#64773=CARTESIAN_POINT('',(-1.44337567297407,-2.5,-6.));
#64774=CARTESIAN_POINT('',(1.44337567297406,-2.5,-3.));
#64775=CARTESIAN_POINT('',(-1.44337567297407,-2.5,-3.));
#64776=CARTESIAN_POINT('',(1.44337567297406,-2.5,-6.));
#64777=CARTESIAN_POINT('Origin',(-2.88675134594813,3.53525079574969E-16,
-6.));
#64778=CARTESIAN_POINT('',(-2.88675134594813,3.53525079574969E-16,-6.));
#64779=CARTESIAN_POINT('',(-2.52590742770461,-0.625,-6.));
#64780=CARTESIAN_POINT('',(-2.88675134594813,5.55111512312578E-16,-3.));
#64781=CARTESIAN_POINT('',(-2.88675134594813,3.53525079574969E-16,-6.));
#64782=CARTESIAN_POINT('',(-2.88675134594813,3.53525079574969E-16,-3.));
#64783=CARTESIAN_POINT('Origin',(-1.44337567297406,2.5,-6.));
#64784=CARTESIAN_POINT('',(-1.44337567297406,2.5,-6.));
#64785=CARTESIAN_POINT('',(-1.80421959121758,1.875,-6.));
#64786=CARTESIAN_POINT('',(-1.44337567297406,2.5,-3.));
#64787=CARTESIAN_POINT('',(-1.44337567297406,2.5,-6.));
#64788=CARTESIAN_POINT('',(-1.44337567297406,2.5,-3.));
#64789=CARTESIAN_POINT('Origin',(1.44337567297406,2.5,-6.));
#64790=CARTESIAN_POINT('',(1.44337567297406,2.5,-6.));
#64791=CARTESIAN_POINT('',(0.721687836487033,2.5,-6.));
#64792=CARTESIAN_POINT('',(1.44337567297406,2.5,-3.));
#64793=CARTESIAN_POINT('',(1.44337567297406,2.5,-6.));
#64794=CARTESIAN_POINT('',(1.44337567297406,2.5,-3.));
#64795=CARTESIAN_POINT('Origin',(2.88675134594813,0.,-6.));
#64796=CARTESIAN_POINT('',(2.88675134594813,0.,-6.));
#64797=CARTESIAN_POINT('',(2.52590742770461,0.625,-6.));
#64798=CARTESIAN_POINT('',(2.88675134594813,0.,-3.));
#64799=CARTESIAN_POINT('',(2.88675134594813,0.,-6.));
#64800=CARTESIAN_POINT('',(2.88675134594813,0.,-3.));
#64801=CARTESIAN_POINT('Origin',(1.44337567297406,-2.5,-6.));
#64802=CARTESIAN_POINT('',(1.80421959121758,-1.875,-6.));
#64803=CARTESIAN_POINT('',(1.44337567297406,-2.5,-3.));
#64804=CARTESIAN_POINT('Origin',(0.,0.,-3.));
#64805=CARTESIAN_POINT('Origin',(0.,0.,0.));
#64806=CARTESIAN_POINT('',(-5.,-6.12323399573677E-16,0.));
#64807=CARTESIAN_POINT('Origin',(0.,0.,0.));
#64808=CARTESIAN_POINT('Origin',(0.,0.,-6.));
#64809=CARTESIAN_POINT('',(-5.,-6.12323399573677E-16,-6.));
#64810=CARTESIAN_POINT('',(-5.,-6.12323399573677E-16,-6.));
#64811=CARTESIAN_POINT('Origin',(0.,0.,-6.));
#64812=CARTESIAN_POINT('Origin',(0.,0.,-6.));
#64813=CARTESIAN_POINT('Origin',(0.,0.,40.));
#69475=UNCERTAINTY_MEASURE_WITH_UNIT(LENGTH_MEASURE(0.01),#69492,
'DISTANCE_ACCURACY_VALUE',
'Maximum model space distance between geometric entities at asserted c
onnectivities');
#69478=UNCERTAINTY_MEASURE_WITH_UNIT(LENGTH_MEASURE(0.01),#69492,
'DISTANCE_ACCURACY_VALUE',
'Maximum model space distance between geometric entities at asserted c
onnectivities');
#69488=(
GEOMETRIC_REPRESENTATION_CONTEXT(3)
GLOBAL_UNCERTAINTY_ASSIGNED_CONTEXT((#69475))
GLOBAL_UNIT_ASSIGNED_CONTEXT((#69492,#69494,#69495))
REPRESENTATION_CONTEXT('','3D')
);
#69491=(
GEOMETRIC_REPRESENTATION_CONTEXT(3)
GLOBAL_UNCERTAINTY_ASSIGNED_CONTEXT((#69478))
GLOBAL_UNIT_ASSIGNED_CONTEXT((#69492,#69494,#69495))
REPRESENTATION_CONTEXT('','3D')
);
#69492=(
LENGTH_UNIT()
NAMED_UNIT(*)
SI_UNIT(.MILLI.,.METRE.)
);
#69494=(
NAMED_UNIT(*)
PLANE_ANGLE_UNIT()
SI_UNIT($,.RADIAN.)
);
#69495=(
NAMED_UNIT(*)
SI_UNIT($,.STERADIAN.)
SOLID_ANGLE_UNIT()
);
#69505=SHAPE_DEFINITION_REPRESENTATION(#69517,#69579);
#69517=PRODUCT_DEFINITION_SHAPE('',$,#69592);
#69579=SHAPE_REPRESENTATION('',(#15615),#69488);
#69582=PRODUCT_DEFINITION_CONTEXT('part definition',#69620,'design');
#69592=PRODUCT_DEFINITION('Socket head cap screw M6x40',
'Socket head cap screw M6x40',#69604,#69582);
#69604=PRODUCT_DEFINITION_FORMATION('',$,#69631);
#69620=APPLICATION_CONTEXT(
'Core Data for Automotive Mechanical Design Process');
#69621=PRODUCT_CONTEXT('part definition',#69620,'mechanical');
#69631=PRODUCT('Socket head cap screw M6x40',
'Socket head cap screw M6x40',$,(#69621));
#69640=PRESENTATION_STYLE_ASSIGNMENT((#69650));
#69650=SURFACE_STYLE_USAGE(.BOTH.,#69660);
#69660=SURFACE_SIDE_STYLE('',(#69670));
#69670=SURFACE_STYLE_FILL_AREA(#69680);
#69680=FILL_AREA_STYLE('Dark gray',(#69690));
#69690=FILL_AREA_STYLE_COLOUR('Dark gray',#69700);
#69700=COLOUR_RGB('Dark gray',0.250980392156863,0.282352941176471,0.32156862745098);
ENDSEC;
END-ISO-10303-21;
